ISO-10303-21;
HEADER;
/* Generated by software containing ST-Developer
 * from STEP Tools, Inc. (www.steptools.com) 
 */

FILE_DESCRIPTION(
/* description */ (''),
/* implementation_level */ '2;1');

FILE_NAME(
/* name */ 'V_Slot.step',
/* time_stamp */ '2026-10-19T01:17:59+06:00',
/* author */ (''),
/* organization */ (''),
/* preprocessor_version */ 'ST-DEVELOPER v20.2',
/* originating_system */ 'Autodesk Translation Framework v15.15.0.0',
/* authorisation */ '');

FILE_SCHEMA (('AUTOMOTIVE_DESIGN { 1 0 10303 214 3 1 1 }'));
ENDSEC;

DATA;
#10=MECHANICAL_DESIGN_GEOMETRIC_PRESENTATION_REPRESENTATION('',(#747),#48369);
#616=SHAPE_REPRESENTATION_RELATIONSHIP('SRR','None',#48416,#627);
#627=ADVANCED_BREP_SHAPE_REPRESENTATION('',(#773),#48361);
#659=FACE_BOUND('',#2914,.T.);
#660=FACE_BOUND('',#2915,.T.);
#661=FACE_BOUND('',#2916,.T.);
#662=FACE_BOUND('',#2917,.T.);
#663=FACE_BOUND('',#2918,.T.);
#664=FACE_BOUND('',#2919,.T.);
#665=FACE_BOUND('',#2920,.T.);
#666=FACE_BOUND('',#2921,.T.);
#667=FACE_BOUND('',#2922,.T.);
#668=FACE_BOUND('',#2923,.T.);
#669=FACE_BOUND('',#2924,.T.);
#670=FACE_BOUND('',#2925,.T.);
#671=FACE_BOUND('',#2926,.T.);
#672=FACE_BOUND('',#2966,.T.);
#673=FACE_BOUND('',#2967,.T.);
#674=FACE_BOUND('',#2968,.T.);
#675=FACE_BOUND('',#2969,.T.);
#676=FACE_BOUND('',#2970,.T.);
#677=FACE_BOUND('',#2971,.T.);
#678=FACE_BOUND('',#2972,.T.);
#679=FACE_BOUND('',#2973,.T.);
#680=FACE_BOUND('',#2974,.T.);
#681=FACE_BOUND('',#2975,.T.);
#682=FACE_BOUND('',#2976,.T.);
#683=FACE_BOUND('',#2977,.T.);
#684=FACE_BOUND('',#2978,.T.);
#747=STYLED_ITEM('',(#48531),#773);
#773=MANIFOLD_SOLID_BREP('V_Slot',#20126);
#897=CYLINDRICAL_SURFACE('',#21114,3.25);
#898=CYLINDRICAL_SURFACE('',#21125,0.499999999999999);
#899=CYLINDRICAL_SURFACE('',#21129,0.499999999999998);
#900=CYLINDRICAL_SURFACE('',#21143,0.499999999999998);
#901=CYLINDRICAL_SURFACE('',#21147,0.499999999999999);
#902=CYLINDRICAL_SURFACE('',#21159,2.);
#903=CYLINDRICAL_SURFACE('',#21170,0.499999999999999);
#904=CYLINDRICAL_SURFACE('',#21174,0.499999999999998);
#905=CYLINDRICAL_SURFACE('',#21189,3.25);
#906=CYLINDRICAL_SURFACE('',#21193,0.499999999999998);
#907=CYLINDRICAL_SURFACE('',#21197,0.499999999999999);
#908=CYLINDRICAL_SURFACE('',#21209,2.);
#909=CYLINDRICAL_SURFACE('',#21255,3.25);
#910=CYLINDRICAL_SURFACE('',#21302,3.25);
#911=CYLINDRICAL_SURFACE('',#21314,0.499999999999999);
#912=CYLINDRICAL_SURFACE('',#21318,0.499999999999998);
#913=CYLINDRICAL_SURFACE('',#21332,0.499999999999998);
#914=CYLINDRICAL_SURFACE('',#21336,0.499999999999999);
#915=CYLINDRICAL_SURFACE('',#21348,2.);
#916=CYLINDRICAL_SURFACE('',#21366,0.499999999999999);
#917=CYLINDRICAL_SURFACE('',#21369,0.499999999999998);
#918=CYLINDRICAL_SURFACE('',#21383,3.25);
#919=CYLINDRICAL_SURFACE('',#21386,0.499999999999998);
#920=CYLINDRICAL_SURFACE('',#21389,0.499999999999999);
#921=CYLINDRICAL_SURFACE('',#21400,2.);
#1606=FACE_OUTER_BOUND('',#2674,.T.);
#1607=FACE_OUTER_BOUND('',#2675,.T.);
#1608=FACE_OUTER_BOUND('',#2676,.T.);
#1609=FACE_OUTER_BOUND('',#2677,.T.);
#1610=FACE_OUTER_BOUND('',#2678,.T.);
#1611=FACE_OUTER_BOUND('',#2679,.T.);
#1612=FACE_OUTER_BOUND('',#2680,.T.);
#1613=FACE_OUTER_BOUND('',#2681,.T.);
#1614=FACE_OUTER_BOUND('',#2682,.T.);
#1615=FACE_OUTER_BOUND('',#2683,.T.);
#1616=FACE_OUTER_BOUND('',#2684,.T.);
#1617=FACE_OUTER_BOUND('',#2685,.T.);
#1618=FACE_OUTER_BOUND('',#2686,.T.);
#1619=FACE_OUTER_BOUND('',#2687,.T.);
#1620=FACE_OUTER_BOUND('',#2688,.T.);
#1621=FACE_OUTER_BOUND('',#2689,.T.);
#1622=FACE_OUTER_BOUND('',#2690,.T.);
#1623=FACE_OUTER_BOUND('',#2691,.T.);
#1624=FACE_OUTER_BOUND('',#2692,.T.);
#1625=FACE_OUTER_BOUND('',#2693,.T.);
#1626=FACE_OUTER_BOUND('',#2694,.T.);
#1627=FACE_OUTER_BOUND('',#2695,.T.);
#1628=FACE_OUTER_BOUND('',#2696,.T.);
#1629=FACE_OUTER_BOUND('',#2697,.T.);
#1630=FACE_OUTER_BOUND('',#2698,.T.);
#1631=FACE_OUTER_BOUND('',#2699,.T.);
#1632=FACE_OUTER_BOUND('',#2700,.T.);
#1633=FACE_OUTER_BOUND('',#2701,.T.);
#1634=FACE_OUTER_BOUND('',#2702,.T.);
#1635=FACE_OUTER_BOUND('',#2703,.T.);
#1636=FACE_OUTER_BOUND('',#2704,.T.);
#1637=FACE_OUTER_BOUND('',#2705,.T.);
#1638=FACE_OUTER_BOUND('',#2706,.T.);
#1639=FACE_OUTER_BOUND('',#2707,.T.);
#1640=FACE_OUTER_BOUND('',#2708,.T.);
#1641=FACE_OUTER_BOUND('',#2709,.T.);
#1642=FACE_OUTER_BOUND('',#2710,.T.);
#1643=FACE_OUTER_BOUND('',#2711,.T.);
#1644=FACE_OUTER_BOUND('',#2712,.T.);
#1645=FACE_OUTER_BOUND('',#2713,.T.);
#1646=FACE_OUTER_BOUND('',#2714,.T.);
#1647=FACE_OUTER_BOUND('',#2715,.T.);
#1648=FACE_OUTER_BOUND('',#2716,.T.);
#1649=FACE_OUTER_BOUND('',#2717,.T.);
#1650=FACE_OUTER_BOUND('',#2718,.T.);
#1651=FACE_OUTER_BOUND('',#2719,.T.);
#1652=FACE_OUTER_BOUND('',#2720,.T.);
#1653=FACE_OUTER_BOUND('',#2721,.T.);
#1654=FACE_OUTER_BOUND('',#2722,.T.);
#1655=FACE_OUTER_BOUND('',#2723,.T.);
#1656=FACE_OUTER_BOUND('',#2724,.T.);
#1657=FACE_OUTER_BOUND('',#2725,.T.);
#1658=FACE_OUTER_BOUND('',#2726,.T.);
#1659=FACE_OUTER_BOUND('',#2727,.T.);
#1660=FACE_OUTER_BOUND('',#2728,.T.);
#1661=FACE_OUTER_BOUND('',#2729,.T.);
#1662=FACE_OUTER_BOUND('',#2730,.T.);
#1663=FACE_OUTER_BOUND('',#2731,.T.);
#1664=FACE_OUTER_BOUND('',#2732,.T.);
#1665=FACE_OUTER_BOUND('',#2733,.T.);
#1666=FACE_OUTER_BOUND('',#2734,.T.);
#1667=FACE_OUTER_BOUND('',#2735,.T.);
#1668=FACE_OUTER_BOUND('',#2736,.T.);
#1669=FACE_OUTER_BOUND('',#2737,.T.);
#1670=FACE_OUTER_BOUND('',#2738,.T.);
#1671=FACE_OUTER_BOUND('',#2739,.T.);
#1672=FACE_OUTER_BOUND('',#2740,.T.);
#1673=FACE_OUTER_BOUND('',#2741,.T.);
#1674=FACE_OUTER_BOUND('',#2742,.T.);
#1675=FACE_OUTER_BOUND('',#2743,.T.);
#1676=FACE_OUTER_BOUND('',#2744,.T.);
#1677=FACE_OUTER_BOUND('',#2745,.T.);
#1678=FACE_OUTER_BOUND('',#2746,.T.);
#1679=FACE_OUTER_BOUND('',#2747,.T.);
#1680=FACE_OUTER_BOUND('',#2748,.T.);
#1681=FACE_OUTER_BOUND('',#2749,.T.);
#1682=FACE_OUTER_BOUND('',#2750,.T.);
#1683=FACE_OUTER_BOUND('',#2751,.T.);
#1684=FACE_OUTER_BOUND('',#2752,.T.);
#1685=FACE_OUTER_BOUND('',#2753,.T.);
#1686=FACE_OUTER_BOUND('',#2754,.T.);
#1687=FACE_OUTER_BOUND('',#2755,.T.);
#1688=FACE_OUTER_BOUND('',#2756,.T.);
#1689=FACE_OUTER_BOUND('',#2757,.T.);
#1690=FACE_OUTER_BOUND('',#2758,.T.);
#1691=FACE_OUTER_BOUND('',#2759,.T.);
#1692=FACE_OUTER_BOUND('',#2760,.T.);
#1693=FACE_OUTER_BOUND('',#2761,.T.);
#1694=FACE_OUTER_BOUND('',#2762,.T.);
#1695=FACE_OUTER_BOUND('',#2763,.T.);
#1696=FACE_OUTER_BOUND('',#2764,.T.);
#1697=FACE_OUTER_BOUND('',#2765,.T.);
#1698=FACE_OUTER_BOUND('',#2766,.T.);
#1699=FACE_OUTER_BOUND('',#2767,.T.);
#1700=FACE_OUTER_BOUND('',#2768,.T.);
#1701=FACE_OUTER_BOUND('',#2769,.T.);
#1702=FACE_OUTER_BOUND('',#2770,.T.);
#1703=FACE_OUTER_BOUND('',#2771,.T.);
#1704=FACE_OUTER_BOUND('',#2772,.T.);
#1705=FACE_OUTER_BOUND('',#2773,.T.);
#1706=FACE_OUTER_BOUND('',#2774,.T.);
#1707=FACE_OUTER_BOUND('',#2775,.T.);
#1708=FACE_OUTER_BOUND('',#2776,.T.);
#1709=FACE_OUTER_BOUND('',#2777,.T.);
#1710=FACE_OUTER_BOUND('',#2778,.T.);
#1711=FACE_OUTER_BOUND('',#2779,.T.);
#1712=FACE_OUTER_BOUND('',#2780,.T.);
#1713=FACE_OUTER_BOUND('',#2781,.T.);
#1714=FACE_OUTER_BOUND('',#2782,.T.);
#1715=FACE_OUTER_BOUND('',#2783,.T.);
#1716=FACE_OUTER_BOUND('',#2784,.T.);
#1717=FACE_OUTER_BOUND('',#2785,.T.);
#1718=FACE_OUTER_BOUND('',#2786,.T.);
#1719=FACE_OUTER_BOUND('',#2787,.T.);
#1720=FACE_OUTER_BOUND('',#2788,.T.);
#1721=FACE_OUTER_BOUND('',#2789,.T.);
#1722=FACE_OUTER_BOUND('',#2790,.T.);
#1723=FACE_OUTER_BOUND('',#2791,.T.);
#1724=FACE_OUTER_BOUND('',#2792,.T.);
#1725=FACE_OUTER_BOUND('',#2793,.T.);
#1726=FACE_OUTER_BOUND('',#2794,.T.);
#1727=FACE_OUTER_BOUND('',#2795,.T.);
#1728=FACE_OUTER_BOUND('',#2796,.T.);
#1729=FACE_OUTER_BOUND('',#2797,.T.);
#1730=FACE_OUTER_BOUND('',#2798,.T.);
#1731=FACE_OUTER_BOUND('',#2799,.T.);
#1732=FACE_OUTER_BOUND('',#2800,.T.);
#1733=FACE_OUTER_BOUND('',#2801,.T.);
#1734=FACE_OUTER_BOUND('',#2802,.T.);
#1735=FACE_OUTER_BOUND('',#2803,.T.);
#1736=FACE_OUTER_BOUND('',#2804,.T.);
#1737=FACE_OUTER_BOUND('',#2805,.T.);
#1738=FACE_OUTER_BOUND('',#2806,.T.);
#1739=FACE_OUTER_BOUND('',#2807,.T.);
#1740=FACE_OUTER_BOUND('',#2808,.T.);
#1741=FACE_OUTER_BOUND('',#2809,.T.);
#1742=FACE_OUTER_BOUND('',#2810,.T.);
#1743=FACE_OUTER_BOUND('',#2811,.T.);
#1744=FACE_OUTER_BOUND('',#2812,.T.);
#1745=FACE_OUTER_BOUND('',#2813,.T.);
#1746=FACE_OUTER_BOUND('',#2814,.T.);
#1747=FACE_OUTER_BOUND('',#2815,.T.);
#1748=FACE_OUTER_BOUND('',#2816,.T.);
#1749=FACE_OUTER_BOUND('',#2817,.T.);
#1750=FACE_OUTER_BOUND('',#2818,.T.);
#1751=FACE_OUTER_BOUND('',#2819,.T.);
#1752=FACE_OUTER_BOUND('',#2820,.T.);
#1753=FACE_OUTER_BOUND('',#2821,.T.);
#1754=FACE_OUTER_BOUND('',#2822,.T.);
#1755=FACE_OUTER_BOUND('',#2823,.T.);
#1756=FACE_OUTER_BOUND('',#2824,.T.);
#1757=FACE_OUTER_BOUND('',#2825,.T.);
#1758=FACE_OUTER_BOUND('',#2826,.T.);
#1759=FACE_OUTER_BOUND('',#2827,.T.);
#1760=FACE_OUTER_BOUND('',#2828,.T.);
#1761=FACE_OUTER_BOUND('',#2829,.T.);
#1762=FACE_OUTER_BOUND('',#2830,.T.);
#1763=FACE_OUTER_BOUND('',#2831,.T.);
#1764=FACE_OUTER_BOUND('',#2832,.T.);
#1765=FACE_OUTER_BOUND('',#2833,.T.);
#1766=FACE_OUTER_BOUND('',#2834,.T.);
#1767=FACE_OUTER_BOUND('',#2835,.T.);
#1768=FACE_OUTER_BOUND('',#2836,.T.);
#1769=FACE_OUTER_BOUND('',#2837,.T.);
#1770=FACE_OUTER_BOUND('',#2838,.T.);
#1771=FACE_OUTER_BOUND('',#2839,.T.);
#1772=FACE_OUTER_BOUND('',#2840,.T.);
#1773=FACE_OUTER_BOUND('',#2841,.T.);
#1774=FACE_OUTER_BOUND('',#2842,.T.);
#1775=FACE_OUTER_BOUND('',#2843,.T.);
#1776=FACE_OUTER_BOUND('',#2844,.T.);
#1777=FACE_OUTER_BOUND('',#2845,.T.);
#1778=FACE_OUTER_BOUND('',#2846,.T.);
#1779=FACE_OUTER_BOUND('',#2847,.T.);
#1780=FACE_OUTER_BOUND('',#2848,.T.);
#1781=FACE_OUTER_BOUND('',#2849,.T.);
#1782=FACE_OUTER_BOUND('',#2850,.T.);
#1783=FACE_OUTER_BOUND('',#2851,.T.);
#1784=FACE_OUTER_BOUND('',#2852,.T.);
#1785=FACE_OUTER_BOUND('',#2853,.T.);
#1786=FACE_OUTER_BOUND('',#2854,.T.);
#1787=FACE_OUTER_BOUND('',#2855,.T.);
#1788=FACE_OUTER_BOUND('',#2856,.T.);
#1789=FACE_OUTER_BOUND('',#2857,.T.);
#1790=FACE_OUTER_BOUND('',#2858,.T.);
#1791=FACE_OUTER_BOUND('',#2859,.T.);
#1792=FACE_OUTER_BOUND('',#2860,.T.);
#1793=FACE_OUTER_BOUND('',#2861,.T.);
#1794=FACE_OUTER_BOUND('',#2862,.T.);
#1795=FACE_OUTER_BOUND('',#2863,.T.);
#1796=FACE_OUTER_BOUND('',#2864,.T.);
#1797=FACE_OUTER_BOUND('',#2865,.T.);
#1798=FACE_OUTER_BOUND('',#2866,.T.);
#1799=FACE_OUTER_BOUND('',#2867,.T.);
#1800=FACE_OUTER_BOUND('',#2868,.T.);
#1801=FACE_OUTER_BOUND('',#2869,.T.);
#1802=FACE_OUTER_BOUND('',#2870,.T.);
#1803=FACE_OUTER_BOUND('',#2871,.T.);
#1804=FACE_OUTER_BOUND('',#2872,.T.);
#1805=FACE_OUTER_BOUND('',#2873,.T.);
#1806=FACE_OUTER_BOUND('',#2874,.T.);
#1807=FACE_OUTER_BOUND('',#2875,.T.);
#1808=FACE_OUTER_BOUND('',#2876,.T.);
#1809=FACE_OUTER_BOUND('',#2877,.T.);
#1810=FACE_OUTER_BOUND('',#2878,.T.);
#1811=FACE_OUTER_BOUND('',#2879,.T.);
#1812=FACE_OUTER_BOUND('',#2880,.T.);
#1813=FACE_OUTER_BOUND('',#2881,.T.);
#1814=FACE_OUTER_BOUND('',#2882,.T.);
#1815=FACE_OUTER_BOUND('',#2883,.T.);
#1816=FACE_OUTER_BOUND('',#2884,.T.);
#1817=FACE_OUTER_BOUND('',#2885,.T.);
#1818=FACE_OUTER_BOUND('',#2886,.T.);
#1819=FACE_OUTER_BOUND('',#2887,.T.);
#1820=FACE_OUTER_BOUND('',#2888,.T.);
#1821=FACE_OUTER_BOUND('',#2889,.T.);
#1822=FACE_OUTER_BOUND('',#2890,.T.);
#1823=FACE_OUTER_BOUND('',#2891,.T.);
#1824=FACE_OUTER_BOUND('',#2892,.T.);
#1825=FACE_OUTER_BOUND('',#2893,.T.);
#1826=FACE_OUTER_BOUND('',#2894,.T.);
#1827=FACE_OUTER_BOUND('',#2895,.T.);
#1828=FACE_OUTER_BOUND('',#2896,.T.);
#1829=FACE_OUTER_BOUND('',#2897,.T.);
#1830=FACE_OUTER_BOUND('',#2898,.T.);
#1831=FACE_OUTER_BOUND('',#2899,.T.);
#1832=FACE_OUTER_BOUND('',#2900,.T.);
#1833=FACE_OUTER_BOUND('',#2901,.T.);
#1834=FACE_OUTER_BOUND('',#2902,.T.);
#1835=FACE_OUTER_BOUND('',#2903,.T.);
#1836=FACE_OUTER_BOUND('',#2904,.T.);
#1837=FACE_OUTER_BOUND('',#2905,.T.);
#1838=FACE_OUTER_BOUND('',#2906,.T.);
#1839=FACE_OUTER_BOUND('',#2907,.T.);
#1840=FACE_OUTER_BOUND('',#2908,.T.);
#1841=FACE_OUTER_BOUND('',#2909,.T.);
#1842=FACE_OUTER_BOUND('',#2910,.T.);
#1843=FACE_OUTER_BOUND('',#2911,.T.);
#1844=FACE_OUTER_BOUND('',#2912,.T.);
#1845=FACE_OUTER_BOUND('',#2913,.T.);
#1846=FACE_OUTER_BOUND('',#2927,.T.);
#1847=FACE_OUTER_BOUND('',#2928,.T.);
#1848=FACE_OUTER_BOUND('',#2929,.T.);
#1849=FACE_OUTER_BOUND('',#2930,.T.);
#1850=FACE_OUTER_BOUND('',#2931,.T.);
#1851=FACE_OUTER_BOUND('',#2932,.T.);
#1852=FACE_OUTER_BOUND('',#2933,.T.);
#1853=FACE_OUTER_BOUND('',#2934,.T.);
#1854=FACE_OUTER_BOUND('',#2935,.T.);
#1855=FACE_OUTER_BOUND('',#2936,.T.);
#1856=FACE_OUTER_BOUND('',#2937,.T.);
#1857=FACE_OUTER_BOUND('',#2938,.T.);
#1858=FACE_OUTER_BOUND('',#2939,.T.);
#1859=FACE_OUTER_BOUND('',#2940,.T.);
#1860=FACE_OUTER_BOUND('',#2941,.T.);
#1861=FACE_OUTER_BOUND('',#2942,.T.);
#1862=FACE_OUTER_BOUND('',#2943,.T.);
#1863=FACE_OUTER_BOUND('',#2944,.T.);
#1864=FACE_OUTER_BOUND('',#2945,.T.);
#1865=FACE_OUTER_BOUND('',#2946,.T.);
#1866=FACE_OUTER_BOUND('',#2947,.T.);
#1867=FACE_OUTER_BOUND('',#2948,.T.);
#1868=FACE_OUTER_BOUND('',#2949,.T.);
#1869=FACE_OUTER_BOUND('',#2950,.T.);
#1870=FACE_OUTER_BOUND('',#2951,.T.);
#1871=FACE_OUTER_BOUND('',#2952,.T.);
#1872=FACE_OUTER_BOUND('',#2953,.T.);
#1873=FACE_OUTER_BOUND('',#2954,.T.);
#1874=FACE_OUTER_BOUND('',#2955,.T.);
#1875=FACE_OUTER_BOUND('',#2956,.T.);
#1876=FACE_OUTER_BOUND('',#2957,.T.);
#1877=FACE_OUTER_BOUND('',#2958,.T.);
#1878=FACE_OUTER_BOUND('',#2959,.T.);
#1879=FACE_OUTER_BOUND('',#2960,.T.);
#1880=FACE_OUTER_BOUND('',#2961,.T.);
#1881=FACE_OUTER_BOUND('',#2962,.T.);
#1882=FACE_OUTER_BOUND('',#2963,.T.);
#1883=FACE_OUTER_BOUND('',#2964,.T.);
#1884=FACE_OUTER_BOUND('',#2965,.T.);
#2674=EDGE_LOOP('',(#14789,#14790,#14791,#14792));
#2675=EDGE_LOOP('',(#14793,#14794,#14795,#14796));
#2676=EDGE_LOOP('',(#14797,#14798,#14799,#14800));
#2677=EDGE_LOOP('',(#14801,#14802,#14803,#14804));
#2678=EDGE_LOOP('',(#14805,#14806,#14807,#14808));
#2679=EDGE_LOOP('',(#14809,#14810,#14811,#14812));
#2680=EDGE_LOOP('',(#14813,#14814,#14815,#14816));
#2681=EDGE_LOOP('',(#14817,#14818,#14819,#14820));
#2682=EDGE_LOOP('',(#14821,#14822,#14823,#14824));
#2683=EDGE_LOOP('',(#14825,#14826,#14827,#14828));
#2684=EDGE_LOOP('',(#14829,#14830,#14831,#14832));
#2685=EDGE_LOOP('',(#14833,#14834,#14835,#14836));
#2686=EDGE_LOOP('',(#14837,#14838,#14839,#14840));
#2687=EDGE_LOOP('',(#14841,#14842,#14843,#14844));
#2688=EDGE_LOOP('',(#14845,#14846,#14847,#14848));
#2689=EDGE_LOOP('',(#14849,#14850,#14851,#14852));
#2690=EDGE_LOOP('',(#14853,#14854,#14855,#14856));
#2691=EDGE_LOOP('',(#14857,#14858,#14859,#14860));
#2692=EDGE_LOOP('',(#14861,#14862,#14863,#14864));
#2693=EDGE_LOOP('',(#14865,#14866,#14867,#14868));
#2694=EDGE_LOOP('',(#14869,#14870,#14871,#14872));
#2695=EDGE_LOOP('',(#14873,#14874,#14875,#14876));
#2696=EDGE_LOOP('',(#14877,#14878,#14879,#14880));
#2697=EDGE_LOOP('',(#14881,#14882,#14883,#14884));
#2698=EDGE_LOOP('',(#14885,#14886,#14887,#14888));
#2699=EDGE_LOOP('',(#14889,#14890,#14891,#14892));
#2700=EDGE_LOOP('',(#14893,#14894,#14895,#14896));
#2701=EDGE_LOOP('',(#14897,#14898,#14899,#14900));
#2702=EDGE_LOOP('',(#14901,#14902,#14903,#14904));
#2703=EDGE_LOOP('',(#14905,#14906,#14907,#14908));
#2704=EDGE_LOOP('',(#14909,#14910,#14911,#14912));
#2705=EDGE_LOOP('',(#14913,#14914,#14915,#14916));
#2706=EDGE_LOOP('',(#14917,#14918,#14919,#14920));
#2707=EDGE_LOOP('',(#14921,#14922,#14923,#14924));
#2708=EDGE_LOOP('',(#14925,#14926,#14927,#14928));
#2709=EDGE_LOOP('',(#14929,#14930,#14931,#14932));
#2710=EDGE_LOOP('',(#14933,#14934,#14935,#14936));
#2711=EDGE_LOOP('',(#14937,#14938,#14939,#14940));
#2712=EDGE_LOOP('',(#14941,#14942,#14943,#14944));
#2713=EDGE_LOOP('',(#14945,#14946,#14947,#14948));
#2714=EDGE_LOOP('',(#14949,#14950,#14951,#14952));
#2715=EDGE_LOOP('',(#14953,#14954,#14955,#14956));
#2716=EDGE_LOOP('',(#14957,#14958,#14959,#14960));
#2717=EDGE_LOOP('',(#14961,#14962,#14963,#14964));
#2718=EDGE_LOOP('',(#14965,#14966,#14967,#14968));
#2719=EDGE_LOOP('',(#14969,#14970,#14971,#14972));
#2720=EDGE_LOOP('',(#14973,#14974,#14975,#14976));
#2721=EDGE_LOOP('',(#14977,#14978,#14979,#14980));
#2722=EDGE_LOOP('',(#14981,#14982,#14983,#14984));
#2723=EDGE_LOOP('',(#14985,#14986,#14987,#14988));
#2724=EDGE_LOOP('',(#14989,#14990,#14991,#14992));
#2725=EDGE_LOOP('',(#14993,#14994,#14995,#14996));
#2726=EDGE_LOOP('',(#14997,#14998,#14999,#15000));
#2727=EDGE_LOOP('',(#15001,#15002,#15003,#15004));
#2728=EDGE_LOOP('',(#15005,#15006,#15007,#15008));
#2729=EDGE_LOOP('',(#15009,#15010,#15011,#15012));
#2730=EDGE_LOOP('',(#15013,#15014,#15015,#15016));
#2731=EDGE_LOOP('',(#15017,#15018,#15019,#15020));
#2732=EDGE_LOOP('',(#15021,#15022,#15023,#15024));
#2733=EDGE_LOOP('',(#15025,#15026,#15027,#15028));
#2734=EDGE_LOOP('',(#15029,#15030,#15031,#15032));
#2735=EDGE_LOOP('',(#15033,#15034,#15035,#15036));
#2736=EDGE_LOOP('',(#15037,#15038,#15039,#15040));
#2737=EDGE_LOOP('',(#15041,#15042,#15043,#15044));
#2738=EDGE_LOOP('',(#15045,#15046,#15047,#15048));
#2739=EDGE_LOOP('',(#15049,#15050,#15051,#15052));
#2740=EDGE_LOOP('',(#15053,#15054,#15055,#15056));
#2741=EDGE_LOOP('',(#15057,#15058,#15059,#15060));
#2742=EDGE_LOOP('',(#15061,#15062,#15063,#15064));
#2743=EDGE_LOOP('',(#15065,#15066,#15067,#15068));
#2744=EDGE_LOOP('',(#15069,#15070,#15071,#15072));
#2745=EDGE_LOOP('',(#15073,#15074,#15075,#15076));
#2746=EDGE_LOOP('',(#15077,#15078,#15079,#15080));
#2747=EDGE_LOOP('',(#15081,#15082,#15083,#15084));
#2748=EDGE_LOOP('',(#15085,#15086,#15087,#15088));
#2749=EDGE_LOOP('',(#15089,#15090,#15091,#15092));
#2750=EDGE_LOOP('',(#15093,#15094,#15095,#15096));
#2751=EDGE_LOOP('',(#15097,#15098,#15099,#15100));
#2752=EDGE_LOOP('',(#15101,#15102,#15103,#15104));
#2753=EDGE_LOOP('',(#15105,#15106,#15107,#15108));
#2754=EDGE_LOOP('',(#15109,#15110,#15111,#15112));
#2755=EDGE_LOOP('',(#15113,#15114,#15115,#15116));
#2756=EDGE_LOOP('',(#15117,#15118,#15119,#15120));
#2757=EDGE_LOOP('',(#15121,#15122,#15123,#15124));
#2758=EDGE_LOOP('',(#15125,#15126,#15127,#15128));
#2759=EDGE_LOOP('',(#15129,#15130,#15131,#15132));
#2760=EDGE_LOOP('',(#15133,#15134,#15135,#15136));
#2761=EDGE_LOOP('',(#15137,#15138,#15139,#15140));
#2762=EDGE_LOOP('',(#15141,#15142,#15143,#15144));
#2763=EDGE_LOOP('',(#15145,#15146,#15147,#15148));
#2764=EDGE_LOOP('',(#15149,#15150,#15151,#15152));
#2765=EDGE_LOOP('',(#15153,#15154,#15155,#15156));
#2766=EDGE_LOOP('',(#15157,#15158,#15159,#15160));
#2767=EDGE_LOOP('',(#15161,#15162,#15163,#15164));
#2768=EDGE_LOOP('',(#15165,#15166,#15167,#15168));
#2769=EDGE_LOOP('',(#15169,#15170,#15171,#15172));
#2770=EDGE_LOOP('',(#15173,#15174,#15175,#15176));
#2771=EDGE_LOOP('',(#15177,#15178,#15179,#15180));
#2772=EDGE_LOOP('',(#15181,#15182,#15183,#15184));
#2773=EDGE_LOOP('',(#15185,#15186,#15187,#15188));
#2774=EDGE_LOOP('',(#15189,#15190,#15191,#15192));
#2775=EDGE_LOOP('',(#15193,#15194,#15195,#15196));
#2776=EDGE_LOOP('',(#15197,#15198,#15199,#15200));
#2777=EDGE_LOOP('',(#15201,#15202,#15203,#15204));
#2778=EDGE_LOOP('',(#15205,#15206,#15207,#15208));
#2779=EDGE_LOOP('',(#15209,#15210,#15211,#15212));
#2780=EDGE_LOOP('',(#15213,#15214,#15215,#15216));
#2781=EDGE_LOOP('',(#15217,#15218,#15219,#15220));
#2782=EDGE_LOOP('',(#15221,#15222,#15223,#15224));
#2783=EDGE_LOOP('',(#15225,#15226,#15227,#15228));
#2784=EDGE_LOOP('',(#15229,#15230,#15231,#15232));
#2785=EDGE_LOOP('',(#15233,#15234,#15235,#15236));
#2786=EDGE_LOOP('',(#15237,#15238,#15239,#15240));
#2787=EDGE_LOOP('',(#15241,#15242,#15243,#15244));
#2788=EDGE_LOOP('',(#15245,#15246,#15247,#15248));
#2789=EDGE_LOOP('',(#15249,#15250,#15251,#15252));
#2790=EDGE_LOOP('',(#15253,#15254,#15255,#15256));
#2791=EDGE_LOOP('',(#15257,#15258,#15259,#15260));
#2792=EDGE_LOOP('',(#15261,#15262,#15263,#15264));
#2793=EDGE_LOOP('',(#15265,#15266,#15267,#15268));
#2794=EDGE_LOOP('',(#15269,#15270,#15271,#15272));
#2795=EDGE_LOOP('',(#15273,#15274,#15275,#15276));
#2796=EDGE_LOOP('',(#15277,#15278,#15279,#15280));
#2797=EDGE_LOOP('',(#15281,#15282,#15283,#15284));
#2798=EDGE_LOOP('',(#15285,#15286,#15287,#15288));
#2799=EDGE_LOOP('',(#15289,#15290,#15291,#15292));
#2800=EDGE_LOOP('',(#15293,#15294,#15295,#15296));
#2801=EDGE_LOOP('',(#15297,#15298,#15299,#15300));
#2802=EDGE_LOOP('',(#15301,#15302,#15303,#15304));
#2803=EDGE_LOOP('',(#15305,#15306,#15307,#15308));
#2804=EDGE_LOOP('',(#15309,#15310,#15311,#15312));
#2805=EDGE_LOOP('',(#15313,#15314,#15315,#15316));
#2806=EDGE_LOOP('',(#15317,#15318,#15319,#15320));
#2807=EDGE_LOOP('',(#15321,#15322,#15323,#15324));
#2808=EDGE_LOOP('',(#15325,#15326,#15327,#15328));
#2809=EDGE_LOOP('',(#15329,#15330,#15331,#15332));
#2810=EDGE_LOOP('',(#15333,#15334,#15335,#15336));
#2811=EDGE_LOOP('',(#15337,#15338,#15339,#15340));
#2812=EDGE_LOOP('',(#15341,#15342,#15343,#15344));
#2813=EDGE_LOOP('',(#15345,#15346,#15347,#15348));
#2814=EDGE_LOOP('',(#15349,#15350,#15351,#15352));
#2815=EDGE_LOOP('',(#15353,#15354,#15355,#15356));
#2816=EDGE_LOOP('',(#15357,#15358,#15359,#15360));
#2817=EDGE_LOOP('',(#15361,#15362,#15363,#15364));
#2818=EDGE_LOOP('',(#15365,#15366,#15367,#15368));
#2819=EDGE_LOOP('',(#15369,#15370,#15371,#15372));
#2820=EDGE_LOOP('',(#15373,#15374,#15375,#15376));
#2821=EDGE_LOOP('',(#15377,#15378,#15379,#15380));
#2822=EDGE_LOOP('',(#15381,#15382,#15383,#15384));
#2823=EDGE_LOOP('',(#15385,#15386,#15387,#15388));
#2824=EDGE_LOOP('',(#15389,#15390,#15391,#15392));
#2825=EDGE_LOOP('',(#15393,#15394,#15395,#15396));
#2826=EDGE_LOOP('',(#15397,#15398,#15399,#15400));
#2827=EDGE_LOOP('',(#15401,#15402,#15403,#15404));
#2828=EDGE_LOOP('',(#15405,#15406,#15407,#15408));
#2829=EDGE_LOOP('',(#15409,#15410,#15411,#15412));
#2830=EDGE_LOOP('',(#15413,#15414,#15415,#15416));
#2831=EDGE_LOOP('',(#15417,#15418,#15419,#15420));
#2832=EDGE_LOOP('',(#15421,#15422,#15423,#15424));
#2833=EDGE_LOOP('',(#15425,#15426,#15427,#15428));
#2834=EDGE_LOOP('',(#15429,#15430,#15431,#15432));
#2835=EDGE_LOOP('',(#15433,#15434,#15435,#15436));
#2836=EDGE_LOOP('',(#15437,#15438,#15439,#15440));
#2837=EDGE_LOOP('',(#15441,#15442,#15443,#15444));
#2838=EDGE_LOOP('',(#15445,#15446,#15447,#15448));
#2839=EDGE_LOOP('',(#15449,#15450,#15451,#15452));
#2840=EDGE_LOOP('',(#15453,#15454,#15455,#15456));
#2841=EDGE_LOOP('',(#15457,#15458,#15459,#15460));
#2842=EDGE_LOOP('',(#15461,#15462,#15463,#15464));
#2843=EDGE_LOOP('',(#15465,#15466,#15467,#15468));
#2844=EDGE_LOOP('',(#15469,#15470,#15471,#15472));
#2845=EDGE_LOOP('',(#15473,#15474,#15475,#15476));
#2846=EDGE_LOOP('',(#15477,#15478,#15479,#15480));
#2847=EDGE_LOOP('',(#15481,#15482,#15483,#15484));
#2848=EDGE_LOOP('',(#15485,#15486,#15487,#15488));
#2849=EDGE_LOOP('',(#15489,#15490,#15491,#15492));
#2850=EDGE_LOOP('',(#15493,#15494,#15495,#15496));
#2851=EDGE_LOOP('',(#15497,#15498,#15499,#15500));
#2852=EDGE_LOOP('',(#15501,#15502,#15503,#15504));
#2853=EDGE_LOOP('',(#15505,#15506,#15507,#15508));
#2854=EDGE_LOOP('',(#15509,#15510,#15511,#15512));
#2855=EDGE_LOOP('',(#15513,#15514,#15515,#15516));
#2856=EDGE_LOOP('',(#15517,#15518,#15519,#15520));
#2857=EDGE_LOOP('',(#15521,#15522,#15523,#15524));
#2858=EDGE_LOOP('',(#15525,#15526,#15527,#15528));
#2859=EDGE_LOOP('',(#15529,#15530,#15531,#15532));
#2860=EDGE_LOOP('',(#15533,#15534,#15535,#15536));
#2861=EDGE_LOOP('',(#15537,#15538,#15539,#15540));
#2862=EDGE_LOOP('',(#15541,#15542,#15543,#15544));
#2863=EDGE_LOOP('',(#15545,#15546,#15547,#15548));
#2864=EDGE_LOOP('',(#15549,#15550,#15551,#15552));
#2865=EDGE_LOOP('',(#15553,#15554,#15555,#15556));
#2866=EDGE_LOOP('',(#15557,#15558,#15559,#15560));
#2867=EDGE_LOOP('',(#15561,#15562,#15563,#15564));
#2868=EDGE_LOOP('',(#15565,#15566,#15567,#15568));
#2869=EDGE_LOOP('',(#15569,#15570,#15571,#15572));
#2870=EDGE_LOOP('',(#15573,#15574,#15575,#15576));
#2871=EDGE_LOOP('',(#15577,#15578,#15579,#15580));
#2872=EDGE_LOOP('',(#15581,#15582,#15583,#15584));
#2873=EDGE_LOOP('',(#15585,#15586,#15587,#15588));
#2874=EDGE_LOOP('',(#15589,#15590,#15591,#15592));
#2875=EDGE_LOOP('',(#15593,#15594,#15595,#15596));
#2876=EDGE_LOOP('',(#15597,#15598,#15599,#15600));
#2877=EDGE_LOOP('',(#15601,#15602,#15603,#15604));
#2878=EDGE_LOOP('',(#15605,#15606,#15607,#15608));
#2879=EDGE_LOOP('',(#15609,#15610,#15611,#15612));
#2880=EDGE_LOOP('',(#15613,#15614,#15615,#15616));
#2881=EDGE_LOOP('',(#15617,#15618,#15619,#15620));
#2882=EDGE_LOOP('',(#15621,#15622,#15623,#15624));
#2883=EDGE_LOOP('',(#15625,#15626,#15627,#15628));
#2884=EDGE_LOOP('',(#15629,#15630,#15631,#15632));
#2885=EDGE_LOOP('',(#15633,#15634,#15635,#15636));
#2886=EDGE_LOOP('',(#15637,#15638,#15639,#15640));
#2887=EDGE_LOOP('',(#15641,#15642,#15643,#15644));
#2888=EDGE_LOOP('',(#15645,#15646,#15647,#15648));
#2889=EDGE_LOOP('',(#15649,#15650,#15651,#15652));
#2890=EDGE_LOOP('',(#15653,#15654,#15655,#15656));
#2891=EDGE_LOOP('',(#15657,#15658,#15659,#15660));
#2892=EDGE_LOOP('',(#15661,#15662,#15663,#15664));
#2893=EDGE_LOOP('',(#15665,#15666,#15667,#15668));
#2894=EDGE_LOOP('',(#15669,#15670,#15671,#15672));
#2895=EDGE_LOOP('',(#15673,#15674,#15675,#15676));
#2896=EDGE_LOOP('',(#15677,#15678,#15679,#15680));
#2897=EDGE_LOOP('',(#15681,#15682,#15683,#15684));
#2898=EDGE_LOOP('',(#15685,#15686,#15687,#15688));
#2899=EDGE_LOOP('',(#15689,#15690,#15691,#15692));
#2900=EDGE_LOOP('',(#15693,#15694,#15695,#15696));
#2901=EDGE_LOOP('',(#15697,#15698,#15699,#15700));
#2902=EDGE_LOOP('',(#15701,#15702,#15703,#15704));
#2903=EDGE_LOOP('',(#15705,#15706,#15707,#15708));
#2904=EDGE_LOOP('',(#15709,#15710,#15711,#15712));
#2905=EDGE_LOOP('',(#15713,#15714,#15715,#15716));
#2906=EDGE_LOOP('',(#15717,#15718,#15719,#15720));
#2907=EDGE_LOOP('',(#15721,#15722,#15723,#15724));
#2908=EDGE_LOOP('',(#15725,#15726,#15727,#15728));
#2909=EDGE_LOOP('',(#15729,#15730,#15731,#15732));
#2910=EDGE_LOOP('',(#15733,#15734,#15735,#15736));
#2911=EDGE_LOOP('',(#15737,#15738,#15739,#15740));
#2912=EDGE_LOOP('',(#15741,#15742,#15743,#15744));
#2913=EDGE_LOOP('',(#15745,#15746,#15747,#15748,#15749,#15750,#15751,#15752,
#15753,#15754,#15755,#15756,#15757,#15758,#15759,#15760,#15761,#15762,#15763,
#15764,#15765,#15766,#15767,#15768,#15769,#15770,#15771,#15772,#15773,#15774,
#15775,#15776,#15777,#15778,#15779,#15780,#15781,#15782,#15783,#15784,#15785,
#15786,#15787,#15788,#15789,#15790,#15791,#15792,#15793,#15794,#15795,#15796,
#15797,#15798,#15799,#15800,#15801,#15802,#15803,#15804,#15805,#15806,#15807,
#15808,#15809,#15810,#15811,#15812,#15813,#15814,#15815,#15816,#15817,#15818,
#15819,#15820,#15821,#15822,#15823,#15824,#15825,#15826,#15827,#15828,#15829,
#15830,#15831,#15832,#15833,#15834,#15835,#15836,#15837,#15838,#15839,#15840,
#15841,#15842,#15843,#15844,#15845,#15846,#15847,#15848,#15849,#15850,#15851,
#15852,#15853,#15854,#15855,#15856,#15857,#15858,#15859,#15860,#15861,#15862,
#15863,#15864,#15865,#15866,#15867,#15868,#15869,#15870,#15871,#15872,#15873,
#15874,#15875,#15876,#15877,#15878,#15879,#15880,#15881,#15882,#15883,#15884,
#15885,#15886,#15887,#15888,#15889,#15890,#15891,#15892,#15893,#15894,#15895,
#15896,#15897,#15898,#15899,#15900,#15901,#15902,#15903,#15904,#15905,#15906,
#15907,#15908,#15909,#15910,#15911,#15912,#15913,#15914,#15915,#15916,#15917,
#15918,#15919,#15920));
#2914=EDGE_LOOP('',(#15921,#15922,#15923,#15924,#15925,#15926,#15927,#15928,
#15929,#15930,#15931,#15932,#15933,#15934,#15935,#15936));
#2915=EDGE_LOOP('',(#15937));
#2916=EDGE_LOOP('',(#15938,#15939,#15940,#15941,#15942,#15943,#15944,#15945));
#2917=EDGE_LOOP('',(#15946,#15947,#15948,#15949,#15950,#15951,#15952,#15953));
#2918=EDGE_LOOP('',(#15954,#15955,#15956,#15957,#15958,#15959,#15960,#15961,
#15962,#15963,#15964,#15965,#15966,#15967,#15968,#15969));
#2919=EDGE_LOOP('',(#15970));
#2920=EDGE_LOOP('',(#15971,#15972,#15973,#15974,#15975,#15976,#15977,#15978,
#15979,#15980,#15981,#15982,#15983,#15984,#15985,#15986));
#2921=EDGE_LOOP('',(#15987));
#2922=EDGE_LOOP('',(#15988,#15989,#15990,#15991,#15992,#15993,#15994,#15995,
#15996,#15997,#15998,#15999,#16000,#16001,#16002,#16003));
#2923=EDGE_LOOP('',(#16004));
#2924=EDGE_LOOP('',(#16005,#16006,#16007,#16008,#16009,#16010,#16011,#16012));
#2925=EDGE_LOOP('',(#16013,#16014,#16015,#16016,#16017,#16018,#16019,#16020));
#2926=EDGE_LOOP('',(#16021));
#2927=EDGE_LOOP('',(#16022,#16023,#16024,#16025));
#2928=EDGE_LOOP('',(#16026,#16027,#16028,#16029));
#2929=EDGE_LOOP('',(#16030,#16031,#16032,#16033));
#2930=EDGE_LOOP('',(#16034,#16035,#16036,#16037));
#2931=EDGE_LOOP('',(#16038,#16039,#16040,#16041));
#2932=EDGE_LOOP('',(#16042,#16043,#16044,#16045));
#2933=EDGE_LOOP('',(#16046,#16047,#16048,#16049));
#2934=EDGE_LOOP('',(#16050,#16051,#16052,#16053));
#2935=EDGE_LOOP('',(#16054,#16055,#16056,#16057));
#2936=EDGE_LOOP('',(#16058,#16059,#16060,#16061));
#2937=EDGE_LOOP('',(#16062,#16063,#16064,#16065));
#2938=EDGE_LOOP('',(#16066,#16067,#16068,#16069));
#2939=EDGE_LOOP('',(#16070,#16071,#16072,#16073));
#2940=EDGE_LOOP('',(#16074,#16075,#16076,#16077));
#2941=EDGE_LOOP('',(#16078,#16079,#16080,#16081));
#2942=EDGE_LOOP('',(#16082,#16083,#16084,#16085));
#2943=EDGE_LOOP('',(#16086,#16087,#16088,#16089));
#2944=EDGE_LOOP('',(#16090,#16091,#16092,#16093));
#2945=EDGE_LOOP('',(#16094,#16095,#16096,#16097));
#2946=EDGE_LOOP('',(#16098,#16099,#16100,#16101));
#2947=EDGE_LOOP('',(#16102,#16103,#16104,#16105));
#2948=EDGE_LOOP('',(#16106,#16107,#16108,#16109));
#2949=EDGE_LOOP('',(#16110,#16111,#16112,#16113));
#2950=EDGE_LOOP('',(#16114,#16115,#16116,#16117));
#2951=EDGE_LOOP('',(#16118,#16119,#16120,#16121));
#2952=EDGE_LOOP('',(#16122,#16123,#16124,#16125));
#2953=EDGE_LOOP('',(#16126,#16127,#16128,#16129));
#2954=EDGE_LOOP('',(#16130,#16131,#16132,#16133));
#2955=EDGE_LOOP('',(#16134,#16135,#16136,#16137));
#2956=EDGE_LOOP('',(#16138,#16139,#16140,#16141));
#2957=EDGE_LOOP('',(#16142,#16143,#16144,#16145));
#2958=EDGE_LOOP('',(#16146,#16147,#16148,#16149));
#2959=EDGE_LOOP('',(#16150,#16151,#16152,#16153));
#2960=EDGE_LOOP('',(#16154,#16155,#16156,#16157));
#2961=EDGE_LOOP('',(#16158,#16159,#16160,#16161));
#2962=EDGE_LOOP('',(#16162,#16163,#16164,#16165));
#2963=EDGE_LOOP('',(#16166,#16167,#16168,#16169));
#2964=EDGE_LOOP('',(#16170,#16171,#16172,#16173));
#2965=EDGE_LOOP('',(#16174,#16175,#16176,#16177,#16178,#16179,#16180,#16181,
#16182,#16183,#16184,#16185,#16186,#16187,#16188,#16189,#16190,#16191,#16192,
#16193,#16194,#16195,#16196,#16197,#16198,#16199,#16200,#16201,#16202,#16203,
#16204,#16205,#16206,#16207,#16208,#16209,#16210,#16211,#16212,#16213,#16214,
#16215,#16216,#16217,#16218,#16219,#16220,#16221,#16222,#16223,#16224,#16225,
#16226,#16227,#16228,#16229,#16230,#16231,#16232,#16233,#16234,#16235,#16236,
#16237,#16238,#16239,#16240,#16241,#16242,#16243,#16244,#16245,#16246,#16247,
#16248,#16249,#16250,#16251,#16252,#16253,#16254,#16255,#16256,#16257,#16258,
#16259,#16260,#16261,#16262,#16263,#16264,#16265,#16266,#16267,#16268,#16269,
#16270,#16271,#16272,#16273,#16274,#16275,#16276,#16277,#16278,#16279,#16280,
#16281,#16282,#16283,#16284,#16285,#16286,#16287,#16288,#16289,#16290,#16291,
#16292,#16293,#16294,#16295,#16296,#16297,#16298,#16299,#16300,#16301,#16302,
#16303,#16304,#16305,#16306,#16307,#16308,#16309,#16310,#16311,#16312,#16313,
#16314,#16315,#16316,#16317,#16318,#16319,#16320,#16321,#16322,#16323,#16324,
#16325,#16326,#16327,#16328,#16329,#16330,#16331,#16332,#16333,#16334,#16335,
#16336,#16337,#16338,#16339,#16340,#16341,#16342,#16343,#16344,#16345,#16346,
#16347,#16348,#16349));
#2966=EDGE_LOOP('',(#16350,#16351,#16352,#16353,#16354,#16355,#16356,#16357));
#2967=EDGE_LOOP('',(#16358,#16359,#16360,#16361,#16362,#16363,#16364,#16365));
#2968=EDGE_LOOP('',(#16366));
#2969=EDGE_LOOP('',(#16367));
#2970=EDGE_LOOP('',(#16368,#16369,#16370,#16371,#16372,#16373,#16374,#16375,
#16376,#16377,#16378,#16379,#16380,#16381,#16382,#16383));
#2971=EDGE_LOOP('',(#16384,#16385,#16386,#16387,#16388,#16389,#16390,#16391,
#16392,#16393,#16394,#16395,#16396,#16397,#16398,#16399));
#2972=EDGE_LOOP('',(#16400));
#2973=EDGE_LOOP('',(#16401,#16402,#16403,#16404,#16405,#16406,#16407,#16408,
#16409,#16410,#16411,#16412,#16413,#16414,#16415,#16416));
#2974=EDGE_LOOP('',(#16417));
#2975=EDGE_LOOP('',(#16418));
#2976=EDGE_LOOP('',(#16419,#16420,#16421,#16422,#16423,#16424,#16425,#16426));
#2977=EDGE_LOOP('',(#16427,#16428,#16429,#16430,#16431,#16432,#16433,#16434));
#2978=EDGE_LOOP('',(#16435,#16436,#16437,#16438,#16439,#16440,#16441,#16442,
#16443,#16444,#16445,#16446,#16447,#16448,#16449,#16450));
#3810=CIRCLE('',#21115,3.25);
#3811=CIRCLE('',#21116,3.25);
#3812=CIRCLE('',#21126,0.499999999999999);
#3813=CIRCLE('',#21127,0.499999999999999);
#3814=CIRCLE('',#21130,0.499999999999998);
#3815=CIRCLE('',#21131,0.499999999999998);
#3816=CIRCLE('',#21144,0.499999999999998);
#3817=CIRCLE('',#21145,0.499999999999998);
#3818=CIRCLE('',#21148,0.499999999999999);
#3819=CIRCLE('',#21149,0.499999999999999);
#3820=CIRCLE('',#21160,2.);
#3821=CIRCLE('',#21161,2.);
#3822=CIRCLE('',#21171,0.499999999999999);
#3823=CIRCLE('',#21172,0.499999999999999);
#3824=CIRCLE('',#21175,0.499999999999998);
#3825=CIRCLE('',#21176,0.499999999999998);
#3826=CIRCLE('',#21190,3.25);
#3827=CIRCLE('',#21191,3.25);
#3828=CIRCLE('',#21194,0.499999999999998);
#3829=CIRCLE('',#21195,0.499999999999998);
#3830=CIRCLE('',#21198,0.499999999999999);
#3831=CIRCLE('',#21199,0.499999999999999);
#3832=CIRCLE('',#21210,2.);
#3833=CIRCLE('',#21211,2.);
#3834=CIRCLE('',#21256,3.25);
#3835=CIRCLE('',#21257,3.25);
#3836=CIRCLE('',#21303,3.25);
#3837=CIRCLE('',#21304,3.25);
#3838=CIRCLE('',#21315,0.499999999999999);
#3839=CIRCLE('',#21316,0.499999999999999);
#3840=CIRCLE('',#21319,0.499999999999998);
#3841=CIRCLE('',#21320,0.499999999999998);
#3842=CIRCLE('',#21333,0.499999999999998);
#3843=CIRCLE('',#21334,0.499999999999998);
#3844=CIRCLE('',#21337,0.499999999999999);
#3845=CIRCLE('',#21338,0.499999999999999);
#3846=CIRCLE('',#21349,2.);
#3847=CIRCLE('',#21350,2.);
#3848=CIRCLE('',#21359,2.);
#3849=CIRCLE('',#21360,0.499999999999998);
#3850=CIRCLE('',#21361,0.499999999999999);
#3851=CIRCLE('',#21362,0.499999999999998);
#3852=CIRCLE('',#21363,0.499999999999999);
#3853=CIRCLE('',#21364,3.25);
#3854=CIRCLE('',#21367,0.499999999999999);
#3855=CIRCLE('',#21370,0.499999999999998);
#3856=CIRCLE('',#21384,3.25);
#3857=CIRCLE('',#21387,0.499999999999998);
#3858=CIRCLE('',#21390,0.499999999999999);
#3859=CIRCLE('',#21401,2.);
#4641=LINE('',#29329,#6522);
#4642=LINE('',#29331,#6523);
#4643=LINE('',#29333,#6524);
#4644=LINE('',#29334,#6525);
#4645=LINE('',#29337,#6526);
#4646=LINE('',#29339,#6527);
#4647=LINE('',#29340,#6528);
#4648=LINE('',#29343,#6529);
#4649=LINE('',#29345,#6530);
#4650=LINE('',#29346,#6531);
#4651=LINE('',#29350,#6532);
#4652=LINE('',#29352,#6533);
#4653=LINE('',#29354,#6534);
#4654=LINE('',#29355,#6535);
#4655=LINE('',#29358,#6536);
#4656=LINE('',#29360,#6537);
#4657=LINE('',#29361,#6538);
#4658=LINE('',#29364,#6539);
#4659=LINE('',#29366,#6540);
#4660=LINE('',#29367,#6541);
#4661=LINE('',#29370,#6542);
#4662=LINE('',#29372,#6543);
#4663=LINE('',#29373,#6544);
#4664=LINE('',#29376,#6545);
#4665=LINE('',#29378,#6546);
#4666=LINE('',#29379,#6547);
#4667=LINE('',#29382,#6548);
#4668=LINE('',#29384,#6549);
#4669=LINE('',#29385,#6550);
#4670=LINE('',#29389,#6551);
#4671=LINE('',#29391,#6552);
#4672=LINE('',#29393,#6553);
#4673=LINE('',#29394,#6554);
#4674=LINE('',#29397,#6555);
#4675=LINE('',#29399,#6556);
#4676=LINE('',#29400,#6557);
#4677=LINE('',#29403,#6558);
#4678=LINE('',#29405,#6559);
#4679=LINE('',#29406,#6560);
#4680=LINE('',#29409,#6561);
#4681=LINE('',#29411,#6562);
#4682=LINE('',#29412,#6563);
#4683=LINE('',#29416,#6564);
#4684=LINE('',#29418,#6565);
#4685=LINE('',#29420,#6566);
#4686=LINE('',#29421,#6567);
#4687=LINE('',#29424,#6568);
#4688=LINE('',#29426,#6569);
#4689=LINE('',#29427,#6570);
#4690=LINE('',#29430,#6571);
#4691=LINE('',#29432,#6572);
#4692=LINE('',#29433,#6573);
#4693=LINE('',#29436,#6574);
#4694=LINE('',#29438,#6575);
#4695=LINE('',#29439,#6576);
#4696=LINE('',#29442,#6577);
#4697=LINE('',#29444,#6578);
#4698=LINE('',#29445,#6579);
#4699=LINE('',#29447,#6580);
#4700=LINE('',#29448,#6581);
#4701=LINE('',#29452,#6582);
#4702=LINE('',#29454,#6583);
#4703=LINE('',#29456,#6584);
#4704=LINE('',#29457,#6585);
#4705=LINE('',#29460,#6586);
#4706=LINE('',#29462,#6587);
#4707=LINE('',#29463,#6588);
#4708=LINE('',#29466,#6589);
#4709=LINE('',#29468,#6590);
#4710=LINE('',#29469,#6591);
#4711=LINE('',#29471,#6592);
#4712=LINE('',#29472,#6593);
#4713=LINE('',#29476,#6594);
#4714=LINE('',#29478,#6595);
#4715=LINE('',#29480,#6596);
#4716=LINE('',#29481,#6597);
#4717=LINE('',#29484,#6598);
#4718=LINE('',#29486,#6599);
#4719=LINE('',#29487,#6600);
#4720=LINE('',#29490,#6601);
#4721=LINE('',#29492,#6602);
#4722=LINE('',#29493,#6603);
#4723=LINE('',#29496,#6604);
#4724=LINE('',#29498,#6605);
#4725=LINE('',#29499,#6606);
#4726=LINE('',#29502,#6607);
#4727=LINE('',#29504,#6608);
#4728=LINE('',#29505,#6609);
#4729=LINE('',#29508,#6610);
#4730=LINE('',#29510,#6611);
#4731=LINE('',#29511,#6612);
#4732=LINE('',#29515,#6613);
#4733=LINE('',#29517,#6614);
#4734=LINE('',#29519,#6615);
#4735=LINE('',#29520,#6616);
#4736=LINE('',#29523,#6617);
#4737=LINE('',#29525,#6618);
#4738=LINE('',#29526,#6619);
#4739=LINE('',#29529,#6620);
#4740=LINE('',#29531,#6621);
#4741=LINE('',#29532,#6622);
#4742=LINE('',#29534,#6623);
#4743=LINE('',#29535,#6624);
#4744=LINE('',#29540,#6625);
#4745=LINE('',#29544,#6626);
#4746=LINE('',#29546,#6627);
#4747=LINE('',#29547,#6628);
#4748=LINE('',#29551,#6629);
#4749=LINE('',#29553,#6630);
#4750=LINE('',#29555,#6631);
#4751=LINE('',#29556,#6632);
#4752=LINE('',#29559,#6633);
#4753=LINE('',#29561,#6634);
#4754=LINE('',#29562,#6635);
#4755=LINE('',#29565,#6636);
#4756=LINE('',#29567,#6637);
#4757=LINE('',#29568,#6638);
#4758=LINE('',#29571,#6639);
#4759=LINE('',#29573,#6640);
#4760=LINE('',#29574,#6641);
#4761=LINE('',#29577,#6642);
#4762=LINE('',#29579,#6643);
#4763=LINE('',#29580,#6644);
#4764=LINE('',#29582,#6645);
#4765=LINE('',#29583,#6646);
#4766=LINE('',#29587,#6647);
#4767=LINE('',#29589,#6648);
#4768=LINE('',#29591,#6649);
#4769=LINE('',#29592,#6650);
#4770=LINE('',#29598,#6651);
#4771=LINE('',#29601,#6652);
#4772=LINE('',#29603,#6653);
#4773=LINE('',#29604,#6654);
#4774=LINE('',#29610,#6655);
#4775=LINE('',#29614,#6656);
#4776=LINE('',#29616,#6657);
#4777=LINE('',#29618,#6658);
#4778=LINE('',#29619,#6659);
#4779=LINE('',#29622,#6660);
#4780=LINE('',#29624,#6661);
#4781=LINE('',#29625,#6662);
#4782=LINE('',#29628,#6663);
#4783=LINE('',#29630,#6664);
#4784=LINE('',#29631,#6665);
#4785=LINE('',#29634,#6666);
#4786=LINE('',#29636,#6667);
#4787=LINE('',#29637,#6668);
#4788=LINE('',#29640,#6669);
#4789=LINE('',#29642,#6670);
#4790=LINE('',#29643,#6671);
#4791=LINE('',#29646,#6672);
#4792=LINE('',#29648,#6673);
#4793=LINE('',#29649,#6674);
#4794=LINE('',#29651,#6675);
#4795=LINE('',#29652,#6676);
#4796=LINE('',#29655,#6677);
#4797=LINE('',#29657,#6678);
#4798=LINE('',#29658,#6679);
#4799=LINE('',#29661,#6680);
#4800=LINE('',#29663,#6681);
#4801=LINE('',#29664,#6682);
#4802=LINE('',#29667,#6683);
#4803=LINE('',#29669,#6684);
#4804=LINE('',#29670,#6685);
#4805=LINE('',#29673,#6686);
#4806=LINE('',#29675,#6687);
#4807=LINE('',#29676,#6688);
#4808=LINE('',#29681,#6689);
#4809=LINE('',#29685,#6690);
#4810=LINE('',#29687,#6691);
#4811=LINE('',#29688,#6692);
#4812=LINE('',#29693,#6693);
#4813=LINE('',#29696,#6694);
#4814=LINE('',#29697,#6695);
#4815=LINE('',#29700,#6696);
#4816=LINE('',#29702,#6697);
#4817=LINE('',#29703,#6698);
#4818=LINE('',#29706,#6699);
#4819=LINE('',#29708,#6700);
#4820=LINE('',#29709,#6701);
#4821=LINE('',#29712,#6702);
#4822=LINE('',#29714,#6703);
#4823=LINE('',#29715,#6704);
#4824=LINE('',#29718,#6705);
#4825=LINE('',#29720,#6706);
#4826=LINE('',#29721,#6707);
#4827=LINE('',#29724,#6708);
#4828=LINE('',#29726,#6709);
#4829=LINE('',#29727,#6710);
#4830=LINE('',#29730,#6711);
#4831=LINE('',#29732,#6712);
#4832=LINE('',#29733,#6713);
#4833=LINE('',#29736,#6714);
#4834=LINE('',#29738,#6715);
#4835=LINE('',#29739,#6716);
#4836=LINE('',#29742,#6717);
#4837=LINE('',#29744,#6718);
#4838=LINE('',#29745,#6719);
#4839=LINE('',#29750,#6720);
#4840=LINE('',#29754,#6721);
#4841=LINE('',#29756,#6722);
#4842=LINE('',#29757,#6723);
#4843=LINE('',#29760,#6724);
#4844=LINE('',#29762,#6725);
#4845=LINE('',#29763,#6726);
#4846=LINE('',#29766,#6727);
#4847=LINE('',#29768,#6728);
#4848=LINE('',#29769,#6729);
#4849=LINE('',#29772,#6730);
#4850=LINE('',#29774,#6731);
#4851=LINE('',#29775,#6732);
#4852=LINE('',#29778,#6733);
#4853=LINE('',#29780,#6734);
#4854=LINE('',#29781,#6735);
#4855=LINE('',#29784,#6736);
#4856=LINE('',#29786,#6737);
#4857=LINE('',#29787,#6738);
#4858=LINE('',#29790,#6739);
#4859=LINE('',#29792,#6740);
#4860=LINE('',#29793,#6741);
#4861=LINE('',#29797,#6742);
#4862=LINE('',#29799,#6743);
#4863=LINE('',#29801,#6744);
#4864=LINE('',#29802,#6745);
#4865=LINE('',#29807,#6746);
#4866=LINE('',#29811,#6747);
#4867=LINE('',#29813,#6748);
#4868=LINE('',#29814,#6749);
#4869=LINE('',#29819,#6750);
#4870=LINE('',#29824,#6751);
#4871=LINE('',#29826,#6752);
#4872=LINE('',#29828,#6753);
#4873=LINE('',#29829,#6754);
#4874=LINE('',#29832,#6755);
#4875=LINE('',#29834,#6756);
#4876=LINE('',#29835,#6757);
#4877=LINE('',#29838,#6758);
#4878=LINE('',#29840,#6759);
#4879=LINE('',#29841,#6760);
#4880=LINE('',#29844,#6761);
#4881=LINE('',#29846,#6762);
#4882=LINE('',#29847,#6763);
#4883=LINE('',#29850,#6764);
#4884=LINE('',#29852,#6765);
#4885=LINE('',#29853,#6766);
#4886=LINE('',#29856,#6767);
#4887=LINE('',#29858,#6768);
#4888=LINE('',#29859,#6769);
#4889=LINE('',#29861,#6770);
#4890=LINE('',#29862,#6771);
#4891=LINE('',#29865,#6772);
#4892=LINE('',#29867,#6773);
#4893=LINE('',#29868,#6774);
#4894=LINE('',#29871,#6775);
#4895=LINE('',#29873,#6776);
#4896=LINE('',#29874,#6777);
#4897=LINE('',#29877,#6778);
#4898=LINE('',#29879,#6779);
#4899=LINE('',#29880,#6780);
#4900=LINE('',#29883,#6781);
#4901=LINE('',#29885,#6782);
#4902=LINE('',#29886,#6783);
#4903=LINE('',#29888,#6784);
#4904=LINE('',#29889,#6785);
#4905=LINE('',#29894,#6786);
#4906=LINE('',#29898,#6787);
#4907=LINE('',#29900,#6788);
#4908=LINE('',#29901,#6789);
#4909=LINE('',#29907,#6790);
#4910=LINE('',#29910,#6791);
#4911=LINE('',#29912,#6792);
#4912=LINE('',#29913,#6793);
#4913=LINE('',#29919,#6794);
#4914=LINE('',#29921,#6795);
#4915=LINE('',#29922,#6796);
#4916=LINE('',#29925,#6797);
#4917=LINE('',#29927,#6798);
#4918=LINE('',#29928,#6799);
#4919=LINE('',#29931,#6800);
#4920=LINE('',#29933,#6801);
#4921=LINE('',#29934,#6802);
#4922=LINE('',#29937,#6803);
#4923=LINE('',#29939,#6804);
#4924=LINE('',#29940,#6805);
#4925=LINE('',#29943,#6806);
#4926=LINE('',#29945,#6807);
#4927=LINE('',#29946,#6808);
#4928=LINE('',#29949,#6809);
#4929=LINE('',#29951,#6810);
#4930=LINE('',#29952,#6811);
#4931=LINE('',#29955,#6812);
#4932=LINE('',#29957,#6813);
#4933=LINE('',#29958,#6814);
#4934=LINE('',#29961,#6815);
#4935=LINE('',#29963,#6816);
#4936=LINE('',#29964,#6817);
#4937=LINE('',#29967,#6818);
#4938=LINE('',#29969,#6819);
#4939=LINE('',#29970,#6820);
#4940=LINE('',#29976,#6821);
#4941=LINE('',#29979,#6822);
#4942=LINE('',#29981,#6823);
#4943=LINE('',#29982,#6824);
#4944=LINE('',#29985,#6825);
#4945=LINE('',#29987,#6826);
#4946=LINE('',#29988,#6827);
#4947=LINE('',#29991,#6828);
#4948=LINE('',#29993,#6829);
#4949=LINE('',#29994,#6830);
#4950=LINE('',#29997,#6831);
#4951=LINE('',#29999,#6832);
#4952=LINE('',#30000,#6833);
#4953=LINE('',#30003,#6834);
#4954=LINE('',#30005,#6835);
#4955=LINE('',#30006,#6836);
#4956=LINE('',#30009,#6837);
#4957=LINE('',#30011,#6838);
#4958=LINE('',#30012,#6839);
#4959=LINE('',#30014,#6840);
#4960=LINE('',#30015,#6841);
#4961=LINE('',#30019,#6842);
#4962=LINE('',#30021,#6843);
#4963=LINE('',#30023,#6844);
#4964=LINE('',#30024,#6845);
#4965=LINE('',#30027,#6846);
#4966=LINE('',#30029,#6847);
#4967=LINE('',#30030,#6848);
#4968=LINE('',#30033,#6849);
#4969=LINE('',#30035,#6850);
#4970=LINE('',#30036,#6851);
#4971=LINE('',#30040,#6852);
#4972=LINE('',#30042,#6853);
#4973=LINE('',#30044,#6854);
#4974=LINE('',#30045,#6855);
#4975=LINE('',#30048,#6856);
#4976=LINE('',#30050,#6857);
#4977=LINE('',#30051,#6858);
#4978=LINE('',#30054,#6859);
#4979=LINE('',#30056,#6860);
#4980=LINE('',#30057,#6861);
#4981=LINE('',#30060,#6862);
#4982=LINE('',#30062,#6863);
#4983=LINE('',#30063,#6864);
#4984=LINE('',#30066,#6865);
#4985=LINE('',#30068,#6866);
#4986=LINE('',#30069,#6867);
#4987=LINE('',#30072,#6868);
#4988=LINE('',#30074,#6869);
#4989=LINE('',#30075,#6870);
#4990=LINE('',#30078,#6871);
#4991=LINE('',#30080,#6872);
#4992=LINE('',#30081,#6873);
#4993=LINE('',#30084,#6874);
#4994=LINE('',#30086,#6875);
#4995=LINE('',#30087,#6876);
#4996=LINE('',#30090,#6877);
#4997=LINE('',#30092,#6878);
#4998=LINE('',#30093,#6879);
#4999=LINE('',#30096,#6880);
#5000=LINE('',#30098,#6881);
#5001=LINE('',#30099,#6882);
#5002=LINE('',#30102,#6883);
#5003=LINE('',#30104,#6884);
#5004=LINE('',#30105,#6885);
#5005=LINE('',#30108,#6886);
#5006=LINE('',#30110,#6887);
#5007=LINE('',#30111,#6888);
#5008=LINE('',#30114,#6889);
#5009=LINE('',#30116,#6890);
#5010=LINE('',#30117,#6891);
#5011=LINE('',#30120,#6892);
#5012=LINE('',#30122,#6893);
#5013=LINE('',#30123,#6894);
#5014=LINE('',#30126,#6895);
#5015=LINE('',#30128,#6896);
#5016=LINE('',#30129,#6897);
#5017=LINE('',#30132,#6898);
#5018=LINE('',#30134,#6899);
#5019=LINE('',#30135,#6900);
#5020=LINE('',#30138,#6901);
#5021=LINE('',#30140,#6902);
#5022=LINE('',#30141,#6903);
#5023=LINE('',#30143,#6904);
#5024=LINE('',#30144,#6905);
#5025=LINE('',#30148,#6906);
#5026=LINE('',#30150,#6907);
#5027=LINE('',#30152,#6908);
#5028=LINE('',#30153,#6909);
#5029=LINE('',#30156,#6910);
#5030=LINE('',#30158,#6911);
#5031=LINE('',#30159,#6912);
#5032=LINE('',#30162,#6913);
#5033=LINE('',#30164,#6914);
#5034=LINE('',#30165,#6915);
#5035=LINE('',#30167,#6916);
#5036=LINE('',#30168,#6917);
#5037=LINE('',#30172,#6918);
#5038=LINE('',#30174,#6919);
#5039=LINE('',#30176,#6920);
#5040=LINE('',#30177,#6921);
#5041=LINE('',#30180,#6922);
#5042=LINE('',#30182,#6923);
#5043=LINE('',#30183,#6924);
#5044=LINE('',#30186,#6925);
#5045=LINE('',#30188,#6926);
#5046=LINE('',#30189,#6927);
#5047=LINE('',#30192,#6928);
#5048=LINE('',#30194,#6929);
#5049=LINE('',#30195,#6930);
#5050=LINE('',#30198,#6931);
#5051=LINE('',#30200,#6932);
#5052=LINE('',#30201,#6933);
#5053=LINE('',#30204,#6934);
#5054=LINE('',#30206,#6935);
#5055=LINE('',#30207,#6936);
#5056=LINE('',#30210,#6937);
#5057=LINE('',#30212,#6938);
#5058=LINE('',#30213,#6939);
#5059=LINE('',#30216,#6940);
#5060=LINE('',#30218,#6941);
#5061=LINE('',#30219,#6942);
#5062=LINE('',#30222,#6943);
#5063=LINE('',#30224,#6944);
#5064=LINE('',#30225,#6945);
#5065=LINE('',#30228,#6946);
#5066=LINE('',#30230,#6947);
#5067=LINE('',#30231,#6948);
#5068=LINE('',#30233,#6949);
#5069=LINE('',#30234,#6950);
#5070=LINE('',#30239,#6951);
#5071=LINE('',#30243,#6952);
#5072=LINE('',#30245,#6953);
#5073=LINE('',#30246,#6954);
#5074=LINE('',#30249,#6955);
#5075=LINE('',#30251,#6956);
#5076=LINE('',#30252,#6957);
#5077=LINE('',#30255,#6958);
#5078=LINE('',#30257,#6959);
#5079=LINE('',#30258,#6960);
#5080=LINE('',#30261,#6961);
#5081=LINE('',#30263,#6962);
#5082=LINE('',#30264,#6963);
#5083=LINE('',#30267,#6964);
#5084=LINE('',#30269,#6965);
#5085=LINE('',#30270,#6966);
#5086=LINE('',#30273,#6967);
#5087=LINE('',#30275,#6968);
#5088=LINE('',#30276,#6969);
#5089=LINE('',#30279,#6970);
#5090=LINE('',#30281,#6971);
#5091=LINE('',#30282,#6972);
#5092=LINE('',#30284,#6973);
#5093=LINE('',#30285,#6974);
#5094=LINE('',#30289,#6975);
#5095=LINE('',#30291,#6976);
#5096=LINE('',#30293,#6977);
#5097=LINE('',#30294,#6978);
#5098=LINE('',#30297,#6979);
#5099=LINE('',#30299,#6980);
#5100=LINE('',#30300,#6981);
#5101=LINE('',#30303,#6982);
#5102=LINE('',#30305,#6983);
#5103=LINE('',#30306,#6984);
#5104=LINE('',#30310,#6985);
#5105=LINE('',#30312,#6986);
#5106=LINE('',#30314,#6987);
#5107=LINE('',#30315,#6988);
#5108=LINE('',#30318,#6989);
#5109=LINE('',#30320,#6990);
#5110=LINE('',#30321,#6991);
#5111=LINE('',#30324,#6992);
#5112=LINE('',#30326,#6993);
#5113=LINE('',#30327,#6994);
#5114=LINE('',#30330,#6995);
#5115=LINE('',#30332,#6996);
#5116=LINE('',#30333,#6997);
#5117=LINE('',#30336,#6998);
#5118=LINE('',#30338,#6999);
#5119=LINE('',#30339,#7000);
#5120=LINE('',#30342,#7001);
#5121=LINE('',#30344,#7002);
#5122=LINE('',#30345,#7003);
#5123=LINE('',#30348,#7004);
#5124=LINE('',#30350,#7005);
#5125=LINE('',#30351,#7006);
#5126=LINE('',#30354,#7007);
#5127=LINE('',#30356,#7008);
#5128=LINE('',#30357,#7009);
#5129=LINE('',#30360,#7010);
#5130=LINE('',#30362,#7011);
#5131=LINE('',#30363,#7012);
#5132=LINE('',#30366,#7013);
#5133=LINE('',#30368,#7014);
#5134=LINE('',#30369,#7015);
#5135=LINE('',#30372,#7016);
#5136=LINE('',#30374,#7017);
#5137=LINE('',#30375,#7018);
#5138=LINE('',#30378,#7019);
#5139=LINE('',#30380,#7020);
#5140=LINE('',#30381,#7021);
#5141=LINE('',#30384,#7022);
#5142=LINE('',#30386,#7023);
#5143=LINE('',#30387,#7024);
#5144=LINE('',#30390,#7025);
#5145=LINE('',#30392,#7026);
#5146=LINE('',#30393,#7027);
#5147=LINE('',#30396,#7028);
#5148=LINE('',#30398,#7029);
#5149=LINE('',#30399,#7030);
#5150=LINE('',#30402,#7031);
#5151=LINE('',#30404,#7032);
#5152=LINE('',#30405,#7033);
#5153=LINE('',#30408,#7034);
#5154=LINE('',#30410,#7035);
#5155=LINE('',#30411,#7036);
#5156=LINE('',#30413,#7037);
#5157=LINE('',#30414,#7038);
#5158=LINE('',#30418,#7039);
#5159=LINE('',#30420,#7040);
#5160=LINE('',#30422,#7041);
#5161=LINE('',#30423,#7042);
#5162=LINE('',#30426,#7043);
#5163=LINE('',#30428,#7044);
#5164=LINE('',#30429,#7045);
#5165=LINE('',#30432,#7046);
#5166=LINE('',#30434,#7047);
#5167=LINE('',#30435,#7048);
#5168=LINE('',#30437,#7049);
#5169=LINE('',#30438,#7050);
#5170=LINE('',#30442,#7051);
#5171=LINE('',#30444,#7052);
#5172=LINE('',#30446,#7053);
#5173=LINE('',#30447,#7054);
#5174=LINE('',#30450,#7055);
#5175=LINE('',#30452,#7056);
#5176=LINE('',#30453,#7057);
#5177=LINE('',#30456,#7058);
#5178=LINE('',#30458,#7059);
#5179=LINE('',#30459,#7060);
#5180=LINE('',#30462,#7061);
#5181=LINE('',#30464,#7062);
#5182=LINE('',#30465,#7063);
#5183=LINE('',#30468,#7064);
#5184=LINE('',#30470,#7065);
#5185=LINE('',#30471,#7066);
#5186=LINE('',#30474,#7067);
#5187=LINE('',#30476,#7068);
#5188=LINE('',#30477,#7069);
#5189=LINE('',#30480,#7070);
#5190=LINE('',#30482,#7071);
#5191=LINE('',#30483,#7072);
#5192=LINE('',#30486,#7073);
#5193=LINE('',#30488,#7074);
#5194=LINE('',#30489,#7075);
#5195=LINE('',#30492,#7076);
#5196=LINE('',#30494,#7077);
#5197=LINE('',#30495,#7078);
#5198=LINE('',#30498,#7079);
#5199=LINE('',#30500,#7080);
#5200=LINE('',#30501,#7081);
#5201=LINE('',#30503,#7082);
#5202=LINE('',#30504,#7083);
#5203=LINE('',#30509,#7084);
#5204=LINE('',#30513,#7085);
#5205=LINE('',#30515,#7086);
#5206=LINE('',#30516,#7087);
#5207=LINE('',#30519,#7088);
#5208=LINE('',#30521,#7089);
#5209=LINE('',#30522,#7090);
#5210=LINE('',#30525,#7091);
#5211=LINE('',#30527,#7092);
#5212=LINE('',#30528,#7093);
#5213=LINE('',#30531,#7094);
#5214=LINE('',#30533,#7095);
#5215=LINE('',#30534,#7096);
#5216=LINE('',#30537,#7097);
#5217=LINE('',#30539,#7098);
#5218=LINE('',#30540,#7099);
#5219=LINE('',#30543,#7100);
#5220=LINE('',#30545,#7101);
#5221=LINE('',#30546,#7102);
#5222=LINE('',#30549,#7103);
#5223=LINE('',#30551,#7104);
#5224=LINE('',#30552,#7105);
#5225=LINE('',#30554,#7106);
#5226=LINE('',#30555,#7107);
#5227=LINE('',#30559,#7108);
#5228=LINE('',#30561,#7109);
#5229=LINE('',#30563,#7110);
#5230=LINE('',#30564,#7111);
#5231=LINE('',#30570,#7112);
#5232=LINE('',#30573,#7113);
#5233=LINE('',#30575,#7114);
#5234=LINE('',#30576,#7115);
#5235=LINE('',#30582,#7116);
#5236=LINE('',#30586,#7117);
#5237=LINE('',#30588,#7118);
#5238=LINE('',#30590,#7119);
#5239=LINE('',#30591,#7120);
#5240=LINE('',#30594,#7121);
#5241=LINE('',#30596,#7122);
#5242=LINE('',#30597,#7123);
#5243=LINE('',#30600,#7124);
#5244=LINE('',#30602,#7125);
#5245=LINE('',#30603,#7126);
#5246=LINE('',#30606,#7127);
#5247=LINE('',#30608,#7128);
#5248=LINE('',#30609,#7129);
#5249=LINE('',#30612,#7130);
#5250=LINE('',#30614,#7131);
#5251=LINE('',#30615,#7132);
#5252=LINE('',#30618,#7133);
#5253=LINE('',#30620,#7134);
#5254=LINE('',#30621,#7135);
#5255=LINE('',#30623,#7136);
#5256=LINE('',#30624,#7137);
#5257=LINE('',#30627,#7138);
#5258=LINE('',#30629,#7139);
#5259=LINE('',#30630,#7140);
#5260=LINE('',#30633,#7141);
#5261=LINE('',#30635,#7142);
#5262=LINE('',#30636,#7143);
#5263=LINE('',#30639,#7144);
#5264=LINE('',#30641,#7145);
#5265=LINE('',#30642,#7146);
#5266=LINE('',#30645,#7147);
#5267=LINE('',#30647,#7148);
#5268=LINE('',#30648,#7149);
#5269=LINE('',#30653,#7150);
#5270=LINE('',#30657,#7151);
#5271=LINE('',#30659,#7152);
#5272=LINE('',#30660,#7153);
#5273=LINE('',#30665,#7154);
#5274=LINE('',#30668,#7155);
#5275=LINE('',#30669,#7156);
#5276=LINE('',#30672,#7157);
#5277=LINE('',#30674,#7158);
#5278=LINE('',#30675,#7159);
#5279=LINE('',#30678,#7160);
#5280=LINE('',#30680,#7161);
#5281=LINE('',#30681,#7162);
#5282=LINE('',#30684,#7163);
#5283=LINE('',#30686,#7164);
#5284=LINE('',#30687,#7165);
#5285=LINE('',#30690,#7166);
#5286=LINE('',#30692,#7167);
#5287=LINE('',#30693,#7168);
#5288=LINE('',#30696,#7169);
#5289=LINE('',#30698,#7170);
#5290=LINE('',#30699,#7171);
#5291=LINE('',#30702,#7172);
#5292=LINE('',#30704,#7173);
#5293=LINE('',#30705,#7174);
#5294=LINE('',#30708,#7175);
#5295=LINE('',#30710,#7176);
#5296=LINE('',#30711,#7177);
#5297=LINE('',#30714,#7178);
#5298=LINE('',#30716,#7179);
#5299=LINE('',#30717,#7180);
#5300=LINE('',#30722,#7181);
#5301=LINE('',#30726,#7182);
#5302=LINE('',#30728,#7183);
#5303=LINE('',#30729,#7184);
#5304=LINE('',#30732,#7185);
#5305=LINE('',#30734,#7186);
#5306=LINE('',#30735,#7187);
#5307=LINE('',#30738,#7188);
#5308=LINE('',#30740,#7189);
#5309=LINE('',#30741,#7190);
#5310=LINE('',#30744,#7191);
#5311=LINE('',#30746,#7192);
#5312=LINE('',#30747,#7193);
#5313=LINE('',#30750,#7194);
#5314=LINE('',#30752,#7195);
#5315=LINE('',#30753,#7196);
#5316=LINE('',#30756,#7197);
#5317=LINE('',#30758,#7198);
#5318=LINE('',#30759,#7199);
#5319=LINE('',#30762,#7200);
#5320=LINE('',#30764,#7201);
#5321=LINE('',#30765,#7202);
#5322=LINE('',#30768,#7203);
#5323=LINE('',#30770,#7204);
#5324=LINE('',#30772,#7205);
#5325=LINE('',#30774,#7206);
#5326=LINE('',#30776,#7207);
#5327=LINE('',#30778,#7208);
#5328=LINE('',#30780,#7209);
#5329=LINE('',#30782,#7210);
#5330=LINE('',#30784,#7211);
#5331=LINE('',#30786,#7212);
#5332=LINE('',#30788,#7213);
#5333=LINE('',#30790,#7214);
#5334=LINE('',#30792,#7215);
#5335=LINE('',#30794,#7216);
#5336=LINE('',#30796,#7217);
#5337=LINE('',#30800,#7218);
#5338=LINE('',#30802,#7219);
#5339=LINE('',#30804,#7220);
#5340=LINE('',#30806,#7221);
#5341=LINE('',#30808,#7222);
#5342=LINE('',#30810,#7223);
#5343=LINE('',#30812,#7224);
#5344=LINE('',#30813,#7225);
#5345=LINE('',#30815,#7226);
#5346=LINE('',#30817,#7227);
#5347=LINE('',#30819,#7228);
#5348=LINE('',#30821,#7229);
#5349=LINE('',#30822,#7230);
#5350=LINE('',#30827,#7231);
#5351=LINE('',#30831,#7232);
#5352=LINE('',#30835,#7233);
#5353=LINE('',#30838,#7234);
#5354=LINE('',#30843,#7235);
#5355=LINE('',#30845,#7236);
#5356=LINE('',#30846,#7237);
#5357=LINE('',#30849,#7238);
#5358=LINE('',#30853,#7239);
#5359=LINE('',#30854,#7240);
#5360=LINE('',#30857,#7241);
#5361=LINE('',#30861,#7242);
#5362=LINE('',#30863,#7243);
#5363=LINE('',#30864,#7244);
#5364=LINE('',#30867,#7245);
#5365=LINE('',#30868,#7246);
#5366=LINE('',#30871,#7247);
#5367=LINE('',#30872,#7248);
#5368=LINE('',#30875,#7249);
#5369=LINE('',#30876,#7250);
#5370=LINE('',#30879,#7251);
#5371=LINE('',#30880,#7252);
#5372=LINE('',#30883,#7253);
#5373=LINE('',#30884,#7254);
#5374=LINE('',#30886,#7255);
#5375=LINE('',#30889,#7256);
#5376=LINE('',#30890,#7257);
#5377=LINE('',#30893,#7258);
#5378=LINE('',#30894,#7259);
#5379=LINE('',#30897,#7260);
#5380=LINE('',#30898,#7261);
#5381=LINE('',#30901,#7262);
#5382=LINE('',#30902,#7263);
#5383=LINE('',#30904,#7264);
#5384=LINE('',#30908,#7265);
#5385=LINE('',#30911,#7266);
#5386=LINE('',#30912,#7267);
#5387=LINE('',#30916,#7268);
#5388=LINE('',#30919,#7269);
#5389=LINE('',#30920,#7270);
#5390=LINE('',#30924,#7271);
#5391=LINE('',#30926,#7272);
#5392=LINE('',#30929,#7273);
#5393=LINE('',#30930,#7274);
#5394=LINE('',#30933,#7275);
#5395=LINE('',#30934,#7276);
#5396=LINE('',#30937,#7277);
#5397=LINE('',#30938,#7278);
#5398=LINE('',#30941,#7279);
#5399=LINE('',#30942,#7280);
#5400=LINE('',#30945,#7281);
#5401=LINE('',#30946,#7282);
#5402=LINE('',#30949,#7283);
#5403=LINE('',#30950,#7284);
#5404=LINE('',#30953,#7285);
#5405=LINE('',#30954,#7286);
#5406=LINE('',#30957,#7287);
#5407=LINE('',#30958,#7288);
#5408=LINE('',#30962,#7289);
#5409=LINE('',#30965,#7290);
#5410=LINE('',#30966,#7291);
#5411=LINE('',#30969,#7292);
#5412=LINE('',#30970,#7293);
#5413=LINE('',#30973,#7294);
#5414=LINE('',#30974,#7295);
#5415=LINE('',#30977,#7296);
#5416=LINE('',#30978,#7297);
#5417=LINE('',#30981,#7298);
#5418=LINE('',#30982,#7299);
#5419=LINE('',#30985,#7300);
#5420=LINE('',#30986,#7301);
#5421=LINE('',#30988,#7302);
#6522=VECTOR('',#24226,10.);
#6523=VECTOR('',#24227,10.);
#6524=VECTOR('',#24228,10.);
#6525=VECTOR('',#24229,10.);
#6526=VECTOR('',#24232,10.);
#6527=VECTOR('',#24233,10.);
#6528=VECTOR('',#24234,10.);
#6529=VECTOR('',#24237,10.);
#6530=VECTOR('',#24238,10.);
#6531=VECTOR('',#24239,10.);
#6532=VECTOR('',#24242,10.);
#6533=VECTOR('',#24243,10.);
#6534=VECTOR('',#24244,10.);
#6535=VECTOR('',#24245,10.);
#6536=VECTOR('',#24248,10.);
#6537=VECTOR('',#24249,10.);
#6538=VECTOR('',#24250,10.);
#6539=VECTOR('',#24253,10.);
#6540=VECTOR('',#24254,10.);
#6541=VECTOR('',#24255,10.);
#6542=VECTOR('',#24258,10.);
#6543=VECTOR('',#24259,10.);
#6544=VECTOR('',#24260,10.);
#6545=VECTOR('',#24263,10.);
#6546=VECTOR('',#24264,10.);
#6547=VECTOR('',#24265,10.);
#6548=VECTOR('',#24268,10.);
#6549=VECTOR('',#24269,10.);
#6550=VECTOR('',#24270,10.);
#6551=VECTOR('',#24273,10.);
#6552=VECTOR('',#24274,10.);
#6553=VECTOR('',#24275,10.);
#6554=VECTOR('',#24276,10.);
#6555=VECTOR('',#24279,10.);
#6556=VECTOR('',#24280,10.);
#6557=VECTOR('',#24281,10.);
#6558=VECTOR('',#24284,10.);
#6559=VECTOR('',#24285,10.);
#6560=VECTOR('',#24286,10.);
#6561=VECTOR('',#24289,10.);
#6562=VECTOR('',#24290,10.);
#6563=VECTOR('',#24291,10.);
#6564=VECTOR('',#24294,10.);
#6565=VECTOR('',#24295,10.);
#6566=VECTOR('',#24296,10.);
#6567=VECTOR('',#24297,10.);
#6568=VECTOR('',#24300,10.);
#6569=VECTOR('',#24301,10.);
#6570=VECTOR('',#24302,10.);
#6571=VECTOR('',#24305,10.);
#6572=VECTOR('',#24306,10.);
#6573=VECTOR('',#24307,10.);
#6574=VECTOR('',#24310,10.);
#6575=VECTOR('',#24311,10.);
#6576=VECTOR('',#24312,10.);
#6577=VECTOR('',#24315,10.);
#6578=VECTOR('',#24316,10.);
#6579=VECTOR('',#24317,10.);
#6580=VECTOR('',#24320,10.);
#6581=VECTOR('',#24321,10.);
#6582=VECTOR('',#24324,10.);
#6583=VECTOR('',#24325,10.);
#6584=VECTOR('',#24326,10.);
#6585=VECTOR('',#24327,10.);
#6586=VECTOR('',#24330,10.);
#6587=VECTOR('',#24331,10.);
#6588=VECTOR('',#24332,10.);
#6589=VECTOR('',#24335,10.);
#6590=VECTOR('',#24336,10.);
#6591=VECTOR('',#24337,10.);
#6592=VECTOR('',#24340,10.);
#6593=VECTOR('',#24341,10.);
#6594=VECTOR('',#24344,10.);
#6595=VECTOR('',#24345,10.);
#6596=VECTOR('',#24346,10.);
#6597=VECTOR('',#24347,10.);
#6598=VECTOR('',#24350,10.);
#6599=VECTOR('',#24351,10.);
#6600=VECTOR('',#24352,10.);
#6601=VECTOR('',#24355,10.);
#6602=VECTOR('',#24356,10.);
#6603=VECTOR('',#24357,10.);
#6604=VECTOR('',#24360,10.);
#6605=VECTOR('',#24361,10.);
#6606=VECTOR('',#24362,10.);
#6607=VECTOR('',#24365,10.);
#6608=VECTOR('',#24366,10.);
#6609=VECTOR('',#24367,10.);
#6610=VECTOR('',#24370,10.);
#6611=VECTOR('',#24371,10.);
#6612=VECTOR('',#24372,10.);
#6613=VECTOR('',#24375,10.);
#6614=VECTOR('',#24376,10.);
#6615=VECTOR('',#24377,10.);
#6616=VECTOR('',#24378,10.);
#6617=VECTOR('',#24381,10.);
#6618=VECTOR('',#24382,10.);
#6619=VECTOR('',#24383,10.);
#6620=VECTOR('',#24386,10.);
#6621=VECTOR('',#24387,10.);
#6622=VECTOR('',#24388,10.);
#6623=VECTOR('',#24391,10.);
#6624=VECTOR('',#24392,10.);
#6625=VECTOR('',#24397,3.25);
#6626=VECTOR('',#24402,10.);
#6627=VECTOR('',#24403,10.);
#6628=VECTOR('',#24404,10.);
#6629=VECTOR('',#24407,10.);
#6630=VECTOR('',#24408,10.);
#6631=VECTOR('',#24409,10.);
#6632=VECTOR('',#24410,10.);
#6633=VECTOR('',#24413,10.);
#6634=VECTOR('',#24414,10.);
#6635=VECTOR('',#24415,10.);
#6636=VECTOR('',#24418,10.);
#6637=VECTOR('',#24419,10.);
#6638=VECTOR('',#24420,10.);
#6639=VECTOR('',#24423,10.);
#6640=VECTOR('',#24424,10.);
#6641=VECTOR('',#24425,10.);
#6642=VECTOR('',#24428,10.);
#6643=VECTOR('',#24429,10.);
#6644=VECTOR('',#24430,10.);
#6645=VECTOR('',#24433,10.);
#6646=VECTOR('',#24434,10.);
#6647=VECTOR('',#24437,10.);
#6648=VECTOR('',#24438,10.);
#6649=VECTOR('',#24439,10.);
#6650=VECTOR('',#24440,10.);
#6651=VECTOR('',#24447,10.);
#6652=VECTOR('',#24450,10.);
#6653=VECTOR('',#24451,10.);
#6654=VECTOR('',#24452,10.);
#6655=VECTOR('',#24459,10.);
#6656=VECTOR('',#24462,10.);
#6657=VECTOR('',#24463,10.);
#6658=VECTOR('',#24464,10.);
#6659=VECTOR('',#24465,10.);
#6660=VECTOR('',#24468,10.);
#6661=VECTOR('',#24469,10.);
#6662=VECTOR('',#24470,10.);
#6663=VECTOR('',#24473,10.);
#6664=VECTOR('',#24474,10.);
#6665=VECTOR('',#24475,10.);
#6666=VECTOR('',#24478,10.);
#6667=VECTOR('',#24479,10.);
#6668=VECTOR('',#24480,10.);
#6669=VECTOR('',#24483,10.);
#6670=VECTOR('',#24484,10.);
#6671=VECTOR('',#24485,10.);
#6672=VECTOR('',#24488,10.);
#6673=VECTOR('',#24489,10.);
#6674=VECTOR('',#24490,10.);
#6675=VECTOR('',#24493,10.);
#6676=VECTOR('',#24494,10.);
#6677=VECTOR('',#24497,10.);
#6678=VECTOR('',#24498,10.);
#6679=VECTOR('',#24499,10.);
#6680=VECTOR('',#24502,10.);
#6681=VECTOR('',#24503,10.);
#6682=VECTOR('',#24504,10.);
#6683=VECTOR('',#24507,10.);
#6684=VECTOR('',#24508,10.);
#6685=VECTOR('',#24509,10.);
#6686=VECTOR('',#24512,10.);
#6687=VECTOR('',#24513,10.);
#6688=VECTOR('',#24514,10.);
#6689=VECTOR('',#24519,10.);
#6690=VECTOR('',#24524,10.);
#6691=VECTOR('',#24525,10.);
#6692=VECTOR('',#24526,10.);
#6693=VECTOR('',#24531,10.);
#6694=VECTOR('',#24536,10.);
#6695=VECTOR('',#24537,10.);
#6696=VECTOR('',#24540,10.);
#6697=VECTOR('',#24541,10.);
#6698=VECTOR('',#24542,10.);
#6699=VECTOR('',#24545,10.);
#6700=VECTOR('',#24546,10.);
#6701=VECTOR('',#24547,10.);
#6702=VECTOR('',#24550,10.);
#6703=VECTOR('',#24551,10.);
#6704=VECTOR('',#24552,10.);
#6705=VECTOR('',#24555,10.);
#6706=VECTOR('',#24556,10.);
#6707=VECTOR('',#24557,10.);
#6708=VECTOR('',#24560,10.);
#6709=VECTOR('',#24561,10.);
#6710=VECTOR('',#24562,10.);
#6711=VECTOR('',#24565,10.);
#6712=VECTOR('',#24566,10.);
#6713=VECTOR('',#24567,10.);
#6714=VECTOR('',#24570,10.);
#6715=VECTOR('',#24571,10.);
#6716=VECTOR('',#24572,10.);
#6717=VECTOR('',#24575,10.);
#6718=VECTOR('',#24576,10.);
#6719=VECTOR('',#24577,10.);
#6720=VECTOR('',#24582,10.);
#6721=VECTOR('',#24587,10.);
#6722=VECTOR('',#24588,10.);
#6723=VECTOR('',#24589,10.);
#6724=VECTOR('',#24592,10.);
#6725=VECTOR('',#24593,10.);
#6726=VECTOR('',#24594,10.);
#6727=VECTOR('',#24597,10.);
#6728=VECTOR('',#24598,10.);
#6729=VECTOR('',#24599,10.);
#6730=VECTOR('',#24602,10.);
#6731=VECTOR('',#24603,10.);
#6732=VECTOR('',#24604,10.);
#6733=VECTOR('',#24607,10.);
#6734=VECTOR('',#24608,10.);
#6735=VECTOR('',#24609,10.);
#6736=VECTOR('',#24612,10.);
#6737=VECTOR('',#24613,10.);
#6738=VECTOR('',#24614,10.);
#6739=VECTOR('',#24617,10.);
#6740=VECTOR('',#24618,10.);
#6741=VECTOR('',#24619,10.);
#6742=VECTOR('',#24622,10.);
#6743=VECTOR('',#24623,10.);
#6744=VECTOR('',#24624,10.);
#6745=VECTOR('',#24625,10.);
#6746=VECTOR('',#24630,10.);
#6747=VECTOR('',#24635,10.);
#6748=VECTOR('',#24636,10.);
#6749=VECTOR('',#24637,10.);
#6750=VECTOR('',#24642,10.);
#6751=VECTOR('',#24647,10.);
#6752=VECTOR('',#24648,10.);
#6753=VECTOR('',#24649,10.);
#6754=VECTOR('',#24650,10.);
#6755=VECTOR('',#24653,10.);
#6756=VECTOR('',#24654,10.);
#6757=VECTOR('',#24655,10.);
#6758=VECTOR('',#24658,10.);
#6759=VECTOR('',#24659,10.);
#6760=VECTOR('',#24660,10.);
#6761=VECTOR('',#24663,10.);
#6762=VECTOR('',#24664,10.);
#6763=VECTOR('',#24665,10.);
#6764=VECTOR('',#24668,10.);
#6765=VECTOR('',#24669,10.);
#6766=VECTOR('',#24670,10.);
#6767=VECTOR('',#24673,10.);
#6768=VECTOR('',#24674,10.);
#6769=VECTOR('',#24675,10.);
#6770=VECTOR('',#24678,10.);
#6771=VECTOR('',#24679,10.);
#6772=VECTOR('',#24682,10.);
#6773=VECTOR('',#24683,10.);
#6774=VECTOR('',#24684,10.);
#6775=VECTOR('',#24687,10.);
#6776=VECTOR('',#24688,10.);
#6777=VECTOR('',#24689,10.);
#6778=VECTOR('',#24692,10.);
#6779=VECTOR('',#24693,10.);
#6780=VECTOR('',#24694,10.);
#6781=VECTOR('',#24697,10.);
#6782=VECTOR('',#24698,10.);
#6783=VECTOR('',#24699,10.);
#6784=VECTOR('',#24702,10.);
#6785=VECTOR('',#24703,10.);
#6786=VECTOR('',#24708,3.25);
#6787=VECTOR('',#24713,10.);
#6788=VECTOR('',#24714,10.);
#6789=VECTOR('',#24715,10.);
#6790=VECTOR('',#24722,10.);
#6791=VECTOR('',#24725,10.);
#6792=VECTOR('',#24726,10.);
#6793=VECTOR('',#24727,10.);
#6794=VECTOR('',#24734,10.);
#6795=VECTOR('',#24737,10.);
#6796=VECTOR('',#24738,10.);
#6797=VECTOR('',#24741,10.);
#6798=VECTOR('',#24742,10.);
#6799=VECTOR('',#24743,10.);
#6800=VECTOR('',#24746,10.);
#6801=VECTOR('',#24747,10.);
#6802=VECTOR('',#24748,10.);
#6803=VECTOR('',#24751,10.);
#6804=VECTOR('',#24752,10.);
#6805=VECTOR('',#24753,10.);
#6806=VECTOR('',#24756,10.);
#6807=VECTOR('',#24757,10.);
#6808=VECTOR('',#24758,10.);
#6809=VECTOR('',#24761,10.);
#6810=VECTOR('',#24762,10.);
#6811=VECTOR('',#24763,10.);
#6812=VECTOR('',#24766,10.);
#6813=VECTOR('',#24767,10.);
#6814=VECTOR('',#24768,10.);
#6815=VECTOR('',#24771,10.);
#6816=VECTOR('',#24772,10.);
#6817=VECTOR('',#24773,10.);
#6818=VECTOR('',#24776,10.);
#6819=VECTOR('',#24777,10.);
#6820=VECTOR('',#24778,10.);
#6821=VECTOR('',#24785,10.);
#6822=VECTOR('',#24788,10.);
#6823=VECTOR('',#24789,10.);
#6824=VECTOR('',#24790,10.);
#6825=VECTOR('',#24793,10.);
#6826=VECTOR('',#24794,10.);
#6827=VECTOR('',#24795,10.);
#6828=VECTOR('',#24798,10.);
#6829=VECTOR('',#24799,10.);
#6830=VECTOR('',#24800,10.);
#6831=VECTOR('',#24803,10.);
#6832=VECTOR('',#24804,10.);
#6833=VECTOR('',#24805,10.);
#6834=VECTOR('',#24808,10.);
#6835=VECTOR('',#24809,10.);
#6836=VECTOR('',#24810,10.);
#6837=VECTOR('',#24813,10.);
#6838=VECTOR('',#24814,10.);
#6839=VECTOR('',#24815,10.);
#6840=VECTOR('',#24818,10.);
#6841=VECTOR('',#24819,10.);
#6842=VECTOR('',#24822,10.);
#6843=VECTOR('',#24823,10.);
#6844=VECTOR('',#24824,10.);
#6845=VECTOR('',#24825,10.);
#6846=VECTOR('',#24828,10.);
#6847=VECTOR('',#24829,10.);
#6848=VECTOR('',#24830,10.);
#6849=VECTOR('',#24833,10.);
#6850=VECTOR('',#24834,10.);
#6851=VECTOR('',#24835,10.);
#6852=VECTOR('',#24838,10.);
#6853=VECTOR('',#24839,10.);
#6854=VECTOR('',#24840,10.);
#6855=VECTOR('',#24841,10.);
#6856=VECTOR('',#24844,10.);
#6857=VECTOR('',#24845,10.);
#6858=VECTOR('',#24846,10.);
#6859=VECTOR('',#24849,10.);
#6860=VECTOR('',#24850,10.);
#6861=VECTOR('',#24851,10.);
#6862=VECTOR('',#24854,10.);
#6863=VECTOR('',#24855,10.);
#6864=VECTOR('',#24856,10.);
#6865=VECTOR('',#24859,10.);
#6866=VECTOR('',#24860,10.);
#6867=VECTOR('',#24861,10.);
#6868=VECTOR('',#24864,10.);
#6869=VECTOR('',#24865,10.);
#6870=VECTOR('',#24866,10.);
#6871=VECTOR('',#24869,10.);
#6872=VECTOR('',#24870,10.);
#6873=VECTOR('',#24871,10.);
#6874=VECTOR('',#24874,10.);
#6875=VECTOR('',#24875,10.);
#6876=VECTOR('',#24876,10.);
#6877=VECTOR('',#24879,10.);
#6878=VECTOR('',#24880,10.);
#6879=VECTOR('',#24881,10.);
#6880=VECTOR('',#24884,10.);
#6881=VECTOR('',#24885,10.);
#6882=VECTOR('',#24886,10.);
#6883=VECTOR('',#24889,10.);
#6884=VECTOR('',#24890,10.);
#6885=VECTOR('',#24891,10.);
#6886=VECTOR('',#24894,10.);
#6887=VECTOR('',#24895,10.);
#6888=VECTOR('',#24896,10.);
#6889=VECTOR('',#24899,10.);
#6890=VECTOR('',#24900,10.);
#6891=VECTOR('',#24901,10.);
#6892=VECTOR('',#24904,10.);
#6893=VECTOR('',#24905,10.);
#6894=VECTOR('',#24906,10.);
#6895=VECTOR('',#24909,10.);
#6896=VECTOR('',#24910,10.);
#6897=VECTOR('',#24911,10.);
#6898=VECTOR('',#24914,10.);
#6899=VECTOR('',#24915,10.);
#6900=VECTOR('',#24916,10.);
#6901=VECTOR('',#24919,10.);
#6902=VECTOR('',#24920,10.);
#6903=VECTOR('',#24921,10.);
#6904=VECTOR('',#24924,10.);
#6905=VECTOR('',#24925,10.);
#6906=VECTOR('',#24928,10.);
#6907=VECTOR('',#24929,10.);
#6908=VECTOR('',#24930,10.);
#6909=VECTOR('',#24931,10.);
#6910=VECTOR('',#24934,10.);
#6911=VECTOR('',#24935,10.);
#6912=VECTOR('',#24936,10.);
#6913=VECTOR('',#24939,10.);
#6914=VECTOR('',#24940,10.);
#6915=VECTOR('',#24941,10.);
#6916=VECTOR('',#24944,10.);
#6917=VECTOR('',#24945,10.);
#6918=VECTOR('',#24948,10.);
#6919=VECTOR('',#24949,10.);
#6920=VECTOR('',#24950,10.);
#6921=VECTOR('',#24951,10.);
#6922=VECTOR('',#24954,10.);
#6923=VECTOR('',#24955,10.);
#6924=VECTOR('',#24956,10.);
#6925=VECTOR('',#24959,10.);
#6926=VECTOR('',#24960,10.);
#6927=VECTOR('',#24961,10.);
#6928=VECTOR('',#24964,10.);
#6929=VECTOR('',#24965,10.);
#6930=VECTOR('',#24966,10.);
#6931=VECTOR('',#24969,10.);
#6932=VECTOR('',#24970,10.);
#6933=VECTOR('',#24971,10.);
#6934=VECTOR('',#24974,10.);
#6935=VECTOR('',#24975,10.);
#6936=VECTOR('',#24976,10.);
#6937=VECTOR('',#24979,10.);
#6938=VECTOR('',#24980,10.);
#6939=VECTOR('',#24981,10.);
#6940=VECTOR('',#24984,10.);
#6941=VECTOR('',#24985,10.);
#6942=VECTOR('',#24986,10.);
#6943=VECTOR('',#24989,10.);
#6944=VECTOR('',#24990,10.);
#6945=VECTOR('',#24991,10.);
#6946=VECTOR('',#24994,10.);
#6947=VECTOR('',#24995,10.);
#6948=VECTOR('',#24996,10.);
#6949=VECTOR('',#24999,10.);
#6950=VECTOR('',#25000,10.);
#6951=VECTOR('',#25005,3.25);
#6952=VECTOR('',#25010,10.);
#6953=VECTOR('',#25011,10.);
#6954=VECTOR('',#25012,10.);
#6955=VECTOR('',#25015,10.);
#6956=VECTOR('',#25016,10.);
#6957=VECTOR('',#25017,10.);
#6958=VECTOR('',#25020,10.);
#6959=VECTOR('',#25021,10.);
#6960=VECTOR('',#25022,10.);
#6961=VECTOR('',#25025,10.);
#6962=VECTOR('',#25026,10.);
#6963=VECTOR('',#25027,10.);
#6964=VECTOR('',#25030,10.);
#6965=VECTOR('',#25031,10.);
#6966=VECTOR('',#25032,10.);
#6967=VECTOR('',#25035,10.);
#6968=VECTOR('',#25036,10.);
#6969=VECTOR('',#25037,10.);
#6970=VECTOR('',#25040,10.);
#6971=VECTOR('',#25041,10.);
#6972=VECTOR('',#25042,10.);
#6973=VECTOR('',#25045,10.);
#6974=VECTOR('',#25046,10.);
#6975=VECTOR('',#25049,10.);
#6976=VECTOR('',#25050,10.);
#6977=VECTOR('',#25051,10.);
#6978=VECTOR('',#25052,10.);
#6979=VECTOR('',#25055,10.);
#6980=VECTOR('',#25056,10.);
#6981=VECTOR('',#25057,10.);
#6982=VECTOR('',#25060,10.);
#6983=VECTOR('',#25061,10.);
#6984=VECTOR('',#25062,10.);
#6985=VECTOR('',#25065,10.);
#6986=VECTOR('',#25066,10.);
#6987=VECTOR('',#25067,10.);
#6988=VECTOR('',#25068,10.);
#6989=VECTOR('',#25071,10.);
#6990=VECTOR('',#25072,10.);
#6991=VECTOR('',#25073,10.);
#6992=VECTOR('',#25076,10.);
#6993=VECTOR('',#25077,10.);
#6994=VECTOR('',#25078,10.);
#6995=VECTOR('',#25081,10.);
#6996=VECTOR('',#25082,10.);
#6997=VECTOR('',#25083,10.);
#6998=VECTOR('',#25086,10.);
#6999=VECTOR('',#25087,10.);
#7000=VECTOR('',#25088,10.);
#7001=VECTOR('',#25091,10.);
#7002=VECTOR('',#25092,10.);
#7003=VECTOR('',#25093,10.);
#7004=VECTOR('',#25096,10.);
#7005=VECTOR('',#25097,10.);
#7006=VECTOR('',#25098,10.);
#7007=VECTOR('',#25101,10.);
#7008=VECTOR('',#25102,10.);
#7009=VECTOR('',#25103,10.);
#7010=VECTOR('',#25106,10.);
#7011=VECTOR('',#25107,10.);
#7012=VECTOR('',#25108,10.);
#7013=VECTOR('',#25111,10.);
#7014=VECTOR('',#25112,10.);
#7015=VECTOR('',#25113,10.);
#7016=VECTOR('',#25116,10.);
#7017=VECTOR('',#25117,10.);
#7018=VECTOR('',#25118,10.);
#7019=VECTOR('',#25121,10.);
#7020=VECTOR('',#25122,10.);
#7021=VECTOR('',#25123,10.);
#7022=VECTOR('',#25126,10.);
#7023=VECTOR('',#25127,10.);
#7024=VECTOR('',#25128,10.);
#7025=VECTOR('',#25131,10.);
#7026=VECTOR('',#25132,10.);
#7027=VECTOR('',#25133,10.);
#7028=VECTOR('',#25136,10.);
#7029=VECTOR('',#25137,10.);
#7030=VECTOR('',#25138,10.);
#7031=VECTOR('',#25141,10.);
#7032=VECTOR('',#25142,10.);
#7033=VECTOR('',#25143,10.);
#7034=VECTOR('',#25146,10.);
#7035=VECTOR('',#25147,10.);
#7036=VECTOR('',#25148,10.);
#7037=VECTOR('',#25151,10.);
#7038=VECTOR('',#25152,10.);
#7039=VECTOR('',#25155,10.);
#7040=VECTOR('',#25156,10.);
#7041=VECTOR('',#25157,10.);
#7042=VECTOR('',#25158,10.);
#7043=VECTOR('',#25161,10.);
#7044=VECTOR('',#25162,10.);
#7045=VECTOR('',#25163,10.);
#7046=VECTOR('',#25166,10.);
#7047=VECTOR('',#25167,10.);
#7048=VECTOR('',#25168,10.);
#7049=VECTOR('',#25171,10.);
#7050=VECTOR('',#25172,10.);
#7051=VECTOR('',#25175,10.);
#7052=VECTOR('',#25176,10.);
#7053=VECTOR('',#25177,10.);
#7054=VECTOR('',#25178,10.);
#7055=VECTOR('',#25181,10.);
#7056=VECTOR('',#25182,10.);
#7057=VECTOR('',#25183,10.);
#7058=VECTOR('',#25186,10.);
#7059=VECTOR('',#25187,10.);
#7060=VECTOR('',#25188,10.);
#7061=VECTOR('',#25191,10.);
#7062=VECTOR('',#25192,10.);
#7063=VECTOR('',#25193,10.);
#7064=VECTOR('',#25196,10.);
#7065=VECTOR('',#25197,10.);
#7066=VECTOR('',#25198,10.);
#7067=VECTOR('',#25201,10.);
#7068=VECTOR('',#25202,10.);
#7069=VECTOR('',#25203,10.);
#7070=VECTOR('',#25206,10.);
#7071=VECTOR('',#25207,10.);
#7072=VECTOR('',#25208,10.);
#7073=VECTOR('',#25211,10.);
#7074=VECTOR('',#25212,10.);
#7075=VECTOR('',#25213,10.);
#7076=VECTOR('',#25216,10.);
#7077=VECTOR('',#25217,10.);
#7078=VECTOR('',#25218,10.);
#7079=VECTOR('',#25221,10.);
#7080=VECTOR('',#25222,10.);
#7081=VECTOR('',#25223,10.);
#7082=VECTOR('',#25226,10.);
#7083=VECTOR('',#25227,10.);
#7084=VECTOR('',#25232,3.25);
#7085=VECTOR('',#25237,10.);
#7086=VECTOR('',#25238,10.);
#7087=VECTOR('',#25239,10.);
#7088=VECTOR('',#25242,10.);
#7089=VECTOR('',#25243,10.);
#7090=VECTOR('',#25244,10.);
#7091=VECTOR('',#25247,10.);
#7092=VECTOR('',#25248,10.);
#7093=VECTOR('',#25249,10.);
#7094=VECTOR('',#25252,10.);
#7095=VECTOR('',#25253,10.);
#7096=VECTOR('',#25254,10.);
#7097=VECTOR('',#25257,10.);
#7098=VECTOR('',#25258,10.);
#7099=VECTOR('',#25259,10.);
#7100=VECTOR('',#25262,10.);
#7101=VECTOR('',#25263,10.);
#7102=VECTOR('',#25264,10.);
#7103=VECTOR('',#25267,10.);
#7104=VECTOR('',#25268,10.);
#7105=VECTOR('',#25269,10.);
#7106=VECTOR('',#25272,10.);
#7107=VECTOR('',#25273,10.);
#7108=VECTOR('',#25276,10.);
#7109=VECTOR('',#25277,10.);
#7110=VECTOR('',#25278,10.);
#7111=VECTOR('',#25279,10.);
#7112=VECTOR('',#25286,10.);
#7113=VECTOR('',#25289,10.);
#7114=VECTOR('',#25290,10.);
#7115=VECTOR('',#25291,10.);
#7116=VECTOR('',#25298,10.);
#7117=VECTOR('',#25301,10.);
#7118=VECTOR('',#25302,10.);
#7119=VECTOR('',#25303,10.);
#7120=VECTOR('',#25304,10.);
#7121=VECTOR('',#25307,10.);
#7122=VECTOR('',#25308,10.);
#7123=VECTOR('',#25309,10.);
#7124=VECTOR('',#25312,10.);
#7125=VECTOR('',#25313,10.);
#7126=VECTOR('',#25314,10.);
#7127=VECTOR('',#25317,10.);
#7128=VECTOR('',#25318,10.);
#7129=VECTOR('',#25319,10.);
#7130=VECTOR('',#25322,10.);
#7131=VECTOR('',#25323,10.);
#7132=VECTOR('',#25324,10.);
#7133=VECTOR('',#25327,10.);
#7134=VECTOR('',#25328,10.);
#7135=VECTOR('',#25329,10.);
#7136=VECTOR('',#25332,10.);
#7137=VECTOR('',#25333,10.);
#7138=VECTOR('',#25336,10.);
#7139=VECTOR('',#25337,10.);
#7140=VECTOR('',#25338,10.);
#7141=VECTOR('',#25341,10.);
#7142=VECTOR('',#25342,10.);
#7143=VECTOR('',#25343,10.);
#7144=VECTOR('',#25346,10.);
#7145=VECTOR('',#25347,10.);
#7146=VECTOR('',#25348,10.);
#7147=VECTOR('',#25351,10.);
#7148=VECTOR('',#25352,10.);
#7149=VECTOR('',#25353,10.);
#7150=VECTOR('',#25358,10.);
#7151=VECTOR('',#25363,10.);
#7152=VECTOR('',#25364,10.);
#7153=VECTOR('',#25365,10.);
#7154=VECTOR('',#25370,10.);
#7155=VECTOR('',#25375,10.);
#7156=VECTOR('',#25376,10.);
#7157=VECTOR('',#25379,10.);
#7158=VECTOR('',#25380,10.);
#7159=VECTOR('',#25381,10.);
#7160=VECTOR('',#25384,10.);
#7161=VECTOR('',#25385,10.);
#7162=VECTOR('',#25386,10.);
#7163=VECTOR('',#25389,10.);
#7164=VECTOR('',#25390,10.);
#7165=VECTOR('',#25391,10.);
#7166=VECTOR('',#25394,10.);
#7167=VECTOR('',#25395,10.);
#7168=VECTOR('',#25396,10.);
#7169=VECTOR('',#25399,10.);
#7170=VECTOR('',#25400,10.);
#7171=VECTOR('',#25401,10.);
#7172=VECTOR('',#25404,10.);
#7173=VECTOR('',#25405,10.);
#7174=VECTOR('',#25406,10.);
#7175=VECTOR('',#25409,10.);
#7176=VECTOR('',#25410,10.);
#7177=VECTOR('',#25411,10.);
#7178=VECTOR('',#25414,10.);
#7179=VECTOR('',#25415,10.);
#7180=VECTOR('',#25416,10.);
#7181=VECTOR('',#25421,10.);
#7182=VECTOR('',#25426,10.);
#7183=VECTOR('',#25427,10.);
#7184=VECTOR('',#25428,10.);
#7185=VECTOR('',#25431,10.);
#7186=VECTOR('',#25432,10.);
#7187=VECTOR('',#25433,10.);
#7188=VECTOR('',#25436,10.);
#7189=VECTOR('',#25437,10.);
#7190=VECTOR('',#25438,10.);
#7191=VECTOR('',#25441,10.);
#7192=VECTOR('',#25442,10.);
#7193=VECTOR('',#25443,10.);
#7194=VECTOR('',#25446,10.);
#7195=VECTOR('',#25447,10.);
#7196=VECTOR('',#25448,10.);
#7197=VECTOR('',#25451,10.);
#7198=VECTOR('',#25452,10.);
#7199=VECTOR('',#25453,10.);
#7200=VECTOR('',#25456,10.);
#7201=VECTOR('',#25457,10.);
#7202=VECTOR('',#25458,10.);
#7203=VECTOR('',#25461,10.);
#7204=VECTOR('',#25462,10.);
#7205=VECTOR('',#25463,10.);
#7206=VECTOR('',#25464,10.);
#7207=VECTOR('',#25465,10.);
#7208=VECTOR('',#25466,10.);
#7209=VECTOR('',#25467,10.);
#7210=VECTOR('',#25468,10.);
#7211=VECTOR('',#25469,10.);
#7212=VECTOR('',#25470,10.);
#7213=VECTOR('',#25471,10.);
#7214=VECTOR('',#25472,10.);
#7215=VECTOR('',#25473,10.);
#7216=VECTOR('',#25474,10.);
#7217=VECTOR('',#25475,10.);
#7218=VECTOR('',#25478,10.);
#7219=VECTOR('',#25479,10.);
#7220=VECTOR('',#25480,10.);
#7221=VECTOR('',#25481,10.);
#7222=VECTOR('',#25482,10.);
#7223=VECTOR('',#25483,10.);
#7224=VECTOR('',#25484,10.);
#7225=VECTOR('',#25485,10.);
#7226=VECTOR('',#25486,10.);
#7227=VECTOR('',#25487,10.);
#7228=VECTOR('',#25488,10.);
#7229=VECTOR('',#25489,10.);
#7230=VECTOR('',#25490,10.);
#7231=VECTOR('',#25493,10.);
#7232=VECTOR('',#25496,10.);
#7233=VECTOR('',#25499,10.);
#7234=VECTOR('',#25502,10.);
#7235=VECTOR('',#25507,10.);
#7236=VECTOR('',#25508,10.);
#7237=VECTOR('',#25509,10.);
#7238=VECTOR('',#25512,10.);
#7239=VECTOR('',#25517,10.);
#7240=VECTOR('',#25518,10.);
#7241=VECTOR('',#25521,10.);
#7242=VECTOR('',#25526,10.);
#7243=VECTOR('',#25527,10.);
#7244=VECTOR('',#25528,10.);
#7245=VECTOR('',#25531,10.);
#7246=VECTOR('',#25532,10.);
#7247=VECTOR('',#25535,10.);
#7248=VECTOR('',#25536,10.);
#7249=VECTOR('',#25539,10.);
#7250=VECTOR('',#25540,10.);
#7251=VECTOR('',#25543,10.);
#7252=VECTOR('',#25544,10.);
#7253=VECTOR('',#25547,10.);
#7254=VECTOR('',#25548,10.);
#7255=VECTOR('',#25551,10.);
#7256=VECTOR('',#25554,10.);
#7257=VECTOR('',#25555,10.);
#7258=VECTOR('',#25558,10.);
#7259=VECTOR('',#25559,10.);
#7260=VECTOR('',#25562,10.);
#7261=VECTOR('',#25563,10.);
#7262=VECTOR('',#25566,10.);
#7263=VECTOR('',#25567,10.);
#7264=VECTOR('',#25570,10.);
#7265=VECTOR('',#25575,3.25);
#7266=VECTOR('',#25578,10.);
#7267=VECTOR('',#25579,10.);
#7268=VECTOR('',#25584,10.);
#7269=VECTOR('',#25587,10.);
#7270=VECTOR('',#25588,10.);
#7271=VECTOR('',#25593,10.);
#7272=VECTOR('',#25596,10.);
#7273=VECTOR('',#25599,10.);
#7274=VECTOR('',#25600,10.);
#7275=VECTOR('',#25603,10.);
#7276=VECTOR('',#25604,10.);
#7277=VECTOR('',#25607,10.);
#7278=VECTOR('',#25608,10.);
#7279=VECTOR('',#25611,10.);
#7280=VECTOR('',#25612,10.);
#7281=VECTOR('',#25615,10.);
#7282=VECTOR('',#25616,10.);
#7283=VECTOR('',#25619,10.);
#7284=VECTOR('',#25620,10.);
#7285=VECTOR('',#25623,10.);
#7286=VECTOR('',#25624,10.);
#7287=VECTOR('',#25627,10.);
#7288=VECTOR('',#25628,10.);
#7289=VECTOR('',#25633,10.);
#7290=VECTOR('',#25636,10.);
#7291=VECTOR('',#25637,10.);
#7292=VECTOR('',#25640,10.);
#7293=VECTOR('',#25641,10.);
#7294=VECTOR('',#25644,10.);
#7295=VECTOR('',#25645,10.);
#7296=VECTOR('',#25648,10.);
#7297=VECTOR('',#25649,10.);
#7298=VECTOR('',#25652,10.);
#7299=VECTOR('',#25653,10.);
#7300=VECTOR('',#25656,10.);
#7301=VECTOR('',#25657,10.);
#7302=VECTOR('',#25660,10.);
#8461=VERTEX_POINT('',#29327);
#8462=VERTEX_POINT('',#29328);
#8463=VERTEX_POINT('',#29330);
#8464=VERTEX_POINT('',#29332);
#8465=VERTEX_POINT('',#29336);
#8466=VERTEX_POINT('',#29338);
#8467=VERTEX_POINT('',#29342);
#8468=VERTEX_POINT('',#29344);
#8469=VERTEX_POINT('',#29348);
#8470=VERTEX_POINT('',#29349);
#8471=VERTEX_POINT('',#29351);
#8472=VERTEX_POINT('',#29353);
#8473=VERTEX_POINT('',#29357);
#8474=VERTEX_POINT('',#29359);
#8475=VERTEX_POINT('',#29363);
#8476=VERTEX_POINT('',#29365);
#8477=VERTEX_POINT('',#29369);
#8478=VERTEX_POINT('',#29371);
#8479=VERTEX_POINT('',#29375);
#8480=VERTEX_POINT('',#29377);
#8481=VERTEX_POINT('',#29381);
#8482=VERTEX_POINT('',#29383);
#8483=VERTEX_POINT('',#29387);
#8484=VERTEX_POINT('',#29388);
#8485=VERTEX_POINT('',#29390);
#8486=VERTEX_POINT('',#29392);
#8487=VERTEX_POINT('',#29396);
#8488=VERTEX_POINT('',#29398);
#8489=VERTEX_POINT('',#29402);
#8490=VERTEX_POINT('',#29404);
#8491=VERTEX_POINT('',#29408);
#8492=VERTEX_POINT('',#29410);
#8493=VERTEX_POINT('',#29414);
#8494=VERTEX_POINT('',#29415);
#8495=VERTEX_POINT('',#29417);
#8496=VERTEX_POINT('',#29419);
#8497=VERTEX_POINT('',#29423);
#8498=VERTEX_POINT('',#29425);
#8499=VERTEX_POINT('',#29429);
#8500=VERTEX_POINT('',#29431);
#8501=VERTEX_POINT('',#29435);
#8502=VERTEX_POINT('',#29437);
#8503=VERTEX_POINT('',#29441);
#8504=VERTEX_POINT('',#29443);
#8505=VERTEX_POINT('',#29450);
#8506=VERTEX_POINT('',#29451);
#8507=VERTEX_POINT('',#29453);
#8508=VERTEX_POINT('',#29455);
#8509=VERTEX_POINT('',#29459);
#8510=VERTEX_POINT('',#29461);
#8511=VERTEX_POINT('',#29465);
#8512=VERTEX_POINT('',#29467);
#8513=VERTEX_POINT('',#29474);
#8514=VERTEX_POINT('',#29475);
#8515=VERTEX_POINT('',#29477);
#8516=VERTEX_POINT('',#29479);
#8517=VERTEX_POINT('',#29483);
#8518=VERTEX_POINT('',#29485);
#8519=VERTEX_POINT('',#29489);
#8520=VERTEX_POINT('',#29491);
#8521=VERTEX_POINT('',#29495);
#8522=VERTEX_POINT('',#29497);
#8523=VERTEX_POINT('',#29501);
#8524=VERTEX_POINT('',#29503);
#8525=VERTEX_POINT('',#29507);
#8526=VERTEX_POINT('',#29509);
#8527=VERTEX_POINT('',#29513);
#8528=VERTEX_POINT('',#29514);
#8529=VERTEX_POINT('',#29516);
#8530=VERTEX_POINT('',#29518);
#8531=VERTEX_POINT('',#29522);
#8532=VERTEX_POINT('',#29524);
#8533=VERTEX_POINT('',#29528);
#8534=VERTEX_POINT('',#29530);
#8535=VERTEX_POINT('',#29537);
#8536=VERTEX_POINT('',#29539);
#8537=VERTEX_POINT('',#29543);
#8538=VERTEX_POINT('',#29545);
#8539=VERTEX_POINT('',#29549);
#8540=VERTEX_POINT('',#29550);
#8541=VERTEX_POINT('',#29552);
#8542=VERTEX_POINT('',#29554);
#8543=VERTEX_POINT('',#29558);
#8544=VERTEX_POINT('',#29560);
#8545=VERTEX_POINT('',#29564);
#8546=VERTEX_POINT('',#29566);
#8547=VERTEX_POINT('',#29570);
#8548=VERTEX_POINT('',#29572);
#8549=VERTEX_POINT('',#29576);
#8550=VERTEX_POINT('',#29578);
#8551=VERTEX_POINT('',#29585);
#8552=VERTEX_POINT('',#29586);
#8553=VERTEX_POINT('',#29588);
#8554=VERTEX_POINT('',#29590);
#8555=VERTEX_POINT('',#29594);
#8556=VERTEX_POINT('',#29596);
#8557=VERTEX_POINT('',#29600);
#8558=VERTEX_POINT('',#29602);
#8559=VERTEX_POINT('',#29606);
#8560=VERTEX_POINT('',#29608);
#8561=VERTEX_POINT('',#29612);
#8562=VERTEX_POINT('',#29613);
#8563=VERTEX_POINT('',#29615);
#8564=VERTEX_POINT('',#29617);
#8565=VERTEX_POINT('',#29621);
#8566=VERTEX_POINT('',#29623);
#8567=VERTEX_POINT('',#29627);
#8568=VERTEX_POINT('',#29629);
#8569=VERTEX_POINT('',#29633);
#8570=VERTEX_POINT('',#29635);
#8571=VERTEX_POINT('',#29639);
#8572=VERTEX_POINT('',#29641);
#8573=VERTEX_POINT('',#29645);
#8574=VERTEX_POINT('',#29647);
#8575=VERTEX_POINT('',#29654);
#8576=VERTEX_POINT('',#29656);
#8577=VERTEX_POINT('',#29660);
#8578=VERTEX_POINT('',#29662);
#8579=VERTEX_POINT('',#29666);
#8580=VERTEX_POINT('',#29668);
#8581=VERTEX_POINT('',#29672);
#8582=VERTEX_POINT('',#29674);
#8583=VERTEX_POINT('',#29678);
#8584=VERTEX_POINT('',#29680);
#8585=VERTEX_POINT('',#29684);
#8586=VERTEX_POINT('',#29686);
#8587=VERTEX_POINT('',#29690);
#8588=VERTEX_POINT('',#29692);
#8589=VERTEX_POINT('',#29699);
#8590=VERTEX_POINT('',#29701);
#8591=VERTEX_POINT('',#29705);
#8592=VERTEX_POINT('',#29707);
#8593=VERTEX_POINT('',#29711);
#8594=VERTEX_POINT('',#29713);
#8595=VERTEX_POINT('',#29717);
#8596=VERTEX_POINT('',#29719);
#8597=VERTEX_POINT('',#29723);
#8598=VERTEX_POINT('',#29725);
#8599=VERTEX_POINT('',#29729);
#8600=VERTEX_POINT('',#29731);
#8601=VERTEX_POINT('',#29735);
#8602=VERTEX_POINT('',#29737);
#8603=VERTEX_POINT('',#29741);
#8604=VERTEX_POINT('',#29743);
#8605=VERTEX_POINT('',#29747);
#8606=VERTEX_POINT('',#29749);
#8607=VERTEX_POINT('',#29753);
#8608=VERTEX_POINT('',#29755);
#8609=VERTEX_POINT('',#29759);
#8610=VERTEX_POINT('',#29761);
#8611=VERTEX_POINT('',#29765);
#8612=VERTEX_POINT('',#29767);
#8613=VERTEX_POINT('',#29771);
#8614=VERTEX_POINT('',#29773);
#8615=VERTEX_POINT('',#29777);
#8616=VERTEX_POINT('',#29779);
#8617=VERTEX_POINT('',#29783);
#8618=VERTEX_POINT('',#29785);
#8619=VERTEX_POINT('',#29789);
#8620=VERTEX_POINT('',#29791);
#8621=VERTEX_POINT('',#29795);
#8622=VERTEX_POINT('',#29796);
#8623=VERTEX_POINT('',#29798);
#8624=VERTEX_POINT('',#29800);
#8625=VERTEX_POINT('',#29804);
#8626=VERTEX_POINT('',#29806);
#8627=VERTEX_POINT('',#29810);
#8628=VERTEX_POINT('',#29812);
#8629=VERTEX_POINT('',#29816);
#8630=VERTEX_POINT('',#29818);
#8631=VERTEX_POINT('',#29822);
#8632=VERTEX_POINT('',#29823);
#8633=VERTEX_POINT('',#29825);
#8634=VERTEX_POINT('',#29827);
#8635=VERTEX_POINT('',#29831);
#8636=VERTEX_POINT('',#29833);
#8637=VERTEX_POINT('',#29837);
#8638=VERTEX_POINT('',#29839);
#8639=VERTEX_POINT('',#29843);
#8640=VERTEX_POINT('',#29845);
#8641=VERTEX_POINT('',#29849);
#8642=VERTEX_POINT('',#29851);
#8643=VERTEX_POINT('',#29855);
#8644=VERTEX_POINT('',#29857);
#8645=VERTEX_POINT('',#29864);
#8646=VERTEX_POINT('',#29866);
#8647=VERTEX_POINT('',#29870);
#8648=VERTEX_POINT('',#29872);
#8649=VERTEX_POINT('',#29876);
#8650=VERTEX_POINT('',#29878);
#8651=VERTEX_POINT('',#29882);
#8652=VERTEX_POINT('',#29884);
#8653=VERTEX_POINT('',#29891);
#8654=VERTEX_POINT('',#29893);
#8655=VERTEX_POINT('',#29897);
#8656=VERTEX_POINT('',#29899);
#8657=VERTEX_POINT('',#29903);
#8658=VERTEX_POINT('',#29905);
#8659=VERTEX_POINT('',#29909);
#8660=VERTEX_POINT('',#29911);
#8661=VERTEX_POINT('',#29915);
#8662=VERTEX_POINT('',#29917);
#8663=VERTEX_POINT('',#29924);
#8664=VERTEX_POINT('',#29926);
#8665=VERTEX_POINT('',#29930);
#8666=VERTEX_POINT('',#29932);
#8667=VERTEX_POINT('',#29936);
#8668=VERTEX_POINT('',#29938);
#8669=VERTEX_POINT('',#29942);
#8670=VERTEX_POINT('',#29944);
#8671=VERTEX_POINT('',#29948);
#8672=VERTEX_POINT('',#29950);
#8673=VERTEX_POINT('',#29954);
#8674=VERTEX_POINT('',#29956);
#8675=VERTEX_POINT('',#29960);
#8676=VERTEX_POINT('',#29962);
#8677=VERTEX_POINT('',#29966);
#8678=VERTEX_POINT('',#29968);
#8679=VERTEX_POINT('',#29972);
#8680=VERTEX_POINT('',#29974);
#8681=VERTEX_POINT('',#29978);
#8682=VERTEX_POINT('',#29980);
#8683=VERTEX_POINT('',#29984);
#8684=VERTEX_POINT('',#29986);
#8685=VERTEX_POINT('',#29990);
#8686=VERTEX_POINT('',#29992);
#8687=VERTEX_POINT('',#29996);
#8688=VERTEX_POINT('',#29998);
#8689=VERTEX_POINT('',#30002);
#8690=VERTEX_POINT('',#30004);
#8691=VERTEX_POINT('',#30008);
#8692=VERTEX_POINT('',#30010);
#8693=VERTEX_POINT('',#30017);
#8694=VERTEX_POINT('',#30018);
#8695=VERTEX_POINT('',#30020);
#8696=VERTEX_POINT('',#30022);
#8697=VERTEX_POINT('',#30026);
#8698=VERTEX_POINT('',#30028);
#8699=VERTEX_POINT('',#30032);
#8700=VERTEX_POINT('',#30034);
#8701=VERTEX_POINT('',#30038);
#8702=VERTEX_POINT('',#30039);
#8703=VERTEX_POINT('',#30041);
#8704=VERTEX_POINT('',#30043);
#8705=VERTEX_POINT('',#30047);
#8706=VERTEX_POINT('',#30049);
#8707=VERTEX_POINT('',#30053);
#8708=VERTEX_POINT('',#30055);
#8709=VERTEX_POINT('',#30059);
#8710=VERTEX_POINT('',#30061);
#8711=VERTEX_POINT('',#30065);
#8712=VERTEX_POINT('',#30067);
#8713=VERTEX_POINT('',#30071);
#8714=VERTEX_POINT('',#30073);
#8715=VERTEX_POINT('',#30077);
#8716=VERTEX_POINT('',#30079);
#8717=VERTEX_POINT('',#30083);
#8718=VERTEX_POINT('',#30085);
#8719=VERTEX_POINT('',#30089);
#8720=VERTEX_POINT('',#30091);
#8721=VERTEX_POINT('',#30095);
#8722=VERTEX_POINT('',#30097);
#8723=VERTEX_POINT('',#30101);
#8724=VERTEX_POINT('',#30103);
#8725=VERTEX_POINT('',#30107);
#8726=VERTEX_POINT('',#30109);
#8727=VERTEX_POINT('',#30113);
#8728=VERTEX_POINT('',#30115);
#8729=VERTEX_POINT('',#30119);
#8730=VERTEX_POINT('',#30121);
#8731=VERTEX_POINT('',#30125);
#8732=VERTEX_POINT('',#30127);
#8733=VERTEX_POINT('',#30131);
#8734=VERTEX_POINT('',#30133);
#8735=VERTEX_POINT('',#30137);
#8736=VERTEX_POINT('',#30139);
#8737=VERTEX_POINT('',#30146);
#8738=VERTEX_POINT('',#30147);
#8739=VERTEX_POINT('',#30149);
#8740=VERTEX_POINT('',#30151);
#8741=VERTEX_POINT('',#30155);
#8742=VERTEX_POINT('',#30157);
#8743=VERTEX_POINT('',#30161);
#8744=VERTEX_POINT('',#30163);
#8745=VERTEX_POINT('',#30170);
#8746=VERTEX_POINT('',#30171);
#8747=VERTEX_POINT('',#30173);
#8748=VERTEX_POINT('',#30175);
#8749=VERTEX_POINT('',#30179);
#8750=VERTEX_POINT('',#30181);
#8751=VERTEX_POINT('',#30185);
#8752=VERTEX_POINT('',#30187);
#8753=VERTEX_POINT('',#30191);
#8754=VERTEX_POINT('',#30193);
#8755=VERTEX_POINT('',#30197);
#8756=VERTEX_POINT('',#30199);
#8757=VERTEX_POINT('',#30203);
#8758=VERTEX_POINT('',#30205);
#8759=VERTEX_POINT('',#30209);
#8760=VERTEX_POINT('',#30211);
#8761=VERTEX_POINT('',#30215);
#8762=VERTEX_POINT('',#30217);
#8763=VERTEX_POINT('',#30221);
#8764=VERTEX_POINT('',#30223);
#8765=VERTEX_POINT('',#30227);
#8766=VERTEX_POINT('',#30229);
#8767=VERTEX_POINT('',#30236);
#8768=VERTEX_POINT('',#30238);
#8769=VERTEX_POINT('',#30242);
#8770=VERTEX_POINT('',#30244);
#8771=VERTEX_POINT('',#30248);
#8772=VERTEX_POINT('',#30250);
#8773=VERTEX_POINT('',#30254);
#8774=VERTEX_POINT('',#30256);
#8775=VERTEX_POINT('',#30260);
#8776=VERTEX_POINT('',#30262);
#8777=VERTEX_POINT('',#30266);
#8778=VERTEX_POINT('',#30268);
#8779=VERTEX_POINT('',#30272);
#8780=VERTEX_POINT('',#30274);
#8781=VERTEX_POINT('',#30278);
#8782=VERTEX_POINT('',#30280);
#8783=VERTEX_POINT('',#30287);
#8784=VERTEX_POINT('',#30288);
#8785=VERTEX_POINT('',#30290);
#8786=VERTEX_POINT('',#30292);
#8787=VERTEX_POINT('',#30296);
#8788=VERTEX_POINT('',#30298);
#8789=VERTEX_POINT('',#30302);
#8790=VERTEX_POINT('',#30304);
#8791=VERTEX_POINT('',#30308);
#8792=VERTEX_POINT('',#30309);
#8793=VERTEX_POINT('',#30311);
#8794=VERTEX_POINT('',#30313);
#8795=VERTEX_POINT('',#30317);
#8796=VERTEX_POINT('',#30319);
#8797=VERTEX_POINT('',#30323);
#8798=VERTEX_POINT('',#30325);
#8799=VERTEX_POINT('',#30329);
#8800=VERTEX_POINT('',#30331);
#8801=VERTEX_POINT('',#30335);
#8802=VERTEX_POINT('',#30337);
#8803=VERTEX_POINT('',#30341);
#8804=VERTEX_POINT('',#30343);
#8805=VERTEX_POINT('',#30347);
#8806=VERTEX_POINT('',#30349);
#8807=VERTEX_POINT('',#30353);
#8808=VERTEX_POINT('',#30355);
#8809=VERTEX_POINT('',#30359);
#8810=VERTEX_POINT('',#30361);
#8811=VERTEX_POINT('',#30365);
#8812=VERTEX_POINT('',#30367);
#8813=VERTEX_POINT('',#30371);
#8814=VERTEX_POINT('',#30373);
#8815=VERTEX_POINT('',#30377);
#8816=VERTEX_POINT('',#30379);
#8817=VERTEX_POINT('',#30383);
#8818=VERTEX_POINT('',#30385);
#8819=VERTEX_POINT('',#30389);
#8820=VERTEX_POINT('',#30391);
#8821=VERTEX_POINT('',#30395);
#8822=VERTEX_POINT('',#30397);
#8823=VERTEX_POINT('',#30401);
#8824=VERTEX_POINT('',#30403);
#8825=VERTEX_POINT('',#30407);
#8826=VERTEX_POINT('',#30409);
#8827=VERTEX_POINT('',#30416);
#8828=VERTEX_POINT('',#30417);
#8829=VERTEX_POINT('',#30419);
#8830=VERTEX_POINT('',#30421);
#8831=VERTEX_POINT('',#30425);
#8832=VERTEX_POINT('',#30427);
#8833=VERTEX_POINT('',#30431);
#8834=VERTEX_POINT('',#30433);
#8835=VERTEX_POINT('',#30440);
#8836=VERTEX_POINT('',#30441);
#8837=VERTEX_POINT('',#30443);
#8838=VERTEX_POINT('',#30445);
#8839=VERTEX_POINT('',#30449);
#8840=VERTEX_POINT('',#30451);
#8841=VERTEX_POINT('',#30455);
#8842=VERTEX_POINT('',#30457);
#8843=VERTEX_POINT('',#30461);
#8844=VERTEX_POINT('',#30463);
#8845=VERTEX_POINT('',#30467);
#8846=VERTEX_POINT('',#30469);
#8847=VERTEX_POINT('',#30473);
#8848=VERTEX_POINT('',#30475);
#8849=VERTEX_POINT('',#30479);
#8850=VERTEX_POINT('',#30481);
#8851=VERTEX_POINT('',#30485);
#8852=VERTEX_POINT('',#30487);
#8853=VERTEX_POINT('',#30491);
#8854=VERTEX_POINT('',#30493);
#8855=VERTEX_POINT('',#30497);
#8856=VERTEX_POINT('',#30499);
#8857=VERTEX_POINT('',#30506);
#8858=VERTEX_POINT('',#30508);
#8859=VERTEX_POINT('',#30512);
#8860=VERTEX_POINT('',#30514);
#8861=VERTEX_POINT('',#30518);
#8862=VERTEX_POINT('',#30520);
#8863=VERTEX_POINT('',#30524);
#8864=VERTEX_POINT('',#30526);
#8865=VERTEX_POINT('',#30530);
#8866=VERTEX_POINT('',#30532);
#8867=VERTEX_POINT('',#30536);
#8868=VERTEX_POINT('',#30538);
#8869=VERTEX_POINT('',#30542);
#8870=VERTEX_POINT('',#30544);
#8871=VERTEX_POINT('',#30548);
#8872=VERTEX_POINT('',#30550);
#8873=VERTEX_POINT('',#30557);
#8874=VERTEX_POINT('',#30558);
#8875=VERTEX_POINT('',#30560);
#8876=VERTEX_POINT('',#30562);
#8877=VERTEX_POINT('',#30566);
#8878=VERTEX_POINT('',#30568);
#8879=VERTEX_POINT('',#30572);
#8880=VERTEX_POINT('',#30574);
#8881=VERTEX_POINT('',#30578);
#8882=VERTEX_POINT('',#30580);
#8883=VERTEX_POINT('',#30584);
#8884=VERTEX_POINT('',#30585);
#8885=VERTEX_POINT('',#30587);
#8886=VERTEX_POINT('',#30589);
#8887=VERTEX_POINT('',#30593);
#8888=VERTEX_POINT('',#30595);
#8889=VERTEX_POINT('',#30599);
#8890=VERTEX_POINT('',#30601);
#8891=VERTEX_POINT('',#30605);
#8892=VERTEX_POINT('',#30607);
#8893=VERTEX_POINT('',#30611);
#8894=VERTEX_POINT('',#30613);
#8895=VERTEX_POINT('',#30617);
#8896=VERTEX_POINT('',#30619);
#8897=VERTEX_POINT('',#30626);
#8898=VERTEX_POINT('',#30628);
#8899=VERTEX_POINT('',#30632);
#8900=VERTEX_POINT('',#30634);
#8901=VERTEX_POINT('',#30638);
#8902=VERTEX_POINT('',#30640);
#8903=VERTEX_POINT('',#30644);
#8904=VERTEX_POINT('',#30646);
#8905=VERTEX_POINT('',#30650);
#8906=VERTEX_POINT('',#30652);
#8907=VERTEX_POINT('',#30656);
#8908=VERTEX_POINT('',#30658);
#8909=VERTEX_POINT('',#30662);
#8910=VERTEX_POINT('',#30664);
#8911=VERTEX_POINT('',#30671);
#8912=VERTEX_POINT('',#30673);
#8913=VERTEX_POINT('',#30677);
#8914=VERTEX_POINT('',#30679);
#8915=VERTEX_POINT('',#30683);
#8916=VERTEX_POINT('',#30685);
#8917=VERTEX_POINT('',#30689);
#8918=VERTEX_POINT('',#30691);
#8919=VERTEX_POINT('',#30695);
#8920=VERTEX_POINT('',#30697);
#8921=VERTEX_POINT('',#30701);
#8922=VERTEX_POINT('',#30703);
#8923=VERTEX_POINT('',#30707);
#8924=VERTEX_POINT('',#30709);
#8925=VERTEX_POINT('',#30713);
#8926=VERTEX_POINT('',#30715);
#8927=VERTEX_POINT('',#30719);
#8928=VERTEX_POINT('',#30721);
#8929=VERTEX_POINT('',#30725);
#8930=VERTEX_POINT('',#30727);
#8931=VERTEX_POINT('',#30731);
#8932=VERTEX_POINT('',#30733);
#8933=VERTEX_POINT('',#30737);
#8934=VERTEX_POINT('',#30739);
#8935=VERTEX_POINT('',#30743);
#8936=VERTEX_POINT('',#30745);
#8937=VERTEX_POINT('',#30749);
#8938=VERTEX_POINT('',#30751);
#8939=VERTEX_POINT('',#30755);
#8940=VERTEX_POINT('',#30757);
#8941=VERTEX_POINT('',#30761);
#8942=VERTEX_POINT('',#30763);
#8943=VERTEX_POINT('',#30767);
#8944=VERTEX_POINT('',#30769);
#8945=VERTEX_POINT('',#30771);
#8946=VERTEX_POINT('',#30773);
#8947=VERTEX_POINT('',#30775);
#8948=VERTEX_POINT('',#30777);
#8949=VERTEX_POINT('',#30779);
#8950=VERTEX_POINT('',#30781);
#8951=VERTEX_POINT('',#30783);
#8952=VERTEX_POINT('',#30785);
#8953=VERTEX_POINT('',#30787);
#8954=VERTEX_POINT('',#30789);
#8955=VERTEX_POINT('',#30791);
#8956=VERTEX_POINT('',#30793);
#8957=VERTEX_POINT('',#30795);
#8958=VERTEX_POINT('',#30797);
#8959=VERTEX_POINT('',#30799);
#8960=VERTEX_POINT('',#30801);
#8961=VERTEX_POINT('',#30803);
#8962=VERTEX_POINT('',#30805);
#8963=VERTEX_POINT('',#30807);
#8964=VERTEX_POINT('',#30809);
#8965=VERTEX_POINT('',#30811);
#8966=VERTEX_POINT('',#30814);
#8967=VERTEX_POINT('',#30816);
#8968=VERTEX_POINT('',#30818);
#8969=VERTEX_POINT('',#30820);
#8970=VERTEX_POINT('',#30823);
#8971=VERTEX_POINT('',#30824);
#8972=VERTEX_POINT('',#30826);
#8973=VERTEX_POINT('',#30828);
#8974=VERTEX_POINT('',#30830);
#8975=VERTEX_POINT('',#30832);
#8976=VERTEX_POINT('',#30834);
#8977=VERTEX_POINT('',#30836);
#8978=VERTEX_POINT('',#30839);
#8979=VERTEX_POINT('',#30842);
#8980=VERTEX_POINT('',#30844);
#8981=VERTEX_POINT('',#30848);
#8982=VERTEX_POINT('',#30852);
#8983=VERTEX_POINT('',#30856);
#8984=VERTEX_POINT('',#30860);
#8985=VERTEX_POINT('',#30862);
#8986=VERTEX_POINT('',#30866);
#8987=VERTEX_POINT('',#30870);
#8988=VERTEX_POINT('',#30874);
#8989=VERTEX_POINT('',#30878);
#8990=VERTEX_POINT('',#30882);
#8991=VERTEX_POINT('',#30888);
#8992=VERTEX_POINT('',#30892);
#8993=VERTEX_POINT('',#30896);
#8994=VERTEX_POINT('',#30900);
#8995=VERTEX_POINT('',#30906);
#8996=VERTEX_POINT('',#30910);
#8997=VERTEX_POINT('',#30914);
#8998=VERTEX_POINT('',#30918);
#8999=VERTEX_POINT('',#30922);
#9000=VERTEX_POINT('',#30928);
#9001=VERTEX_POINT('',#30932);
#9002=VERTEX_POINT('',#30936);
#9003=VERTEX_POINT('',#30940);
#9004=VERTEX_POINT('',#30944);
#9005=VERTEX_POINT('',#30948);
#9006=VERTEX_POINT('',#30952);
#9007=VERTEX_POINT('',#30956);
#9008=VERTEX_POINT('',#30960);
#9009=VERTEX_POINT('',#30964);
#9010=VERTEX_POINT('',#30968);
#9011=VERTEX_POINT('',#30972);
#9012=VERTEX_POINT('',#30976);
#9013=VERTEX_POINT('',#30980);
#9014=VERTEX_POINT('',#30984);
#10778=EDGE_CURVE('',#8461,#8462,#4641,.T.);
#10779=EDGE_CURVE('',#8462,#8463,#4642,.T.);
#10780=EDGE_CURVE('',#8464,#8463,#4643,.T.);
#10781=EDGE_CURVE('',#8461,#8464,#4644,.T.);
#10782=EDGE_CURVE('',#8462,#8465,#4645,.T.);
#10783=EDGE_CURVE('',#8465,#8466,#4646,.T.);
#10784=EDGE_CURVE('',#8463,#8466,#4647,.T.);
#10785=EDGE_CURVE('',#8465,#8467,#4648,.T.);
#10786=EDGE_CURVE('',#8467,#8468,#4649,.T.);
#10787=EDGE_CURVE('',#8466,#8468,#4650,.T.);
#10788=EDGE_CURVE('',#8469,#8470,#4651,.T.);
#10789=EDGE_CURVE('',#8470,#8471,#4652,.T.);
#10790=EDGE_CURVE('',#8472,#8471,#4653,.T.);
#10791=EDGE_CURVE('',#8469,#8472,#4654,.T.);
#10792=EDGE_CURVE('',#8473,#8469,#4655,.T.);
#10793=EDGE_CURVE('',#8474,#8472,#4656,.T.);
#10794=EDGE_CURVE('',#8473,#8474,#4657,.T.);
#10795=EDGE_CURVE('',#8475,#8473,#4658,.T.);
#10796=EDGE_CURVE('',#8476,#8474,#4659,.T.);
#10797=EDGE_CURVE('',#8475,#8476,#4660,.T.);
#10798=EDGE_CURVE('',#8477,#8475,#4661,.T.);
#10799=EDGE_CURVE('',#8478,#8476,#4662,.T.);
#10800=EDGE_CURVE('',#8477,#8478,#4663,.T.);
#10801=EDGE_CURVE('',#8479,#8477,#4664,.T.);
#10802=EDGE_CURVE('',#8480,#8478,#4665,.T.);
#10803=EDGE_CURVE('',#8479,#8480,#4666,.T.);
#10804=EDGE_CURVE('',#8481,#8479,#4667,.T.);
#10805=EDGE_CURVE('',#8482,#8480,#4668,.T.);
#10806=EDGE_CURVE('',#8481,#8482,#4669,.T.);
#10807=EDGE_CURVE('',#8483,#8484,#4670,.T.);
#10808=EDGE_CURVE('',#8483,#8485,#4671,.T.);
#10809=EDGE_CURVE('',#8485,#8486,#4672,.T.);
#10810=EDGE_CURVE('',#8484,#8486,#4673,.T.);
#10811=EDGE_CURVE('',#8484,#8487,#4674,.T.);
#10812=EDGE_CURVE('',#8486,#8488,#4675,.T.);
#10813=EDGE_CURVE('',#8487,#8488,#4676,.T.);
#10814=EDGE_CURVE('',#8487,#8489,#4677,.T.);
#10815=EDGE_CURVE('',#8488,#8490,#4678,.T.);
#10816=EDGE_CURVE('',#8489,#8490,#4679,.T.);
#10817=EDGE_CURVE('',#8481,#8491,#4680,.T.);
#10818=EDGE_CURVE('',#8492,#8482,#4681,.T.);
#10819=EDGE_CURVE('',#8491,#8492,#4682,.T.);
#10820=EDGE_CURVE('',#8493,#8494,#4683,.T.);
#10821=EDGE_CURVE('',#8493,#8495,#4684,.T.);
#10822=EDGE_CURVE('',#8495,#8496,#4685,.T.);
#10823=EDGE_CURVE('',#8494,#8496,#4686,.T.);
#10824=EDGE_CURVE('',#8497,#8493,#4687,.T.);
#10825=EDGE_CURVE('',#8497,#8498,#4688,.T.);
#10826=EDGE_CURVE('',#8498,#8495,#4689,.T.);
#10827=EDGE_CURVE('',#8499,#8497,#4690,.T.);
#10828=EDGE_CURVE('',#8499,#8500,#4691,.T.);
#10829=EDGE_CURVE('',#8500,#8498,#4692,.T.);
#10830=EDGE_CURVE('',#8501,#8499,#4693,.T.);
#10831=EDGE_CURVE('',#8501,#8502,#4694,.T.);
#10832=EDGE_CURVE('',#8502,#8500,#4695,.T.);
#10833=EDGE_CURVE('',#8503,#8501,#4696,.T.);
#10834=EDGE_CURVE('',#8503,#8504,#4697,.T.);
#10835=EDGE_CURVE('',#8504,#8502,#4698,.T.);
#10836=EDGE_CURVE('',#8491,#8503,#4699,.T.);
#10837=EDGE_CURVE('',#8492,#8504,#4700,.T.);
#10838=EDGE_CURVE('',#8505,#8506,#4701,.T.);
#10839=EDGE_CURVE('',#8505,#8507,#4702,.T.);
#10840=EDGE_CURVE('',#8507,#8508,#4703,.T.);
#10841=EDGE_CURVE('',#8506,#8508,#4704,.T.);
#10842=EDGE_CURVE('',#8506,#8509,#4705,.T.);
#10843=EDGE_CURVE('',#8508,#8510,#4706,.T.);
#10844=EDGE_CURVE('',#8509,#8510,#4707,.T.);
#10845=EDGE_CURVE('',#8509,#8511,#4708,.T.);
#10846=EDGE_CURVE('',#8510,#8512,#4709,.T.);
#10847=EDGE_CURVE('',#8511,#8512,#4710,.T.);
#10848=EDGE_CURVE('',#8467,#8511,#4711,.T.);
#10849=EDGE_CURVE('',#8512,#8468,#4712,.T.);
#10850=EDGE_CURVE('',#8513,#8514,#4713,.T.);
#10851=EDGE_CURVE('',#8513,#8515,#4714,.T.);
#10852=EDGE_CURVE('',#8515,#8516,#4715,.T.);
#10853=EDGE_CURVE('',#8514,#8516,#4716,.T.);
#10854=EDGE_CURVE('',#8517,#8513,#4717,.T.);
#10855=EDGE_CURVE('',#8517,#8518,#4718,.T.);
#10856=EDGE_CURVE('',#8518,#8515,#4719,.T.);
#10857=EDGE_CURVE('',#8519,#8517,#4720,.T.);
#10858=EDGE_CURVE('',#8519,#8520,#4721,.T.);
#10859=EDGE_CURVE('',#8520,#8518,#4722,.T.);
#10860=EDGE_CURVE('',#8521,#8519,#4723,.T.);
#10861=EDGE_CURVE('',#8521,#8522,#4724,.T.);
#10862=EDGE_CURVE('',#8522,#8520,#4725,.T.);
#10863=EDGE_CURVE('',#8523,#8521,#4726,.T.);
#10864=EDGE_CURVE('',#8523,#8524,#4727,.T.);
#10865=EDGE_CURVE('',#8524,#8522,#4728,.T.);
#10866=EDGE_CURVE('',#8525,#8523,#4729,.T.);
#10867=EDGE_CURVE('',#8525,#8526,#4730,.T.);
#10868=EDGE_CURVE('',#8526,#8524,#4731,.T.);
#10869=EDGE_CURVE('',#8527,#8528,#4732,.T.);
#10870=EDGE_CURVE('',#8528,#8529,#4733,.T.);
#10871=EDGE_CURVE('',#8530,#8529,#4734,.T.);
#10872=EDGE_CURVE('',#8527,#8530,#4735,.T.);
#10873=EDGE_CURVE('',#8528,#8531,#4736,.T.);
#10874=EDGE_CURVE('',#8531,#8532,#4737,.T.);
#10875=EDGE_CURVE('',#8529,#8532,#4738,.T.);
#10876=EDGE_CURVE('',#8531,#8533,#4739,.T.);
#10877=EDGE_CURVE('',#8533,#8534,#4740,.T.);
#10878=EDGE_CURVE('',#8532,#8534,#4741,.T.);
#10879=EDGE_CURVE('',#8489,#8533,#4742,.T.);
#10880=EDGE_CURVE('',#8534,#8490,#4743,.T.);
#10881=EDGE_CURVE('',#8535,#8535,#3810,.T.);
#10882=EDGE_CURVE('',#8535,#8536,#4744,.T.);
#10883=EDGE_CURVE('',#8536,#8536,#3811,.T.);
#10884=EDGE_CURVE('',#8525,#8537,#4745,.T.);
#10885=EDGE_CURVE('',#8537,#8538,#4746,.T.);
#10886=EDGE_CURVE('',#8538,#8526,#4747,.T.);
#10887=EDGE_CURVE('',#8539,#8540,#4748,.T.);
#10888=EDGE_CURVE('',#8540,#8541,#4749,.T.);
#10889=EDGE_CURVE('',#8542,#8541,#4750,.T.);
#10890=EDGE_CURVE('',#8539,#8542,#4751,.T.);
#10891=EDGE_CURVE('',#8543,#8539,#4752,.T.);
#10892=EDGE_CURVE('',#8544,#8542,#4753,.T.);
#10893=EDGE_CURVE('',#8543,#8544,#4754,.T.);
#10894=EDGE_CURVE('',#8545,#8543,#4755,.T.);
#10895=EDGE_CURVE('',#8546,#8544,#4756,.T.);
#10896=EDGE_CURVE('',#8545,#8546,#4757,.T.);
#10897=EDGE_CURVE('',#8547,#8545,#4758,.T.);
#10898=EDGE_CURVE('',#8548,#8546,#4759,.T.);
#10899=EDGE_CURVE('',#8547,#8548,#4760,.T.);
#10900=EDGE_CURVE('',#8549,#8547,#4761,.T.);
#10901=EDGE_CURVE('',#8550,#8548,#4762,.T.);
#10902=EDGE_CURVE('',#8549,#8550,#4763,.T.);
#10903=EDGE_CURVE('',#8537,#8549,#4764,.T.);
#10904=EDGE_CURVE('',#8538,#8550,#4765,.T.);
#10905=EDGE_CURVE('',#8551,#8552,#4766,.T.);
#10906=EDGE_CURVE('',#8551,#8553,#4767,.T.);
#10907=EDGE_CURVE('',#8553,#8554,#4768,.T.);
#10908=EDGE_CURVE('',#8552,#8554,#4769,.T.);
#10909=EDGE_CURVE('',#8552,#8555,#3812,.T.);
#10910=EDGE_CURVE('',#8554,#8556,#3813,.T.);
#10911=EDGE_CURVE('',#8555,#8556,#4770,.T.);
#10912=EDGE_CURVE('',#8555,#8557,#4771,.T.);
#10913=EDGE_CURVE('',#8556,#8558,#4772,.T.);
#10914=EDGE_CURVE('',#8557,#8558,#4773,.T.);
#10915=EDGE_CURVE('',#8557,#8559,#3814,.T.);
#10916=EDGE_CURVE('',#8558,#8560,#3815,.T.);
#10917=EDGE_CURVE('',#8559,#8560,#4774,.T.);
#10918=EDGE_CURVE('',#8561,#8562,#4775,.T.);
#10919=EDGE_CURVE('',#8561,#8563,#4776,.T.);
#10920=EDGE_CURVE('',#8563,#8564,#4777,.T.);
#10921=EDGE_CURVE('',#8562,#8564,#4778,.T.);
#10922=EDGE_CURVE('',#8562,#8565,#4779,.T.);
#10923=EDGE_CURVE('',#8564,#8566,#4780,.T.);
#10924=EDGE_CURVE('',#8565,#8566,#4781,.T.);
#10925=EDGE_CURVE('',#8565,#8567,#4782,.T.);
#10926=EDGE_CURVE('',#8566,#8568,#4783,.T.);
#10927=EDGE_CURVE('',#8567,#8568,#4784,.T.);
#10928=EDGE_CURVE('',#8567,#8569,#4785,.T.);
#10929=EDGE_CURVE('',#8568,#8570,#4786,.T.);
#10930=EDGE_CURVE('',#8569,#8570,#4787,.T.);
#10931=EDGE_CURVE('',#8569,#8571,#4788,.T.);
#10932=EDGE_CURVE('',#8570,#8572,#4789,.T.);
#10933=EDGE_CURVE('',#8571,#8572,#4790,.T.);
#10934=EDGE_CURVE('',#8571,#8573,#4791,.T.);
#10935=EDGE_CURVE('',#8572,#8574,#4792,.T.);
#10936=EDGE_CURVE('',#8573,#8574,#4793,.T.);
#10937=EDGE_CURVE('',#8540,#8573,#4794,.T.);
#10938=EDGE_CURVE('',#8574,#8541,#4795,.T.);
#10939=EDGE_CURVE('',#8527,#8575,#4796,.T.);
#10940=EDGE_CURVE('',#8576,#8530,#4797,.T.);
#10941=EDGE_CURVE('',#8575,#8576,#4798,.T.);
#10942=EDGE_CURVE('',#8575,#8577,#4799,.T.);
#10943=EDGE_CURVE('',#8576,#8578,#4800,.T.);
#10944=EDGE_CURVE('',#8577,#8578,#4801,.T.);
#10945=EDGE_CURVE('',#8577,#8579,#4802,.T.);
#10946=EDGE_CURVE('',#8578,#8580,#4803,.T.);
#10947=EDGE_CURVE('',#8579,#8580,#4804,.T.);
#10948=EDGE_CURVE('',#8579,#8581,#4805,.T.);
#10949=EDGE_CURVE('',#8580,#8582,#4806,.T.);
#10950=EDGE_CURVE('',#8581,#8582,#4807,.T.);
#10951=EDGE_CURVE('',#8583,#8551,#3816,.T.);
#10952=EDGE_CURVE('',#8583,#8584,#4808,.T.);
#10953=EDGE_CURVE('',#8584,#8553,#3817,.T.);
#10954=EDGE_CURVE('',#8585,#8583,#4809,.T.);
#10955=EDGE_CURVE('',#8585,#8586,#4810,.T.);
#10956=EDGE_CURVE('',#8586,#8584,#4811,.T.);
#10957=EDGE_CURVE('',#8587,#8585,#3818,.T.);
#10958=EDGE_CURVE('',#8587,#8588,#4812,.T.);
#10959=EDGE_CURVE('',#8588,#8586,#3819,.T.);
#10960=EDGE_CURVE('',#8559,#8587,#4813,.T.);
#10961=EDGE_CURVE('',#8560,#8588,#4814,.T.);
#10962=EDGE_CURVE('',#8589,#8561,#4815,.T.);
#10963=EDGE_CURVE('',#8589,#8590,#4816,.T.);
#10964=EDGE_CURVE('',#8590,#8563,#4817,.T.);
#10965=EDGE_CURVE('',#8591,#8589,#4818,.T.);
#10966=EDGE_CURVE('',#8591,#8592,#4819,.T.);
#10967=EDGE_CURVE('',#8592,#8590,#4820,.T.);
#10968=EDGE_CURVE('',#8593,#8591,#4821,.T.);
#10969=EDGE_CURVE('',#8593,#8594,#4822,.T.);
#10970=EDGE_CURVE('',#8594,#8592,#4823,.T.);
#10971=EDGE_CURVE('',#8595,#8593,#4824,.T.);
#10972=EDGE_CURVE('',#8595,#8596,#4825,.T.);
#10973=EDGE_CURVE('',#8596,#8594,#4826,.T.);
#10974=EDGE_CURVE('',#8597,#8595,#4827,.T.);
#10975=EDGE_CURVE('',#8597,#8598,#4828,.T.);
#10976=EDGE_CURVE('',#8598,#8596,#4829,.T.);
#10977=EDGE_CURVE('',#8599,#8597,#4830,.T.);
#10978=EDGE_CURVE('',#8599,#8600,#4831,.T.);
#10979=EDGE_CURVE('',#8600,#8598,#4832,.T.);
#10980=EDGE_CURVE('',#8601,#8599,#4833,.T.);
#10981=EDGE_CURVE('',#8601,#8602,#4834,.T.);
#10982=EDGE_CURVE('',#8602,#8600,#4835,.T.);
#10983=EDGE_CURVE('',#8603,#8601,#4836,.T.);
#10984=EDGE_CURVE('',#8603,#8604,#4837,.T.);
#10985=EDGE_CURVE('',#8604,#8602,#4838,.T.);
#10986=EDGE_CURVE('',#8605,#8603,#3820,.T.);
#10987=EDGE_CURVE('',#8605,#8606,#4839,.T.);
#10988=EDGE_CURVE('',#8606,#8604,#3821,.T.);
#10989=EDGE_CURVE('',#8607,#8605,#4840,.T.);
#10990=EDGE_CURVE('',#8607,#8608,#4841,.T.);
#10991=EDGE_CURVE('',#8608,#8606,#4842,.T.);
#10992=EDGE_CURVE('',#8609,#8607,#4843,.T.);
#10993=EDGE_CURVE('',#8609,#8610,#4844,.T.);
#10994=EDGE_CURVE('',#8610,#8608,#4845,.T.);
#10995=EDGE_CURVE('',#8611,#8609,#4846,.T.);
#10996=EDGE_CURVE('',#8611,#8612,#4847,.T.);
#10997=EDGE_CURVE('',#8612,#8610,#4848,.T.);
#10998=EDGE_CURVE('',#8613,#8611,#4849,.T.);
#10999=EDGE_CURVE('',#8613,#8614,#4850,.T.);
#11000=EDGE_CURVE('',#8614,#8612,#4851,.T.);
#11001=EDGE_CURVE('',#8615,#8613,#4852,.T.);
#11002=EDGE_CURVE('',#8615,#8616,#4853,.T.);
#11003=EDGE_CURVE('',#8616,#8614,#4854,.T.);
#11004=EDGE_CURVE('',#8617,#8615,#4855,.T.);
#11005=EDGE_CURVE('',#8617,#8618,#4856,.T.);
#11006=EDGE_CURVE('',#8618,#8616,#4857,.T.);
#11007=EDGE_CURVE('',#8619,#8617,#4858,.T.);
#11008=EDGE_CURVE('',#8619,#8620,#4859,.T.);
#11009=EDGE_CURVE('',#8620,#8618,#4860,.T.);
#11010=EDGE_CURVE('',#8621,#8622,#4861,.T.);
#11011=EDGE_CURVE('',#8622,#8623,#4862,.T.);
#11012=EDGE_CURVE('',#8624,#8623,#4863,.T.);
#11013=EDGE_CURVE('',#8621,#8624,#4864,.T.);
#11014=EDGE_CURVE('',#8622,#8625,#3822,.T.);
#11015=EDGE_CURVE('',#8625,#8626,#4865,.T.);
#11016=EDGE_CURVE('',#8623,#8626,#3823,.T.);
#11017=EDGE_CURVE('',#8625,#8627,#4866,.T.);
#11018=EDGE_CURVE('',#8627,#8628,#4867,.T.);
#11019=EDGE_CURVE('',#8626,#8628,#4868,.T.);
#11020=EDGE_CURVE('',#8627,#8629,#3824,.T.);
#11021=EDGE_CURVE('',#8629,#8630,#4869,.T.);
#11022=EDGE_CURVE('',#8628,#8630,#3825,.T.);
#11023=EDGE_CURVE('',#8631,#8632,#4870,.T.);
#11024=EDGE_CURVE('',#8632,#8633,#4871,.T.);
#11025=EDGE_CURVE('',#8634,#8633,#4872,.T.);
#11026=EDGE_CURVE('',#8631,#8634,#4873,.T.);
#11027=EDGE_CURVE('',#8632,#8635,#4874,.T.);
#11028=EDGE_CURVE('',#8635,#8636,#4875,.T.);
#11029=EDGE_CURVE('',#8633,#8636,#4876,.T.);
#11030=EDGE_CURVE('',#8635,#8637,#4877,.T.);
#11031=EDGE_CURVE('',#8637,#8638,#4878,.T.);
#11032=EDGE_CURVE('',#8636,#8638,#4879,.T.);
#11033=EDGE_CURVE('',#8637,#8639,#4880,.T.);
#11034=EDGE_CURVE('',#8639,#8640,#4881,.T.);
#11035=EDGE_CURVE('',#8638,#8640,#4882,.T.);
#11036=EDGE_CURVE('',#8639,#8641,#4883,.T.);
#11037=EDGE_CURVE('',#8641,#8642,#4884,.T.);
#11038=EDGE_CURVE('',#8640,#8642,#4885,.T.);
#11039=EDGE_CURVE('',#8641,#8643,#4886,.T.);
#11040=EDGE_CURVE('',#8643,#8644,#4887,.T.);
#11041=EDGE_CURVE('',#8642,#8644,#4888,.T.);
#11042=EDGE_CURVE('',#8494,#8643,#4889,.T.);
#11043=EDGE_CURVE('',#8644,#8496,#4890,.T.);
#11044=EDGE_CURVE('',#8483,#8645,#4891,.T.);
#11045=EDGE_CURVE('',#8645,#8646,#4892,.T.);
#11046=EDGE_CURVE('',#8646,#8485,#4893,.T.);
#11047=EDGE_CURVE('',#8645,#8647,#4894,.T.);
#11048=EDGE_CURVE('',#8647,#8648,#4895,.T.);
#11049=EDGE_CURVE('',#8646,#8648,#4896,.T.);
#11050=EDGE_CURVE('',#8647,#8649,#4897,.T.);
#11051=EDGE_CURVE('',#8649,#8650,#4898,.T.);
#11052=EDGE_CURVE('',#8648,#8650,#4899,.T.);
#11053=EDGE_CURVE('',#8649,#8651,#4900,.T.);
#11054=EDGE_CURVE('',#8651,#8652,#4901,.T.);
#11055=EDGE_CURVE('',#8650,#8652,#4902,.T.);
#11056=EDGE_CURVE('',#8581,#8651,#4903,.T.);
#11057=EDGE_CURVE('',#8652,#8582,#4904,.T.);
#11058=EDGE_CURVE('',#8653,#8653,#3826,.T.);
#11059=EDGE_CURVE('',#8653,#8654,#4905,.T.);
#11060=EDGE_CURVE('',#8654,#8654,#3827,.T.);
#11061=EDGE_CURVE('',#8619,#8655,#4906,.T.);
#11062=EDGE_CURVE('',#8655,#8656,#4907,.T.);
#11063=EDGE_CURVE('',#8656,#8620,#4908,.T.);
#11064=EDGE_CURVE('',#8657,#8621,#3828,.T.);
#11065=EDGE_CURVE('',#8658,#8624,#3829,.T.);
#11066=EDGE_CURVE('',#8657,#8658,#4909,.T.);
#11067=EDGE_CURVE('',#8659,#8657,#4910,.T.);
#11068=EDGE_CURVE('',#8660,#8658,#4911,.T.);
#11069=EDGE_CURVE('',#8659,#8660,#4912,.T.);
#11070=EDGE_CURVE('',#8661,#8659,#3830,.T.);
#11071=EDGE_CURVE('',#8662,#8660,#3831,.T.);
#11072=EDGE_CURVE('',#8661,#8662,#4913,.T.);
#11073=EDGE_CURVE('',#8629,#8661,#4914,.T.);
#11074=EDGE_CURVE('',#8630,#8662,#4915,.T.);
#11075=EDGE_CURVE('',#8663,#8631,#4916,.T.);
#11076=EDGE_CURVE('',#8664,#8634,#4917,.T.);
#11077=EDGE_CURVE('',#8663,#8664,#4918,.T.);
#11078=EDGE_CURVE('',#8665,#8663,#4919,.T.);
#11079=EDGE_CURVE('',#8666,#8664,#4920,.T.);
#11080=EDGE_CURVE('',#8665,#8666,#4921,.T.);
#11081=EDGE_CURVE('',#8667,#8665,#4922,.T.);
#11082=EDGE_CURVE('',#8668,#8666,#4923,.T.);
#11083=EDGE_CURVE('',#8667,#8668,#4924,.T.);
#11084=EDGE_CURVE('',#8669,#8667,#4925,.T.);
#11085=EDGE_CURVE('',#8670,#8668,#4926,.T.);
#11086=EDGE_CURVE('',#8669,#8670,#4927,.T.);
#11087=EDGE_CURVE('',#8671,#8669,#4928,.T.);
#11088=EDGE_CURVE('',#8672,#8670,#4929,.T.);
#11089=EDGE_CURVE('',#8671,#8672,#4930,.T.);
#11090=EDGE_CURVE('',#8673,#8671,#4931,.T.);
#11091=EDGE_CURVE('',#8674,#8672,#4932,.T.);
#11092=EDGE_CURVE('',#8673,#8674,#4933,.T.);
#11093=EDGE_CURVE('',#8675,#8673,#4934,.T.);
#11094=EDGE_CURVE('',#8676,#8674,#4935,.T.);
#11095=EDGE_CURVE('',#8675,#8676,#4936,.T.);
#11096=EDGE_CURVE('',#8677,#8675,#4937,.T.);
#11097=EDGE_CURVE('',#8678,#8676,#4938,.T.);
#11098=EDGE_CURVE('',#8677,#8678,#4939,.T.);
#11099=EDGE_CURVE('',#8679,#8677,#3832,.T.);
#11100=EDGE_CURVE('',#8680,#8678,#3833,.T.);
#11101=EDGE_CURVE('',#8679,#8680,#4940,.T.);
#11102=EDGE_CURVE('',#8681,#8679,#4941,.T.);
#11103=EDGE_CURVE('',#8682,#8680,#4942,.T.);
#11104=EDGE_CURVE('',#8681,#8682,#4943,.T.);
#11105=EDGE_CURVE('',#8683,#8681,#4944,.T.);
#11106=EDGE_CURVE('',#8684,#8682,#4945,.T.);
#11107=EDGE_CURVE('',#8683,#8684,#4946,.T.);
#11108=EDGE_CURVE('',#8685,#8683,#4947,.T.);
#11109=EDGE_CURVE('',#8686,#8684,#4948,.T.);
#11110=EDGE_CURVE('',#8685,#8686,#4949,.T.);
#11111=EDGE_CURVE('',#8687,#8685,#4950,.T.);
#11112=EDGE_CURVE('',#8688,#8686,#4951,.T.);
#11113=EDGE_CURVE('',#8687,#8688,#4952,.T.);
#11114=EDGE_CURVE('',#8689,#8687,#4953,.T.);
#11115=EDGE_CURVE('',#8690,#8688,#4954,.T.);
#11116=EDGE_CURVE('',#8689,#8690,#4955,.T.);
#11117=EDGE_CURVE('',#8691,#8689,#4956,.T.);
#11118=EDGE_CURVE('',#8692,#8690,#4957,.T.);
#11119=EDGE_CURVE('',#8691,#8692,#4958,.T.);
#11120=EDGE_CURVE('',#8655,#8691,#4959,.T.);
#11121=EDGE_CURVE('',#8656,#8692,#4960,.T.);
#11122=EDGE_CURVE('',#8693,#8694,#4961,.T.);
#11123=EDGE_CURVE('',#8694,#8695,#4962,.T.);
#11124=EDGE_CURVE('',#8696,#8695,#4963,.T.);
#11125=EDGE_CURVE('',#8693,#8696,#4964,.T.);
#11126=EDGE_CURVE('',#8694,#8697,#4965,.T.);
#11127=EDGE_CURVE('',#8697,#8698,#4966,.T.);
#11128=EDGE_CURVE('',#8695,#8698,#4967,.T.);
#11129=EDGE_CURVE('',#8697,#8699,#4968,.T.);
#11130=EDGE_CURVE('',#8699,#8700,#4969,.T.);
#11131=EDGE_CURVE('',#8698,#8700,#4970,.T.);
#11132=EDGE_CURVE('',#8701,#8702,#4971,.T.);
#11133=EDGE_CURVE('',#8702,#8703,#4972,.T.);
#11134=EDGE_CURVE('',#8704,#8703,#4973,.T.);
#11135=EDGE_CURVE('',#8701,#8704,#4974,.T.);
#11136=EDGE_CURVE('',#8705,#8701,#4975,.T.);
#11137=EDGE_CURVE('',#8706,#8704,#4976,.T.);
#11138=EDGE_CURVE('',#8705,#8706,#4977,.T.);
#11139=EDGE_CURVE('',#8707,#8705,#4978,.T.);
#11140=EDGE_CURVE('',#8708,#8706,#4979,.T.);
#11141=EDGE_CURVE('',#8707,#8708,#4980,.T.);
#11142=EDGE_CURVE('',#8709,#8707,#4981,.T.);
#11143=EDGE_CURVE('',#8710,#8708,#4982,.T.);
#11144=EDGE_CURVE('',#8709,#8710,#4983,.T.);
#11145=EDGE_CURVE('',#8711,#8709,#4984,.T.);
#11146=EDGE_CURVE('',#8712,#8710,#4985,.T.);
#11147=EDGE_CURVE('',#8711,#8712,#4986,.T.);
#11148=EDGE_CURVE('',#8713,#8711,#4987,.T.);
#11149=EDGE_CURVE('',#8714,#8712,#4988,.T.);
#11150=EDGE_CURVE('',#8713,#8714,#4989,.T.);
#11151=EDGE_CURVE('',#8461,#8715,#4990,.T.);
#11152=EDGE_CURVE('',#8464,#8716,#4991,.T.);
#11153=EDGE_CURVE('',#8715,#8716,#4992,.T.);
#11154=EDGE_CURVE('',#8715,#8717,#4993,.T.);
#11155=EDGE_CURVE('',#8716,#8718,#4994,.T.);
#11156=EDGE_CURVE('',#8717,#8718,#4995,.T.);
#11157=EDGE_CURVE('',#8717,#8719,#4996,.T.);
#11158=EDGE_CURVE('',#8718,#8720,#4997,.T.);
#11159=EDGE_CURVE('',#8719,#8720,#4998,.T.);
#11160=EDGE_CURVE('',#8719,#8721,#4999,.T.);
#11161=EDGE_CURVE('',#8720,#8722,#5000,.T.);
#11162=EDGE_CURVE('',#8721,#8722,#5001,.T.);
#11163=EDGE_CURVE('',#8713,#8723,#5002,.T.);
#11164=EDGE_CURVE('',#8724,#8714,#5003,.T.);
#11165=EDGE_CURVE('',#8723,#8724,#5004,.T.);
#11166=EDGE_CURVE('',#8470,#8725,#5005,.T.);
#11167=EDGE_CURVE('',#8725,#8726,#5006,.T.);
#11168=EDGE_CURVE('',#8726,#8471,#5007,.T.);
#11169=EDGE_CURVE('',#8727,#8725,#5008,.T.);
#11170=EDGE_CURVE('',#8727,#8728,#5009,.T.);
#11171=EDGE_CURVE('',#8728,#8726,#5010,.T.);
#11172=EDGE_CURVE('',#8729,#8727,#5011,.T.);
#11173=EDGE_CURVE('',#8729,#8730,#5012,.T.);
#11174=EDGE_CURVE('',#8730,#8728,#5013,.T.);
#11175=EDGE_CURVE('',#8731,#8729,#5014,.T.);
#11176=EDGE_CURVE('',#8731,#8732,#5015,.T.);
#11177=EDGE_CURVE('',#8732,#8730,#5016,.T.);
#11178=EDGE_CURVE('',#8733,#8731,#5017,.T.);
#11179=EDGE_CURVE('',#8733,#8734,#5018,.T.);
#11180=EDGE_CURVE('',#8734,#8732,#5019,.T.);
#11181=EDGE_CURVE('',#8735,#8733,#5020,.T.);
#11182=EDGE_CURVE('',#8735,#8736,#5021,.T.);
#11183=EDGE_CURVE('',#8736,#8734,#5022,.T.);
#11184=EDGE_CURVE('',#8723,#8735,#5023,.T.);
#11185=EDGE_CURVE('',#8724,#8736,#5024,.T.);
#11186=EDGE_CURVE('',#8737,#8738,#5025,.T.);
#11187=EDGE_CURVE('',#8737,#8739,#5026,.T.);
#11188=EDGE_CURVE('',#8739,#8740,#5027,.T.);
#11189=EDGE_CURVE('',#8738,#8740,#5028,.T.);
#11190=EDGE_CURVE('',#8738,#8741,#5029,.T.);
#11191=EDGE_CURVE('',#8740,#8742,#5030,.T.);
#11192=EDGE_CURVE('',#8741,#8742,#5031,.T.);
#11193=EDGE_CURVE('',#8741,#8743,#5032,.T.);
#11194=EDGE_CURVE('',#8742,#8744,#5033,.T.);
#11195=EDGE_CURVE('',#8743,#8744,#5034,.T.);
#11196=EDGE_CURVE('',#8699,#8743,#5035,.T.);
#11197=EDGE_CURVE('',#8744,#8700,#5036,.T.);
#11198=EDGE_CURVE('',#8745,#8746,#5037,.T.);
#11199=EDGE_CURVE('',#8745,#8747,#5038,.T.);
#11200=EDGE_CURVE('',#8747,#8748,#5039,.T.);
#11201=EDGE_CURVE('',#8746,#8748,#5040,.T.);
#11202=EDGE_CURVE('',#8749,#8745,#5041,.T.);
#11203=EDGE_CURVE('',#8749,#8750,#5042,.T.);
#11204=EDGE_CURVE('',#8750,#8747,#5043,.T.);
#11205=EDGE_CURVE('',#8751,#8749,#5044,.T.);
#11206=EDGE_CURVE('',#8751,#8752,#5045,.T.);
#11207=EDGE_CURVE('',#8752,#8750,#5046,.T.);
#11208=EDGE_CURVE('',#8753,#8751,#5047,.T.);
#11209=EDGE_CURVE('',#8753,#8754,#5048,.T.);
#11210=EDGE_CURVE('',#8754,#8752,#5049,.T.);
#11211=EDGE_CURVE('',#8755,#8753,#5050,.T.);
#11212=EDGE_CURVE('',#8755,#8756,#5051,.T.);
#11213=EDGE_CURVE('',#8756,#8754,#5052,.T.);
#11214=EDGE_CURVE('',#8757,#8755,#5053,.T.);
#11215=EDGE_CURVE('',#8757,#8758,#5054,.T.);
#11216=EDGE_CURVE('',#8758,#8756,#5055,.T.);
#11217=EDGE_CURVE('',#8505,#8759,#5056,.T.);
#11218=EDGE_CURVE('',#8759,#8760,#5057,.T.);
#11219=EDGE_CURVE('',#8760,#8507,#5058,.T.);
#11220=EDGE_CURVE('',#8759,#8761,#5059,.T.);
#11221=EDGE_CURVE('',#8761,#8762,#5060,.T.);
#11222=EDGE_CURVE('',#8760,#8762,#5061,.T.);
#11223=EDGE_CURVE('',#8761,#8763,#5062,.T.);
#11224=EDGE_CURVE('',#8763,#8764,#5063,.T.);
#11225=EDGE_CURVE('',#8762,#8764,#5064,.T.);
#11226=EDGE_CURVE('',#8763,#8765,#5065,.T.);
#11227=EDGE_CURVE('',#8765,#8766,#5066,.T.);
#11228=EDGE_CURVE('',#8764,#8766,#5067,.T.);
#11229=EDGE_CURVE('',#8721,#8765,#5068,.T.);
#11230=EDGE_CURVE('',#8766,#8722,#5069,.T.);
#11231=EDGE_CURVE('',#8767,#8767,#3834,.T.);
#11232=EDGE_CURVE('',#8767,#8768,#5070,.T.);
#11233=EDGE_CURVE('',#8768,#8768,#3835,.T.);
#11234=EDGE_CURVE('',#8757,#8769,#5071,.T.);
#11235=EDGE_CURVE('',#8769,#8770,#5072,.T.);
#11236=EDGE_CURVE('',#8770,#8758,#5073,.T.);
#11237=EDGE_CURVE('',#8514,#8771,#5074,.T.);
#11238=EDGE_CURVE('',#8772,#8516,#5075,.T.);
#11239=EDGE_CURVE('',#8771,#8772,#5076,.T.);
#11240=EDGE_CURVE('',#8773,#8771,#5077,.T.);
#11241=EDGE_CURVE('',#8774,#8772,#5078,.T.);
#11242=EDGE_CURVE('',#8773,#8774,#5079,.T.);
#11243=EDGE_CURVE('',#8775,#8773,#5080,.T.);
#11244=EDGE_CURVE('',#8776,#8774,#5081,.T.);
#11245=EDGE_CURVE('',#8775,#8776,#5082,.T.);
#11246=EDGE_CURVE('',#8777,#8775,#5083,.T.);
#11247=EDGE_CURVE('',#8778,#8776,#5084,.T.);
#11248=EDGE_CURVE('',#8777,#8778,#5085,.T.);
#11249=EDGE_CURVE('',#8779,#8777,#5086,.T.);
#11250=EDGE_CURVE('',#8780,#8778,#5087,.T.);
#11251=EDGE_CURVE('',#8779,#8780,#5088,.T.);
#11252=EDGE_CURVE('',#8781,#8779,#5089,.T.);
#11253=EDGE_CURVE('',#8782,#8780,#5090,.T.);
#11254=EDGE_CURVE('',#8781,#8782,#5091,.T.);
#11255=EDGE_CURVE('',#8769,#8781,#5092,.T.);
#11256=EDGE_CURVE('',#8770,#8782,#5093,.T.);
#11257=EDGE_CURVE('',#8783,#8784,#5094,.T.);
#11258=EDGE_CURVE('',#8784,#8785,#5095,.T.);
#11259=EDGE_CURVE('',#8786,#8785,#5096,.T.);
#11260=EDGE_CURVE('',#8783,#8786,#5097,.T.);
#11261=EDGE_CURVE('',#8784,#8787,#5098,.T.);
#11262=EDGE_CURVE('',#8787,#8788,#5099,.T.);
#11263=EDGE_CURVE('',#8785,#8788,#5100,.T.);
#11264=EDGE_CURVE('',#8787,#8789,#5101,.T.);
#11265=EDGE_CURVE('',#8789,#8790,#5102,.T.);
#11266=EDGE_CURVE('',#8788,#8790,#5103,.T.);
#11267=EDGE_CURVE('',#8791,#8792,#5104,.T.);
#11268=EDGE_CURVE('',#8792,#8793,#5105,.T.);
#11269=EDGE_CURVE('',#8794,#8793,#5106,.T.);
#11270=EDGE_CURVE('',#8791,#8794,#5107,.T.);
#11271=EDGE_CURVE('',#8795,#8791,#5108,.T.);
#11272=EDGE_CURVE('',#8796,#8794,#5109,.T.);
#11273=EDGE_CURVE('',#8795,#8796,#5110,.T.);
#11274=EDGE_CURVE('',#8797,#8795,#5111,.T.);
#11275=EDGE_CURVE('',#8798,#8796,#5112,.T.);
#11276=EDGE_CURVE('',#8797,#8798,#5113,.T.);
#11277=EDGE_CURVE('',#8799,#8797,#5114,.T.);
#11278=EDGE_CURVE('',#8800,#8798,#5115,.T.);
#11279=EDGE_CURVE('',#8799,#8800,#5116,.T.);
#11280=EDGE_CURVE('',#8801,#8799,#5117,.T.);
#11281=EDGE_CURVE('',#8802,#8800,#5118,.T.);
#11282=EDGE_CURVE('',#8801,#8802,#5119,.T.);
#11283=EDGE_CURVE('',#8803,#8801,#5120,.T.);
#11284=EDGE_CURVE('',#8804,#8802,#5121,.T.);
#11285=EDGE_CURVE('',#8803,#8804,#5122,.T.);
#11286=EDGE_CURVE('',#8693,#8805,#5123,.T.);
#11287=EDGE_CURVE('',#8696,#8806,#5124,.T.);
#11288=EDGE_CURVE('',#8805,#8806,#5125,.T.);
#11289=EDGE_CURVE('',#8805,#8807,#5126,.T.);
#11290=EDGE_CURVE('',#8806,#8808,#5127,.T.);
#11291=EDGE_CURVE('',#8807,#8808,#5128,.T.);
#11292=EDGE_CURVE('',#8807,#8809,#5129,.T.);
#11293=EDGE_CURVE('',#8808,#8810,#5130,.T.);
#11294=EDGE_CURVE('',#8809,#8810,#5131,.T.);
#11295=EDGE_CURVE('',#8809,#8811,#5132,.T.);
#11296=EDGE_CURVE('',#8810,#8812,#5133,.T.);
#11297=EDGE_CURVE('',#8811,#8812,#5134,.T.);
#11298=EDGE_CURVE('',#8803,#8813,#5135,.T.);
#11299=EDGE_CURVE('',#8814,#8804,#5136,.T.);
#11300=EDGE_CURVE('',#8813,#8814,#5137,.T.);
#11301=EDGE_CURVE('',#8702,#8815,#5138,.T.);
#11302=EDGE_CURVE('',#8815,#8816,#5139,.T.);
#11303=EDGE_CURVE('',#8816,#8703,#5140,.T.);
#11304=EDGE_CURVE('',#8817,#8815,#5141,.T.);
#11305=EDGE_CURVE('',#8817,#8818,#5142,.T.);
#11306=EDGE_CURVE('',#8818,#8816,#5143,.T.);
#11307=EDGE_CURVE('',#8819,#8817,#5144,.T.);
#11308=EDGE_CURVE('',#8819,#8820,#5145,.T.);
#11309=EDGE_CURVE('',#8820,#8818,#5146,.T.);
#11310=EDGE_CURVE('',#8821,#8819,#5147,.T.);
#11311=EDGE_CURVE('',#8821,#8822,#5148,.T.);
#11312=EDGE_CURVE('',#8822,#8820,#5149,.T.);
#11313=EDGE_CURVE('',#8823,#8821,#5150,.T.);
#11314=EDGE_CURVE('',#8823,#8824,#5151,.T.);
#11315=EDGE_CURVE('',#8824,#8822,#5152,.T.);
#11316=EDGE_CURVE('',#8825,#8823,#5153,.T.);
#11317=EDGE_CURVE('',#8825,#8826,#5154,.T.);
#11318=EDGE_CURVE('',#8826,#8824,#5155,.T.);
#11319=EDGE_CURVE('',#8813,#8825,#5156,.T.);
#11320=EDGE_CURVE('',#8814,#8826,#5157,.T.);
#11321=EDGE_CURVE('',#8827,#8828,#5158,.T.);
#11322=EDGE_CURVE('',#8827,#8829,#5159,.T.);
#11323=EDGE_CURVE('',#8829,#8830,#5160,.T.);
#11324=EDGE_CURVE('',#8828,#8830,#5161,.T.);
#11325=EDGE_CURVE('',#8828,#8831,#5162,.T.);
#11326=EDGE_CURVE('',#8830,#8832,#5163,.T.);
#11327=EDGE_CURVE('',#8831,#8832,#5164,.T.);
#11328=EDGE_CURVE('',#8831,#8833,#5165,.T.);
#11329=EDGE_CURVE('',#8832,#8834,#5166,.T.);
#11330=EDGE_CURVE('',#8833,#8834,#5167,.T.);
#11331=EDGE_CURVE('',#8789,#8833,#5168,.T.);
#11332=EDGE_CURVE('',#8834,#8790,#5169,.T.);
#11333=EDGE_CURVE('',#8835,#8836,#5170,.T.);
#11334=EDGE_CURVE('',#8835,#8837,#5171,.T.);
#11335=EDGE_CURVE('',#8837,#8838,#5172,.T.);
#11336=EDGE_CURVE('',#8836,#8838,#5173,.T.);
#11337=EDGE_CURVE('',#8839,#8835,#5174,.T.);
#11338=EDGE_CURVE('',#8839,#8840,#5175,.T.);
#11339=EDGE_CURVE('',#8840,#8837,#5176,.T.);
#11340=EDGE_CURVE('',#8841,#8839,#5177,.T.);
#11341=EDGE_CURVE('',#8841,#8842,#5178,.T.);
#11342=EDGE_CURVE('',#8842,#8840,#5179,.T.);
#11343=EDGE_CURVE('',#8843,#8841,#5180,.T.);
#11344=EDGE_CURVE('',#8843,#8844,#5181,.T.);
#11345=EDGE_CURVE('',#8844,#8842,#5182,.T.);
#11346=EDGE_CURVE('',#8845,#8843,#5183,.T.);
#11347=EDGE_CURVE('',#8845,#8846,#5184,.T.);
#11348=EDGE_CURVE('',#8846,#8844,#5185,.T.);
#11349=EDGE_CURVE('',#8847,#8845,#5186,.T.);
#11350=EDGE_CURVE('',#8847,#8848,#5187,.T.);
#11351=EDGE_CURVE('',#8848,#8846,#5188,.T.);
#11352=EDGE_CURVE('',#8737,#8849,#5189,.T.);
#11353=EDGE_CURVE('',#8849,#8850,#5190,.T.);
#11354=EDGE_CURVE('',#8850,#8739,#5191,.T.);
#11355=EDGE_CURVE('',#8849,#8851,#5192,.T.);
#11356=EDGE_CURVE('',#8851,#8852,#5193,.T.);
#11357=EDGE_CURVE('',#8850,#8852,#5194,.T.);
#11358=EDGE_CURVE('',#8851,#8853,#5195,.T.);
#11359=EDGE_CURVE('',#8853,#8854,#5196,.T.);
#11360=EDGE_CURVE('',#8852,#8854,#5197,.T.);
#11361=EDGE_CURVE('',#8853,#8855,#5198,.T.);
#11362=EDGE_CURVE('',#8855,#8856,#5199,.T.);
#11363=EDGE_CURVE('',#8854,#8856,#5200,.T.);
#11364=EDGE_CURVE('',#8811,#8855,#5201,.T.);
#11365=EDGE_CURVE('',#8856,#8812,#5202,.T.);
#11366=EDGE_CURVE('',#8857,#8857,#3836,.T.);
#11367=EDGE_CURVE('',#8857,#8858,#5203,.T.);
#11368=EDGE_CURVE('',#8858,#8858,#3837,.T.);
#11369=EDGE_CURVE('',#8847,#8859,#5204,.T.);
#11370=EDGE_CURVE('',#8859,#8860,#5205,.T.);
#11371=EDGE_CURVE('',#8860,#8848,#5206,.T.);
#11372=EDGE_CURVE('',#8746,#8861,#5207,.T.);
#11373=EDGE_CURVE('',#8862,#8748,#5208,.T.);
#11374=EDGE_CURVE('',#8861,#8862,#5209,.T.);
#11375=EDGE_CURVE('',#8863,#8861,#5210,.T.);
#11376=EDGE_CURVE('',#8864,#8862,#5211,.T.);
#11377=EDGE_CURVE('',#8863,#8864,#5212,.T.);
#11378=EDGE_CURVE('',#8865,#8863,#5213,.T.);
#11379=EDGE_CURVE('',#8866,#8864,#5214,.T.);
#11380=EDGE_CURVE('',#8865,#8866,#5215,.T.);
#11381=EDGE_CURVE('',#8867,#8865,#5216,.T.);
#11382=EDGE_CURVE('',#8868,#8866,#5217,.T.);
#11383=EDGE_CURVE('',#8867,#8868,#5218,.T.);
#11384=EDGE_CURVE('',#8869,#8867,#5219,.T.);
#11385=EDGE_CURVE('',#8870,#8868,#5220,.T.);
#11386=EDGE_CURVE('',#8869,#8870,#5221,.T.);
#11387=EDGE_CURVE('',#8871,#8869,#5222,.T.);
#11388=EDGE_CURVE('',#8872,#8870,#5223,.T.);
#11389=EDGE_CURVE('',#8871,#8872,#5224,.T.);
#11390=EDGE_CURVE('',#8859,#8871,#5225,.T.);
#11391=EDGE_CURVE('',#8860,#8872,#5226,.T.);
#11392=EDGE_CURVE('',#8873,#8874,#5227,.T.);
#11393=EDGE_CURVE('',#8873,#8875,#5228,.T.);
#11394=EDGE_CURVE('',#8875,#8876,#5229,.T.);
#11395=EDGE_CURVE('',#8874,#8876,#5230,.T.);
#11396=EDGE_CURVE('',#8874,#8877,#3838,.T.);
#11397=EDGE_CURVE('',#8876,#8878,#3839,.T.);
#11398=EDGE_CURVE('',#8877,#8878,#5231,.T.);
#11399=EDGE_CURVE('',#8877,#8879,#5232,.T.);
#11400=EDGE_CURVE('',#8878,#8880,#5233,.T.);
#11401=EDGE_CURVE('',#8879,#8880,#5234,.T.);
#11402=EDGE_CURVE('',#8879,#8881,#3840,.T.);
#11403=EDGE_CURVE('',#8880,#8882,#3841,.T.);
#11404=EDGE_CURVE('',#8881,#8882,#5235,.T.);
#11405=EDGE_CURVE('',#8883,#8884,#5236,.T.);
#11406=EDGE_CURVE('',#8883,#8885,#5237,.T.);
#11407=EDGE_CURVE('',#8885,#8886,#5238,.T.);
#11408=EDGE_CURVE('',#8884,#8886,#5239,.T.);
#11409=EDGE_CURVE('',#8884,#8887,#5240,.T.);
#11410=EDGE_CURVE('',#8886,#8888,#5241,.T.);
#11411=EDGE_CURVE('',#8887,#8888,#5242,.T.);
#11412=EDGE_CURVE('',#8887,#8889,#5243,.T.);
#11413=EDGE_CURVE('',#8888,#8890,#5244,.T.);
#11414=EDGE_CURVE('',#8889,#8890,#5245,.T.);
#11415=EDGE_CURVE('',#8889,#8891,#5246,.T.);
#11416=EDGE_CURVE('',#8890,#8892,#5247,.T.);
#11417=EDGE_CURVE('',#8891,#8892,#5248,.T.);
#11418=EDGE_CURVE('',#8891,#8893,#5249,.T.);
#11419=EDGE_CURVE('',#8892,#8894,#5250,.T.);
#11420=EDGE_CURVE('',#8893,#8894,#5251,.T.);
#11421=EDGE_CURVE('',#8893,#8895,#5252,.T.);
#11422=EDGE_CURVE('',#8894,#8896,#5253,.T.);
#11423=EDGE_CURVE('',#8895,#8896,#5254,.T.);
#11424=EDGE_CURVE('',#8792,#8895,#5255,.T.);
#11425=EDGE_CURVE('',#8896,#8793,#5256,.T.);
#11426=EDGE_CURVE('',#8783,#8897,#5257,.T.);
#11427=EDGE_CURVE('',#8898,#8786,#5258,.T.);
#11428=EDGE_CURVE('',#8897,#8898,#5259,.T.);
#11429=EDGE_CURVE('',#8897,#8899,#5260,.T.);
#11430=EDGE_CURVE('',#8898,#8900,#5261,.T.);
#11431=EDGE_CURVE('',#8899,#8900,#5262,.T.);
#11432=EDGE_CURVE('',#8899,#8901,#5263,.T.);
#11433=EDGE_CURVE('',#8900,#8902,#5264,.T.);
#11434=EDGE_CURVE('',#8901,#8902,#5265,.T.);
#11435=EDGE_CURVE('',#8901,#8903,#5266,.T.);
#11436=EDGE_CURVE('',#8902,#8904,#5267,.T.);
#11437=EDGE_CURVE('',#8903,#8904,#5268,.T.);
#11438=EDGE_CURVE('',#8905,#8873,#3842,.T.);
#11439=EDGE_CURVE('',#8905,#8906,#5269,.T.);
#11440=EDGE_CURVE('',#8906,#8875,#3843,.T.);
#11441=EDGE_CURVE('',#8907,#8905,#5270,.T.);
#11442=EDGE_CURVE('',#8907,#8908,#5271,.T.);
#11443=EDGE_CURVE('',#8908,#8906,#5272,.T.);
#11444=EDGE_CURVE('',#8909,#8907,#3844,.T.);
#11445=EDGE_CURVE('',#8909,#8910,#5273,.T.);
#11446=EDGE_CURVE('',#8910,#8908,#3845,.T.);
#11447=EDGE_CURVE('',#8881,#8909,#5274,.T.);
#11448=EDGE_CURVE('',#8882,#8910,#5275,.T.);
#11449=EDGE_CURVE('',#8911,#8883,#5276,.T.);
#11450=EDGE_CURVE('',#8911,#8912,#5277,.T.);
#11451=EDGE_CURVE('',#8912,#8885,#5278,.T.);
#11452=EDGE_CURVE('',#8913,#8911,#5279,.T.);
#11453=EDGE_CURVE('',#8913,#8914,#5280,.T.);
#11454=EDGE_CURVE('',#8914,#8912,#5281,.T.);
#11455=EDGE_CURVE('',#8915,#8913,#5282,.T.);
#11456=EDGE_CURVE('',#8915,#8916,#5283,.T.);
#11457=EDGE_CURVE('',#8916,#8914,#5284,.T.);
#11458=EDGE_CURVE('',#8917,#8915,#5285,.T.);
#11459=EDGE_CURVE('',#8917,#8918,#5286,.T.);
#11460=EDGE_CURVE('',#8918,#8916,#5287,.T.);
#11461=EDGE_CURVE('',#8919,#8917,#5288,.T.);
#11462=EDGE_CURVE('',#8919,#8920,#5289,.T.);
#11463=EDGE_CURVE('',#8920,#8918,#5290,.T.);
#11464=EDGE_CURVE('',#8921,#8919,#5291,.T.);
#11465=EDGE_CURVE('',#8921,#8922,#5292,.T.);
#11466=EDGE_CURVE('',#8922,#8920,#5293,.T.);
#11467=EDGE_CURVE('',#8923,#8921,#5294,.T.);
#11468=EDGE_CURVE('',#8923,#8924,#5295,.T.);
#11469=EDGE_CURVE('',#8924,#8922,#5296,.T.);
#11470=EDGE_CURVE('',#8925,#8923,#5297,.T.);
#11471=EDGE_CURVE('',#8925,#8926,#5298,.T.);
#11472=EDGE_CURVE('',#8926,#8924,#5299,.T.);
#11473=EDGE_CURVE('',#8927,#8925,#3846,.T.);
#11474=EDGE_CURVE('',#8927,#8928,#5300,.T.);
#11475=EDGE_CURVE('',#8928,#8926,#3847,.T.);
#11476=EDGE_CURVE('',#8929,#8927,#5301,.T.);
#11477=EDGE_CURVE('',#8929,#8930,#5302,.T.);
#11478=EDGE_CURVE('',#8930,#8928,#5303,.T.);
#11479=EDGE_CURVE('',#8931,#8929,#5304,.T.);
#11480=EDGE_CURVE('',#8931,#8932,#5305,.T.);
#11481=EDGE_CURVE('',#8932,#8930,#5306,.T.);
#11482=EDGE_CURVE('',#8933,#8931,#5307,.T.);
#11483=EDGE_CURVE('',#8933,#8934,#5308,.T.);
#11484=EDGE_CURVE('',#8934,#8932,#5309,.T.);
#11485=EDGE_CURVE('',#8935,#8933,#5310,.T.);
#11486=EDGE_CURVE('',#8935,#8936,#5311,.T.);
#11487=EDGE_CURVE('',#8936,#8934,#5312,.T.);
#11488=EDGE_CURVE('',#8937,#8935,#5313,.T.);
#11489=EDGE_CURVE('',#8937,#8938,#5314,.T.);
#11490=EDGE_CURVE('',#8938,#8936,#5315,.T.);
#11491=EDGE_CURVE('',#8939,#8937,#5316,.T.);
#11492=EDGE_CURVE('',#8939,#8940,#5317,.T.);
#11493=EDGE_CURVE('',#8940,#8938,#5318,.T.);
#11494=EDGE_CURVE('',#8941,#8939,#5319,.T.);
#11495=EDGE_CURVE('',#8941,#8942,#5320,.T.);
#11496=EDGE_CURVE('',#8942,#8940,#5321,.T.);
#11497=EDGE_CURVE('',#8836,#8943,#5322,.T.);
#11498=EDGE_CURVE('',#8944,#8943,#5323,.T.);
#11499=EDGE_CURVE('',#8945,#8944,#5324,.T.);
#11500=EDGE_CURVE('',#8946,#8945,#5325,.T.);
#11501=EDGE_CURVE('',#8947,#8946,#5326,.T.);
#11502=EDGE_CURVE('',#8948,#8947,#5327,.T.);
#11503=EDGE_CURVE('',#8949,#8948,#5328,.T.);
#11504=EDGE_CURVE('',#8950,#8949,#5329,.T.);
#11505=EDGE_CURVE('',#8951,#8950,#5330,.T.);
#11506=EDGE_CURVE('',#8952,#8951,#5331,.T.);
#11507=EDGE_CURVE('',#8953,#8952,#5332,.T.);
#11508=EDGE_CURVE('',#8954,#8953,#5333,.T.);
#11509=EDGE_CURVE('',#8955,#8954,#5334,.T.);
#11510=EDGE_CURVE('',#8956,#8955,#5335,.T.);
#11511=EDGE_CURVE('',#8957,#8956,#5336,.T.);
#11512=EDGE_CURVE('',#8958,#8957,#3848,.T.);
#11513=EDGE_CURVE('',#8959,#8958,#5337,.T.);
#11514=EDGE_CURVE('',#8960,#8959,#5338,.T.);
#11515=EDGE_CURVE('',#8961,#8960,#5339,.T.);
#11516=EDGE_CURVE('',#8962,#8961,#5340,.T.);
#11517=EDGE_CURVE('',#8963,#8962,#5341,.T.);
#11518=EDGE_CURVE('',#8964,#8963,#5342,.T.);
#11519=EDGE_CURVE('',#8965,#8964,#5343,.T.);
#11520=EDGE_CURVE('',#8941,#8965,#5344,.T.);
#11521=EDGE_CURVE('',#8903,#8966,#5345,.T.);
#11522=EDGE_CURVE('',#8967,#8966,#5346,.T.);
#11523=EDGE_CURVE('',#8968,#8967,#5347,.T.);
#11524=EDGE_CURVE('',#8969,#8968,#5348,.T.);
#11525=EDGE_CURVE('',#8827,#8969,#5349,.T.);
#11526=EDGE_CURVE('',#8970,#8971,#3849,.T.);
#11527=EDGE_CURVE('',#8972,#8970,#5350,.T.);
#11528=EDGE_CURVE('',#8973,#8972,#3850,.T.);
#11529=EDGE_CURVE('',#8974,#8973,#5351,.T.);
#11530=EDGE_CURVE('',#8975,#8974,#3851,.T.);
#11531=EDGE_CURVE('',#8976,#8975,#5352,.T.);
#11532=EDGE_CURVE('',#8977,#8976,#3852,.T.);
#11533=EDGE_CURVE('',#8971,#8977,#5353,.T.);
#11534=EDGE_CURVE('',#8978,#8978,#3853,.T.);
#11535=EDGE_CURVE('',#8973,#8979,#5354,.T.);
#11536=EDGE_CURVE('',#8980,#8979,#5355,.T.);
#11537=EDGE_CURVE('',#8974,#8980,#5356,.T.);
#11538=EDGE_CURVE('',#8972,#8981,#5357,.T.);
#11539=EDGE_CURVE('',#8979,#8981,#3854,.T.);
#11540=EDGE_CURVE('',#8970,#8982,#5358,.T.);
#11541=EDGE_CURVE('',#8981,#8982,#5359,.T.);
#11542=EDGE_CURVE('',#8971,#8983,#5360,.T.);
#11543=EDGE_CURVE('',#8982,#8983,#3855,.T.);
#11544=EDGE_CURVE('',#8948,#8984,#5361,.T.);
#11545=EDGE_CURVE('',#8985,#8984,#5362,.T.);
#11546=EDGE_CURVE('',#8949,#8985,#5363,.T.);
#11547=EDGE_CURVE('',#8947,#8986,#5364,.T.);
#11548=EDGE_CURVE('',#8984,#8986,#5365,.T.);
#11549=EDGE_CURVE('',#8946,#8987,#5366,.T.);
#11550=EDGE_CURVE('',#8986,#8987,#5367,.T.);
#11551=EDGE_CURVE('',#8945,#8988,#5368,.T.);
#11552=EDGE_CURVE('',#8987,#8988,#5369,.T.);
#11553=EDGE_CURVE('',#8944,#8989,#5370,.T.);
#11554=EDGE_CURVE('',#8988,#8989,#5371,.T.);
#11555=EDGE_CURVE('',#8943,#8990,#5372,.T.);
#11556=EDGE_CURVE('',#8989,#8990,#5373,.T.);
#11557=EDGE_CURVE('',#8990,#8838,#5374,.T.);
#11558=EDGE_CURVE('',#8969,#8991,#5375,.T.);
#11559=EDGE_CURVE('',#8991,#8829,#5376,.T.);
#11560=EDGE_CURVE('',#8968,#8992,#5377,.T.);
#11561=EDGE_CURVE('',#8991,#8992,#5378,.T.);
#11562=EDGE_CURVE('',#8967,#8993,#5379,.T.);
#11563=EDGE_CURVE('',#8992,#8993,#5380,.T.);
#11564=EDGE_CURVE('',#8966,#8994,#5381,.T.);
#11565=EDGE_CURVE('',#8993,#8994,#5382,.T.);
#11566=EDGE_CURVE('',#8994,#8904,#5383,.T.);
#11567=EDGE_CURVE('',#8995,#8995,#3856,.T.);
#11568=EDGE_CURVE('',#8995,#8978,#5384,.T.);
#11569=EDGE_CURVE('',#8965,#8996,#5385,.T.);
#11570=EDGE_CURVE('',#8996,#8942,#5386,.T.);
#11571=EDGE_CURVE('',#8997,#8980,#3857,.T.);
#11572=EDGE_CURVE('',#8975,#8997,#5387,.T.);
#11573=EDGE_CURVE('',#8998,#8997,#5388,.T.);
#11574=EDGE_CURVE('',#8976,#8998,#5389,.T.);
#11575=EDGE_CURVE('',#8999,#8998,#3858,.T.);
#11576=EDGE_CURVE('',#8977,#8999,#5390,.T.);
#11577=EDGE_CURVE('',#8983,#8999,#5391,.T.);
#11578=EDGE_CURVE('',#9000,#8985,#5392,.T.);
#11579=EDGE_CURVE('',#8950,#9000,#5393,.T.);
#11580=EDGE_CURVE('',#9001,#9000,#5394,.T.);
#11581=EDGE_CURVE('',#8951,#9001,#5395,.T.);
#11582=EDGE_CURVE('',#9002,#9001,#5396,.T.);
#11583=EDGE_CURVE('',#8952,#9002,#5397,.T.);
#11584=EDGE_CURVE('',#9003,#9002,#5398,.T.);
#11585=EDGE_CURVE('',#8953,#9003,#5399,.T.);
#11586=EDGE_CURVE('',#9004,#9003,#5400,.T.);
#11587=EDGE_CURVE('',#8954,#9004,#5401,.T.);
#11588=EDGE_CURVE('',#9005,#9004,#5402,.T.);
#11589=EDGE_CURVE('',#8955,#9005,#5403,.T.);
#11590=EDGE_CURVE('',#9006,#9005,#5404,.T.);
#11591=EDGE_CURVE('',#8956,#9006,#5405,.T.);
#11592=EDGE_CURVE('',#9007,#9006,#5406,.T.);
#11593=EDGE_CURVE('',#8957,#9007,#5407,.T.);
#11594=EDGE_CURVE('',#9008,#9007,#3859,.T.);
#11595=EDGE_CURVE('',#8958,#9008,#5408,.T.);
#11596=EDGE_CURVE('',#9009,#9008,#5409,.T.);
#11597=EDGE_CURVE('',#8959,#9009,#5410,.T.);
#11598=EDGE_CURVE('',#9010,#9009,#5411,.T.);
#11599=EDGE_CURVE('',#8960,#9010,#5412,.T.);
#11600=EDGE_CURVE('',#9011,#9010,#5413,.T.);
#11601=EDGE_CURVE('',#8961,#9011,#5414,.T.);
#11602=EDGE_CURVE('',#9012,#9011,#5415,.T.);
#11603=EDGE_CURVE('',#8962,#9012,#5416,.T.);
#11604=EDGE_CURVE('',#9013,#9012,#5417,.T.);
#11605=EDGE_CURVE('',#8963,#9013,#5418,.T.);
#11606=EDGE_CURVE('',#9014,#9013,#5419,.T.);
#11607=EDGE_CURVE('',#8964,#9014,#5420,.T.);
#11608=EDGE_CURVE('',#8996,#9014,#5421,.T.);
#14789=ORIENTED_EDGE('',*,*,#10778,.T.);
#14790=ORIENTED_EDGE('',*,*,#10779,.T.);
#14791=ORIENTED_EDGE('',*,*,#10780,.F.);
#14792=ORIENTED_EDGE('',*,*,#10781,.F.);
#14793=ORIENTED_EDGE('',*,*,#10782,.T.);
#14794=ORIENTED_EDGE('',*,*,#10783,.T.);
#14795=ORIENTED_EDGE('',*,*,#10784,.F.);
#14796=ORIENTED_EDGE('',*,*,#10779,.F.);
#14797=ORIENTED_EDGE('',*,*,#10785,.T.);
#14798=ORIENTED_EDGE('',*,*,#10786,.T.);
#14799=ORIENTED_EDGE('',*,*,#10787,.F.);
#14800=ORIENTED_EDGE('',*,*,#10783,.F.);
#14801=ORIENTED_EDGE('',*,*,#10788,.T.);
#14802=ORIENTED_EDGE('',*,*,#10789,.T.);
#14803=ORIENTED_EDGE('',*,*,#10790,.F.);
#14804=ORIENTED_EDGE('',*,*,#10791,.F.);
#14805=ORIENTED_EDGE('',*,*,#10792,.T.);
#14806=ORIENTED_EDGE('',*,*,#10791,.T.);
#14807=ORIENTED_EDGE('',*,*,#10793,.F.);
#14808=ORIENTED_EDGE('',*,*,#10794,.F.);
#14809=ORIENTED_EDGE('',*,*,#10795,.T.);
#14810=ORIENTED_EDGE('',*,*,#10794,.T.);
#14811=ORIENTED_EDGE('',*,*,#10796,.F.);
#14812=ORIENTED_EDGE('',*,*,#10797,.F.);
#14813=ORIENTED_EDGE('',*,*,#10798,.T.);
#14814=ORIENTED_EDGE('',*,*,#10797,.T.);
#14815=ORIENTED_EDGE('',*,*,#10799,.F.);
#14816=ORIENTED_EDGE('',*,*,#10800,.F.);
#14817=ORIENTED_EDGE('',*,*,#10801,.T.);
#14818=ORIENTED_EDGE('',*,*,#10800,.T.);
#14819=ORIENTED_EDGE('',*,*,#10802,.F.);
#14820=ORIENTED_EDGE('',*,*,#10803,.F.);
#14821=ORIENTED_EDGE('',*,*,#10804,.T.);
#14822=ORIENTED_EDGE('',*,*,#10803,.T.);
#14823=ORIENTED_EDGE('',*,*,#10805,.F.);
#14824=ORIENTED_EDGE('',*,*,#10806,.F.);
#14825=ORIENTED_EDGE('',*,*,#10807,.F.);
#14826=ORIENTED_EDGE('',*,*,#10808,.T.);
#14827=ORIENTED_EDGE('',*,*,#10809,.T.);
#14828=ORIENTED_EDGE('',*,*,#10810,.F.);
#14829=ORIENTED_EDGE('',*,*,#10811,.F.);
#14830=ORIENTED_EDGE('',*,*,#10810,.T.);
#14831=ORIENTED_EDGE('',*,*,#10812,.T.);
#14832=ORIENTED_EDGE('',*,*,#10813,.F.);
#14833=ORIENTED_EDGE('',*,*,#10814,.F.);
#14834=ORIENTED_EDGE('',*,*,#10813,.T.);
#14835=ORIENTED_EDGE('',*,*,#10815,.T.);
#14836=ORIENTED_EDGE('',*,*,#10816,.F.);
#14837=ORIENTED_EDGE('',*,*,#10817,.F.);
#14838=ORIENTED_EDGE('',*,*,#10806,.T.);
#14839=ORIENTED_EDGE('',*,*,#10818,.F.);
#14840=ORIENTED_EDGE('',*,*,#10819,.F.);
#14841=ORIENTED_EDGE('',*,*,#10820,.F.);
#14842=ORIENTED_EDGE('',*,*,#10821,.T.);
#14843=ORIENTED_EDGE('',*,*,#10822,.T.);
#14844=ORIENTED_EDGE('',*,*,#10823,.F.);
#14845=ORIENTED_EDGE('',*,*,#10824,.F.);
#14846=ORIENTED_EDGE('',*,*,#10825,.T.);
#14847=ORIENTED_EDGE('',*,*,#10826,.T.);
#14848=ORIENTED_EDGE('',*,*,#10821,.F.);
#14849=ORIENTED_EDGE('',*,*,#10827,.F.);
#14850=ORIENTED_EDGE('',*,*,#10828,.T.);
#14851=ORIENTED_EDGE('',*,*,#10829,.T.);
#14852=ORIENTED_EDGE('',*,*,#10825,.F.);
#14853=ORIENTED_EDGE('',*,*,#10830,.F.);
#14854=ORIENTED_EDGE('',*,*,#10831,.T.);
#14855=ORIENTED_EDGE('',*,*,#10832,.T.);
#14856=ORIENTED_EDGE('',*,*,#10828,.F.);
#14857=ORIENTED_EDGE('',*,*,#10833,.F.);
#14858=ORIENTED_EDGE('',*,*,#10834,.T.);
#14859=ORIENTED_EDGE('',*,*,#10835,.T.);
#14860=ORIENTED_EDGE('',*,*,#10831,.F.);
#14861=ORIENTED_EDGE('',*,*,#10836,.F.);
#14862=ORIENTED_EDGE('',*,*,#10819,.T.);
#14863=ORIENTED_EDGE('',*,*,#10837,.T.);
#14864=ORIENTED_EDGE('',*,*,#10834,.F.);
#14865=ORIENTED_EDGE('',*,*,#10838,.F.);
#14866=ORIENTED_EDGE('',*,*,#10839,.T.);
#14867=ORIENTED_EDGE('',*,*,#10840,.T.);
#14868=ORIENTED_EDGE('',*,*,#10841,.F.);
#14869=ORIENTED_EDGE('',*,*,#10842,.F.);
#14870=ORIENTED_EDGE('',*,*,#10841,.T.);
#14871=ORIENTED_EDGE('',*,*,#10843,.T.);
#14872=ORIENTED_EDGE('',*,*,#10844,.F.);
#14873=ORIENTED_EDGE('',*,*,#10845,.F.);
#14874=ORIENTED_EDGE('',*,*,#10844,.T.);
#14875=ORIENTED_EDGE('',*,*,#10846,.T.);
#14876=ORIENTED_EDGE('',*,*,#10847,.F.);
#14877=ORIENTED_EDGE('',*,*,#10848,.T.);
#14878=ORIENTED_EDGE('',*,*,#10847,.T.);
#14879=ORIENTED_EDGE('',*,*,#10849,.T.);
#14880=ORIENTED_EDGE('',*,*,#10786,.F.);
#14881=ORIENTED_EDGE('',*,*,#10850,.F.);
#14882=ORIENTED_EDGE('',*,*,#10851,.T.);
#14883=ORIENTED_EDGE('',*,*,#10852,.T.);
#14884=ORIENTED_EDGE('',*,*,#10853,.F.);
#14885=ORIENTED_EDGE('',*,*,#10854,.F.);
#14886=ORIENTED_EDGE('',*,*,#10855,.T.);
#14887=ORIENTED_EDGE('',*,*,#10856,.T.);
#14888=ORIENTED_EDGE('',*,*,#10851,.F.);
#14889=ORIENTED_EDGE('',*,*,#10857,.F.);
#14890=ORIENTED_EDGE('',*,*,#10858,.T.);
#14891=ORIENTED_EDGE('',*,*,#10859,.T.);
#14892=ORIENTED_EDGE('',*,*,#10855,.F.);
#14893=ORIENTED_EDGE('',*,*,#10860,.F.);
#14894=ORIENTED_EDGE('',*,*,#10861,.T.);
#14895=ORIENTED_EDGE('',*,*,#10862,.T.);
#14896=ORIENTED_EDGE('',*,*,#10858,.F.);
#14897=ORIENTED_EDGE('',*,*,#10863,.F.);
#14898=ORIENTED_EDGE('',*,*,#10864,.T.);
#14899=ORIENTED_EDGE('',*,*,#10865,.T.);
#14900=ORIENTED_EDGE('',*,*,#10861,.F.);
#14901=ORIENTED_EDGE('',*,*,#10866,.F.);
#14902=ORIENTED_EDGE('',*,*,#10867,.T.);
#14903=ORIENTED_EDGE('',*,*,#10868,.T.);
#14904=ORIENTED_EDGE('',*,*,#10864,.F.);
#14905=ORIENTED_EDGE('',*,*,#10869,.T.);
#14906=ORIENTED_EDGE('',*,*,#10870,.T.);
#14907=ORIENTED_EDGE('',*,*,#10871,.F.);
#14908=ORIENTED_EDGE('',*,*,#10872,.F.);
#14909=ORIENTED_EDGE('',*,*,#10873,.T.);
#14910=ORIENTED_EDGE('',*,*,#10874,.T.);
#14911=ORIENTED_EDGE('',*,*,#10875,.F.);
#14912=ORIENTED_EDGE('',*,*,#10870,.F.);
#14913=ORIENTED_EDGE('',*,*,#10876,.T.);
#14914=ORIENTED_EDGE('',*,*,#10877,.T.);
#14915=ORIENTED_EDGE('',*,*,#10878,.F.);
#14916=ORIENTED_EDGE('',*,*,#10874,.F.);
#14917=ORIENTED_EDGE('',*,*,#10879,.F.);
#14918=ORIENTED_EDGE('',*,*,#10816,.T.);
#14919=ORIENTED_EDGE('',*,*,#10880,.F.);
#14920=ORIENTED_EDGE('',*,*,#10877,.F.);
#14921=ORIENTED_EDGE('',*,*,#10881,.T.);
#14922=ORIENTED_EDGE('',*,*,#10882,.T.);
#14923=ORIENTED_EDGE('',*,*,#10883,.F.);
#14924=ORIENTED_EDGE('',*,*,#10882,.F.);
#14925=ORIENTED_EDGE('',*,*,#10884,.T.);
#14926=ORIENTED_EDGE('',*,*,#10885,.T.);
#14927=ORIENTED_EDGE('',*,*,#10886,.T.);
#14928=ORIENTED_EDGE('',*,*,#10867,.F.);
#14929=ORIENTED_EDGE('',*,*,#10887,.T.);
#14930=ORIENTED_EDGE('',*,*,#10888,.T.);
#14931=ORIENTED_EDGE('',*,*,#10889,.F.);
#14932=ORIENTED_EDGE('',*,*,#10890,.F.);
#14933=ORIENTED_EDGE('',*,*,#10891,.T.);
#14934=ORIENTED_EDGE('',*,*,#10890,.T.);
#14935=ORIENTED_EDGE('',*,*,#10892,.F.);
#14936=ORIENTED_EDGE('',*,*,#10893,.F.);
#14937=ORIENTED_EDGE('',*,*,#10894,.T.);
#14938=ORIENTED_EDGE('',*,*,#10893,.T.);
#14939=ORIENTED_EDGE('',*,*,#10895,.F.);
#14940=ORIENTED_EDGE('',*,*,#10896,.F.);
#14941=ORIENTED_EDGE('',*,*,#10897,.T.);
#14942=ORIENTED_EDGE('',*,*,#10896,.T.);
#14943=ORIENTED_EDGE('',*,*,#10898,.F.);
#14944=ORIENTED_EDGE('',*,*,#10899,.F.);
#14945=ORIENTED_EDGE('',*,*,#10900,.T.);
#14946=ORIENTED_EDGE('',*,*,#10899,.T.);
#14947=ORIENTED_EDGE('',*,*,#10901,.F.);
#14948=ORIENTED_EDGE('',*,*,#10902,.F.);
#14949=ORIENTED_EDGE('',*,*,#10903,.T.);
#14950=ORIENTED_EDGE('',*,*,#10902,.T.);
#14951=ORIENTED_EDGE('',*,*,#10904,.F.);
#14952=ORIENTED_EDGE('',*,*,#10885,.F.);
#14953=ORIENTED_EDGE('',*,*,#10905,.F.);
#14954=ORIENTED_EDGE('',*,*,#10906,.T.);
#14955=ORIENTED_EDGE('',*,*,#10907,.T.);
#14956=ORIENTED_EDGE('',*,*,#10908,.F.);
#14957=ORIENTED_EDGE('',*,*,#10909,.F.);
#14958=ORIENTED_EDGE('',*,*,#10908,.T.);
#14959=ORIENTED_EDGE('',*,*,#10910,.T.);
#14960=ORIENTED_EDGE('',*,*,#10911,.F.);
#14961=ORIENTED_EDGE('',*,*,#10912,.F.);
#14962=ORIENTED_EDGE('',*,*,#10911,.T.);
#14963=ORIENTED_EDGE('',*,*,#10913,.T.);
#14964=ORIENTED_EDGE('',*,*,#10914,.F.);
#14965=ORIENTED_EDGE('',*,*,#10915,.F.);
#14966=ORIENTED_EDGE('',*,*,#10914,.T.);
#14967=ORIENTED_EDGE('',*,*,#10916,.T.);
#14968=ORIENTED_EDGE('',*,*,#10917,.F.);
#14969=ORIENTED_EDGE('',*,*,#10918,.F.);
#14970=ORIENTED_EDGE('',*,*,#10919,.T.);
#14971=ORIENTED_EDGE('',*,*,#10920,.T.);
#14972=ORIENTED_EDGE('',*,*,#10921,.F.);
#14973=ORIENTED_EDGE('',*,*,#10922,.F.);
#14974=ORIENTED_EDGE('',*,*,#10921,.T.);
#14975=ORIENTED_EDGE('',*,*,#10923,.T.);
#14976=ORIENTED_EDGE('',*,*,#10924,.F.);
#14977=ORIENTED_EDGE('',*,*,#10925,.F.);
#14978=ORIENTED_EDGE('',*,*,#10924,.T.);
#14979=ORIENTED_EDGE('',*,*,#10926,.T.);
#14980=ORIENTED_EDGE('',*,*,#10927,.F.);
#14981=ORIENTED_EDGE('',*,*,#10928,.F.);
#14982=ORIENTED_EDGE('',*,*,#10927,.T.);
#14983=ORIENTED_EDGE('',*,*,#10929,.T.);
#14984=ORIENTED_EDGE('',*,*,#10930,.F.);
#14985=ORIENTED_EDGE('',*,*,#10931,.F.);
#14986=ORIENTED_EDGE('',*,*,#10930,.T.);
#14987=ORIENTED_EDGE('',*,*,#10932,.T.);
#14988=ORIENTED_EDGE('',*,*,#10933,.F.);
#14989=ORIENTED_EDGE('',*,*,#10934,.F.);
#14990=ORIENTED_EDGE('',*,*,#10933,.T.);
#14991=ORIENTED_EDGE('',*,*,#10935,.T.);
#14992=ORIENTED_EDGE('',*,*,#10936,.F.);
#14993=ORIENTED_EDGE('',*,*,#10937,.T.);
#14994=ORIENTED_EDGE('',*,*,#10936,.T.);
#14995=ORIENTED_EDGE('',*,*,#10938,.T.);
#14996=ORIENTED_EDGE('',*,*,#10888,.F.);
#14997=ORIENTED_EDGE('',*,*,#10939,.F.);
#14998=ORIENTED_EDGE('',*,*,#10872,.T.);
#14999=ORIENTED_EDGE('',*,*,#10940,.F.);
#15000=ORIENTED_EDGE('',*,*,#10941,.F.);
#15001=ORIENTED_EDGE('',*,*,#10942,.F.);
#15002=ORIENTED_EDGE('',*,*,#10941,.T.);
#15003=ORIENTED_EDGE('',*,*,#10943,.T.);
#15004=ORIENTED_EDGE('',*,*,#10944,.F.);
#15005=ORIENTED_EDGE('',*,*,#10945,.F.);
#15006=ORIENTED_EDGE('',*,*,#10944,.T.);
#15007=ORIENTED_EDGE('',*,*,#10946,.T.);
#15008=ORIENTED_EDGE('',*,*,#10947,.F.);
#15009=ORIENTED_EDGE('',*,*,#10948,.F.);
#15010=ORIENTED_EDGE('',*,*,#10947,.T.);
#15011=ORIENTED_EDGE('',*,*,#10949,.T.);
#15012=ORIENTED_EDGE('',*,*,#10950,.F.);
#15013=ORIENTED_EDGE('',*,*,#10951,.F.);
#15014=ORIENTED_EDGE('',*,*,#10952,.T.);
#15015=ORIENTED_EDGE('',*,*,#10953,.T.);
#15016=ORIENTED_EDGE('',*,*,#10906,.F.);
#15017=ORIENTED_EDGE('',*,*,#10954,.F.);
#15018=ORIENTED_EDGE('',*,*,#10955,.T.);
#15019=ORIENTED_EDGE('',*,*,#10956,.T.);
#15020=ORIENTED_EDGE('',*,*,#10952,.F.);
#15021=ORIENTED_EDGE('',*,*,#10957,.F.);
#15022=ORIENTED_EDGE('',*,*,#10958,.T.);
#15023=ORIENTED_EDGE('',*,*,#10959,.T.);
#15024=ORIENTED_EDGE('',*,*,#10955,.F.);
#15025=ORIENTED_EDGE('',*,*,#10960,.F.);
#15026=ORIENTED_EDGE('',*,*,#10917,.T.);
#15027=ORIENTED_EDGE('',*,*,#10961,.T.);
#15028=ORIENTED_EDGE('',*,*,#10958,.F.);
#15029=ORIENTED_EDGE('',*,*,#10962,.F.);
#15030=ORIENTED_EDGE('',*,*,#10963,.T.);
#15031=ORIENTED_EDGE('',*,*,#10964,.T.);
#15032=ORIENTED_EDGE('',*,*,#10919,.F.);
#15033=ORIENTED_EDGE('',*,*,#10965,.F.);
#15034=ORIENTED_EDGE('',*,*,#10966,.T.);
#15035=ORIENTED_EDGE('',*,*,#10967,.T.);
#15036=ORIENTED_EDGE('',*,*,#10963,.F.);
#15037=ORIENTED_EDGE('',*,*,#10968,.F.);
#15038=ORIENTED_EDGE('',*,*,#10969,.T.);
#15039=ORIENTED_EDGE('',*,*,#10970,.T.);
#15040=ORIENTED_EDGE('',*,*,#10966,.F.);
#15041=ORIENTED_EDGE('',*,*,#10971,.F.);
#15042=ORIENTED_EDGE('',*,*,#10972,.T.);
#15043=ORIENTED_EDGE('',*,*,#10973,.T.);
#15044=ORIENTED_EDGE('',*,*,#10969,.F.);
#15045=ORIENTED_EDGE('',*,*,#10974,.F.);
#15046=ORIENTED_EDGE('',*,*,#10975,.T.);
#15047=ORIENTED_EDGE('',*,*,#10976,.T.);
#15048=ORIENTED_EDGE('',*,*,#10972,.F.);
#15049=ORIENTED_EDGE('',*,*,#10977,.F.);
#15050=ORIENTED_EDGE('',*,*,#10978,.T.);
#15051=ORIENTED_EDGE('',*,*,#10979,.T.);
#15052=ORIENTED_EDGE('',*,*,#10975,.F.);
#15053=ORIENTED_EDGE('',*,*,#10980,.F.);
#15054=ORIENTED_EDGE('',*,*,#10981,.T.);
#15055=ORIENTED_EDGE('',*,*,#10982,.T.);
#15056=ORIENTED_EDGE('',*,*,#10978,.F.);
#15057=ORIENTED_EDGE('',*,*,#10983,.F.);
#15058=ORIENTED_EDGE('',*,*,#10984,.T.);
#15059=ORIENTED_EDGE('',*,*,#10985,.T.);
#15060=ORIENTED_EDGE('',*,*,#10981,.F.);
#15061=ORIENTED_EDGE('',*,*,#10986,.F.);
#15062=ORIENTED_EDGE('',*,*,#10987,.T.);
#15063=ORIENTED_EDGE('',*,*,#10988,.T.);
#15064=ORIENTED_EDGE('',*,*,#10984,.F.);
#15065=ORIENTED_EDGE('',*,*,#10989,.F.);
#15066=ORIENTED_EDGE('',*,*,#10990,.T.);
#15067=ORIENTED_EDGE('',*,*,#10991,.T.);
#15068=ORIENTED_EDGE('',*,*,#10987,.F.);
#15069=ORIENTED_EDGE('',*,*,#10992,.F.);
#15070=ORIENTED_EDGE('',*,*,#10993,.T.);
#15071=ORIENTED_EDGE('',*,*,#10994,.T.);
#15072=ORIENTED_EDGE('',*,*,#10990,.F.);
#15073=ORIENTED_EDGE('',*,*,#10995,.F.);
#15074=ORIENTED_EDGE('',*,*,#10996,.T.);
#15075=ORIENTED_EDGE('',*,*,#10997,.T.);
#15076=ORIENTED_EDGE('',*,*,#10993,.F.);
#15077=ORIENTED_EDGE('',*,*,#10998,.F.);
#15078=ORIENTED_EDGE('',*,*,#10999,.T.);
#15079=ORIENTED_EDGE('',*,*,#11000,.T.);
#15080=ORIENTED_EDGE('',*,*,#10996,.F.);
#15081=ORIENTED_EDGE('',*,*,#11001,.F.);
#15082=ORIENTED_EDGE('',*,*,#11002,.T.);
#15083=ORIENTED_EDGE('',*,*,#11003,.T.);
#15084=ORIENTED_EDGE('',*,*,#10999,.F.);
#15085=ORIENTED_EDGE('',*,*,#11004,.F.);
#15086=ORIENTED_EDGE('',*,*,#11005,.T.);
#15087=ORIENTED_EDGE('',*,*,#11006,.T.);
#15088=ORIENTED_EDGE('',*,*,#11002,.F.);
#15089=ORIENTED_EDGE('',*,*,#11007,.F.);
#15090=ORIENTED_EDGE('',*,*,#11008,.T.);
#15091=ORIENTED_EDGE('',*,*,#11009,.T.);
#15092=ORIENTED_EDGE('',*,*,#11005,.F.);
#15093=ORIENTED_EDGE('',*,*,#11010,.T.);
#15094=ORIENTED_EDGE('',*,*,#11011,.T.);
#15095=ORIENTED_EDGE('',*,*,#11012,.F.);
#15096=ORIENTED_EDGE('',*,*,#11013,.F.);
#15097=ORIENTED_EDGE('',*,*,#11014,.T.);
#15098=ORIENTED_EDGE('',*,*,#11015,.T.);
#15099=ORIENTED_EDGE('',*,*,#11016,.F.);
#15100=ORIENTED_EDGE('',*,*,#11011,.F.);
#15101=ORIENTED_EDGE('',*,*,#11017,.T.);
#15102=ORIENTED_EDGE('',*,*,#11018,.T.);
#15103=ORIENTED_EDGE('',*,*,#11019,.F.);
#15104=ORIENTED_EDGE('',*,*,#11015,.F.);
#15105=ORIENTED_EDGE('',*,*,#11020,.T.);
#15106=ORIENTED_EDGE('',*,*,#11021,.T.);
#15107=ORIENTED_EDGE('',*,*,#11022,.F.);
#15108=ORIENTED_EDGE('',*,*,#11018,.F.);
#15109=ORIENTED_EDGE('',*,*,#11023,.T.);
#15110=ORIENTED_EDGE('',*,*,#11024,.T.);
#15111=ORIENTED_EDGE('',*,*,#11025,.F.);
#15112=ORIENTED_EDGE('',*,*,#11026,.F.);
#15113=ORIENTED_EDGE('',*,*,#11027,.T.);
#15114=ORIENTED_EDGE('',*,*,#11028,.T.);
#15115=ORIENTED_EDGE('',*,*,#11029,.F.);
#15116=ORIENTED_EDGE('',*,*,#11024,.F.);
#15117=ORIENTED_EDGE('',*,*,#11030,.T.);
#15118=ORIENTED_EDGE('',*,*,#11031,.T.);
#15119=ORIENTED_EDGE('',*,*,#11032,.F.);
#15120=ORIENTED_EDGE('',*,*,#11028,.F.);
#15121=ORIENTED_EDGE('',*,*,#11033,.T.);
#15122=ORIENTED_EDGE('',*,*,#11034,.T.);
#15123=ORIENTED_EDGE('',*,*,#11035,.F.);
#15124=ORIENTED_EDGE('',*,*,#11031,.F.);
#15125=ORIENTED_EDGE('',*,*,#11036,.T.);
#15126=ORIENTED_EDGE('',*,*,#11037,.T.);
#15127=ORIENTED_EDGE('',*,*,#11038,.F.);
#15128=ORIENTED_EDGE('',*,*,#11034,.F.);
#15129=ORIENTED_EDGE('',*,*,#11039,.T.);
#15130=ORIENTED_EDGE('',*,*,#11040,.T.);
#15131=ORIENTED_EDGE('',*,*,#11041,.F.);
#15132=ORIENTED_EDGE('',*,*,#11037,.F.);
#15133=ORIENTED_EDGE('',*,*,#11042,.F.);
#15134=ORIENTED_EDGE('',*,*,#10823,.T.);
#15135=ORIENTED_EDGE('',*,*,#11043,.F.);
#15136=ORIENTED_EDGE('',*,*,#11040,.F.);
#15137=ORIENTED_EDGE('',*,*,#11044,.T.);
#15138=ORIENTED_EDGE('',*,*,#11045,.T.);
#15139=ORIENTED_EDGE('',*,*,#11046,.T.);
#15140=ORIENTED_EDGE('',*,*,#10808,.F.);
#15141=ORIENTED_EDGE('',*,*,#11047,.T.);
#15142=ORIENTED_EDGE('',*,*,#11048,.T.);
#15143=ORIENTED_EDGE('',*,*,#11049,.F.);
#15144=ORIENTED_EDGE('',*,*,#11045,.F.);
#15145=ORIENTED_EDGE('',*,*,#11050,.T.);
#15146=ORIENTED_EDGE('',*,*,#11051,.T.);
#15147=ORIENTED_EDGE('',*,*,#11052,.F.);
#15148=ORIENTED_EDGE('',*,*,#11048,.F.);
#15149=ORIENTED_EDGE('',*,*,#11053,.T.);
#15150=ORIENTED_EDGE('',*,*,#11054,.T.);
#15151=ORIENTED_EDGE('',*,*,#11055,.F.);
#15152=ORIENTED_EDGE('',*,*,#11051,.F.);
#15153=ORIENTED_EDGE('',*,*,#11056,.F.);
#15154=ORIENTED_EDGE('',*,*,#10950,.T.);
#15155=ORIENTED_EDGE('',*,*,#11057,.F.);
#15156=ORIENTED_EDGE('',*,*,#11054,.F.);
#15157=ORIENTED_EDGE('',*,*,#11058,.F.);
#15158=ORIENTED_EDGE('',*,*,#11059,.T.);
#15159=ORIENTED_EDGE('',*,*,#11060,.F.);
#15160=ORIENTED_EDGE('',*,*,#11059,.F.);
#15161=ORIENTED_EDGE('',*,*,#11061,.T.);
#15162=ORIENTED_EDGE('',*,*,#11062,.T.);
#15163=ORIENTED_EDGE('',*,*,#11063,.T.);
#15164=ORIENTED_EDGE('',*,*,#11008,.F.);
#15165=ORIENTED_EDGE('',*,*,#11064,.T.);
#15166=ORIENTED_EDGE('',*,*,#11013,.T.);
#15167=ORIENTED_EDGE('',*,*,#11065,.F.);
#15168=ORIENTED_EDGE('',*,*,#11066,.F.);
#15169=ORIENTED_EDGE('',*,*,#11067,.T.);
#15170=ORIENTED_EDGE('',*,*,#11066,.T.);
#15171=ORIENTED_EDGE('',*,*,#11068,.F.);
#15172=ORIENTED_EDGE('',*,*,#11069,.F.);
#15173=ORIENTED_EDGE('',*,*,#11070,.T.);
#15174=ORIENTED_EDGE('',*,*,#11069,.T.);
#15175=ORIENTED_EDGE('',*,*,#11071,.F.);
#15176=ORIENTED_EDGE('',*,*,#11072,.F.);
#15177=ORIENTED_EDGE('',*,*,#11073,.T.);
#15178=ORIENTED_EDGE('',*,*,#11072,.T.);
#15179=ORIENTED_EDGE('',*,*,#11074,.F.);
#15180=ORIENTED_EDGE('',*,*,#11021,.F.);
#15181=ORIENTED_EDGE('',*,*,#11075,.T.);
#15182=ORIENTED_EDGE('',*,*,#11026,.T.);
#15183=ORIENTED_EDGE('',*,*,#11076,.F.);
#15184=ORIENTED_EDGE('',*,*,#11077,.F.);
#15185=ORIENTED_EDGE('',*,*,#11078,.T.);
#15186=ORIENTED_EDGE('',*,*,#11077,.T.);
#15187=ORIENTED_EDGE('',*,*,#11079,.F.);
#15188=ORIENTED_EDGE('',*,*,#11080,.F.);
#15189=ORIENTED_EDGE('',*,*,#11081,.T.);
#15190=ORIENTED_EDGE('',*,*,#11080,.T.);
#15191=ORIENTED_EDGE('',*,*,#11082,.F.);
#15192=ORIENTED_EDGE('',*,*,#11083,.F.);
#15193=ORIENTED_EDGE('',*,*,#11084,.T.);
#15194=ORIENTED_EDGE('',*,*,#11083,.T.);
#15195=ORIENTED_EDGE('',*,*,#11085,.F.);
#15196=ORIENTED_EDGE('',*,*,#11086,.F.);
#15197=ORIENTED_EDGE('',*,*,#11087,.T.);
#15198=ORIENTED_EDGE('',*,*,#11086,.T.);
#15199=ORIENTED_EDGE('',*,*,#11088,.F.);
#15200=ORIENTED_EDGE('',*,*,#11089,.F.);
#15201=ORIENTED_EDGE('',*,*,#11090,.T.);
#15202=ORIENTED_EDGE('',*,*,#11089,.T.);
#15203=ORIENTED_EDGE('',*,*,#11091,.F.);
#15204=ORIENTED_EDGE('',*,*,#11092,.F.);
#15205=ORIENTED_EDGE('',*,*,#11093,.T.);
#15206=ORIENTED_EDGE('',*,*,#11092,.T.);
#15207=ORIENTED_EDGE('',*,*,#11094,.F.);
#15208=ORIENTED_EDGE('',*,*,#11095,.F.);
#15209=ORIENTED_EDGE('',*,*,#11096,.T.);
#15210=ORIENTED_EDGE('',*,*,#11095,.T.);
#15211=ORIENTED_EDGE('',*,*,#11097,.F.);
#15212=ORIENTED_EDGE('',*,*,#11098,.F.);
#15213=ORIENTED_EDGE('',*,*,#11099,.T.);
#15214=ORIENTED_EDGE('',*,*,#11098,.T.);
#15215=ORIENTED_EDGE('',*,*,#11100,.F.);
#15216=ORIENTED_EDGE('',*,*,#11101,.F.);
#15217=ORIENTED_EDGE('',*,*,#11102,.T.);
#15218=ORIENTED_EDGE('',*,*,#11101,.T.);
#15219=ORIENTED_EDGE('',*,*,#11103,.F.);
#15220=ORIENTED_EDGE('',*,*,#11104,.F.);
#15221=ORIENTED_EDGE('',*,*,#11105,.T.);
#15222=ORIENTED_EDGE('',*,*,#11104,.T.);
#15223=ORIENTED_EDGE('',*,*,#11106,.F.);
#15224=ORIENTED_EDGE('',*,*,#11107,.F.);
#15225=ORIENTED_EDGE('',*,*,#11108,.T.);
#15226=ORIENTED_EDGE('',*,*,#11107,.T.);
#15227=ORIENTED_EDGE('',*,*,#11109,.F.);
#15228=ORIENTED_EDGE('',*,*,#11110,.F.);
#15229=ORIENTED_EDGE('',*,*,#11111,.T.);
#15230=ORIENTED_EDGE('',*,*,#11110,.T.);
#15231=ORIENTED_EDGE('',*,*,#11112,.F.);
#15232=ORIENTED_EDGE('',*,*,#11113,.F.);
#15233=ORIENTED_EDGE('',*,*,#11114,.T.);
#15234=ORIENTED_EDGE('',*,*,#11113,.T.);
#15235=ORIENTED_EDGE('',*,*,#11115,.F.);
#15236=ORIENTED_EDGE('',*,*,#11116,.F.);
#15237=ORIENTED_EDGE('',*,*,#11117,.T.);
#15238=ORIENTED_EDGE('',*,*,#11116,.T.);
#15239=ORIENTED_EDGE('',*,*,#11118,.F.);
#15240=ORIENTED_EDGE('',*,*,#11119,.F.);
#15241=ORIENTED_EDGE('',*,*,#11120,.T.);
#15242=ORIENTED_EDGE('',*,*,#11119,.T.);
#15243=ORIENTED_EDGE('',*,*,#11121,.F.);
#15244=ORIENTED_EDGE('',*,*,#11062,.F.);
#15245=ORIENTED_EDGE('',*,*,#11122,.T.);
#15246=ORIENTED_EDGE('',*,*,#11123,.T.);
#15247=ORIENTED_EDGE('',*,*,#11124,.F.);
#15248=ORIENTED_EDGE('',*,*,#11125,.F.);
#15249=ORIENTED_EDGE('',*,*,#11126,.T.);
#15250=ORIENTED_EDGE('',*,*,#11127,.T.);
#15251=ORIENTED_EDGE('',*,*,#11128,.F.);
#15252=ORIENTED_EDGE('',*,*,#11123,.F.);
#15253=ORIENTED_EDGE('',*,*,#11129,.T.);
#15254=ORIENTED_EDGE('',*,*,#11130,.T.);
#15255=ORIENTED_EDGE('',*,*,#11131,.F.);
#15256=ORIENTED_EDGE('',*,*,#11127,.F.);
#15257=ORIENTED_EDGE('',*,*,#11132,.T.);
#15258=ORIENTED_EDGE('',*,*,#11133,.T.);
#15259=ORIENTED_EDGE('',*,*,#11134,.F.);
#15260=ORIENTED_EDGE('',*,*,#11135,.F.);
#15261=ORIENTED_EDGE('',*,*,#11136,.T.);
#15262=ORIENTED_EDGE('',*,*,#11135,.T.);
#15263=ORIENTED_EDGE('',*,*,#11137,.F.);
#15264=ORIENTED_EDGE('',*,*,#11138,.F.);
#15265=ORIENTED_EDGE('',*,*,#11139,.T.);
#15266=ORIENTED_EDGE('',*,*,#11138,.T.);
#15267=ORIENTED_EDGE('',*,*,#11140,.F.);
#15268=ORIENTED_EDGE('',*,*,#11141,.F.);
#15269=ORIENTED_EDGE('',*,*,#11142,.T.);
#15270=ORIENTED_EDGE('',*,*,#11141,.T.);
#15271=ORIENTED_EDGE('',*,*,#11143,.F.);
#15272=ORIENTED_EDGE('',*,*,#11144,.F.);
#15273=ORIENTED_EDGE('',*,*,#11145,.T.);
#15274=ORIENTED_EDGE('',*,*,#11144,.T.);
#15275=ORIENTED_EDGE('',*,*,#11146,.F.);
#15276=ORIENTED_EDGE('',*,*,#11147,.F.);
#15277=ORIENTED_EDGE('',*,*,#11148,.T.);
#15278=ORIENTED_EDGE('',*,*,#11147,.T.);
#15279=ORIENTED_EDGE('',*,*,#11149,.F.);
#15280=ORIENTED_EDGE('',*,*,#11150,.F.);
#15281=ORIENTED_EDGE('',*,*,#11151,.F.);
#15282=ORIENTED_EDGE('',*,*,#10781,.T.);
#15283=ORIENTED_EDGE('',*,*,#11152,.T.);
#15284=ORIENTED_EDGE('',*,*,#11153,.F.);
#15285=ORIENTED_EDGE('',*,*,#11154,.F.);
#15286=ORIENTED_EDGE('',*,*,#11153,.T.);
#15287=ORIENTED_EDGE('',*,*,#11155,.T.);
#15288=ORIENTED_EDGE('',*,*,#11156,.F.);
#15289=ORIENTED_EDGE('',*,*,#11157,.F.);
#15290=ORIENTED_EDGE('',*,*,#11156,.T.);
#15291=ORIENTED_EDGE('',*,*,#11158,.T.);
#15292=ORIENTED_EDGE('',*,*,#11159,.F.);
#15293=ORIENTED_EDGE('',*,*,#11160,.F.);
#15294=ORIENTED_EDGE('',*,*,#11159,.T.);
#15295=ORIENTED_EDGE('',*,*,#11161,.T.);
#15296=ORIENTED_EDGE('',*,*,#11162,.F.);
#15297=ORIENTED_EDGE('',*,*,#11163,.F.);
#15298=ORIENTED_EDGE('',*,*,#11150,.T.);
#15299=ORIENTED_EDGE('',*,*,#11164,.F.);
#15300=ORIENTED_EDGE('',*,*,#11165,.F.);
#15301=ORIENTED_EDGE('',*,*,#11166,.T.);
#15302=ORIENTED_EDGE('',*,*,#11167,.T.);
#15303=ORIENTED_EDGE('',*,*,#11168,.T.);
#15304=ORIENTED_EDGE('',*,*,#10789,.F.);
#15305=ORIENTED_EDGE('',*,*,#11169,.F.);
#15306=ORIENTED_EDGE('',*,*,#11170,.T.);
#15307=ORIENTED_EDGE('',*,*,#11171,.T.);
#15308=ORIENTED_EDGE('',*,*,#11167,.F.);
#15309=ORIENTED_EDGE('',*,*,#11172,.F.);
#15310=ORIENTED_EDGE('',*,*,#11173,.T.);
#15311=ORIENTED_EDGE('',*,*,#11174,.T.);
#15312=ORIENTED_EDGE('',*,*,#11170,.F.);
#15313=ORIENTED_EDGE('',*,*,#11175,.F.);
#15314=ORIENTED_EDGE('',*,*,#11176,.T.);
#15315=ORIENTED_EDGE('',*,*,#11177,.T.);
#15316=ORIENTED_EDGE('',*,*,#11173,.F.);
#15317=ORIENTED_EDGE('',*,*,#11178,.F.);
#15318=ORIENTED_EDGE('',*,*,#11179,.T.);
#15319=ORIENTED_EDGE('',*,*,#11180,.T.);
#15320=ORIENTED_EDGE('',*,*,#11176,.F.);
#15321=ORIENTED_EDGE('',*,*,#11181,.F.);
#15322=ORIENTED_EDGE('',*,*,#11182,.T.);
#15323=ORIENTED_EDGE('',*,*,#11183,.T.);
#15324=ORIENTED_EDGE('',*,*,#11179,.F.);
#15325=ORIENTED_EDGE('',*,*,#11184,.F.);
#15326=ORIENTED_EDGE('',*,*,#11165,.T.);
#15327=ORIENTED_EDGE('',*,*,#11185,.T.);
#15328=ORIENTED_EDGE('',*,*,#11182,.F.);
#15329=ORIENTED_EDGE('',*,*,#11186,.F.);
#15330=ORIENTED_EDGE('',*,*,#11187,.T.);
#15331=ORIENTED_EDGE('',*,*,#11188,.T.);
#15332=ORIENTED_EDGE('',*,*,#11189,.F.);
#15333=ORIENTED_EDGE('',*,*,#11190,.F.);
#15334=ORIENTED_EDGE('',*,*,#11189,.T.);
#15335=ORIENTED_EDGE('',*,*,#11191,.T.);
#15336=ORIENTED_EDGE('',*,*,#11192,.F.);
#15337=ORIENTED_EDGE('',*,*,#11193,.F.);
#15338=ORIENTED_EDGE('',*,*,#11192,.T.);
#15339=ORIENTED_EDGE('',*,*,#11194,.T.);
#15340=ORIENTED_EDGE('',*,*,#11195,.F.);
#15341=ORIENTED_EDGE('',*,*,#11196,.T.);
#15342=ORIENTED_EDGE('',*,*,#11195,.T.);
#15343=ORIENTED_EDGE('',*,*,#11197,.T.);
#15344=ORIENTED_EDGE('',*,*,#11130,.F.);
#15345=ORIENTED_EDGE('',*,*,#11198,.F.);
#15346=ORIENTED_EDGE('',*,*,#11199,.T.);
#15347=ORIENTED_EDGE('',*,*,#11200,.T.);
#15348=ORIENTED_EDGE('',*,*,#11201,.F.);
#15349=ORIENTED_EDGE('',*,*,#11202,.F.);
#15350=ORIENTED_EDGE('',*,*,#11203,.T.);
#15351=ORIENTED_EDGE('',*,*,#11204,.T.);
#15352=ORIENTED_EDGE('',*,*,#11199,.F.);
#15353=ORIENTED_EDGE('',*,*,#11205,.F.);
#15354=ORIENTED_EDGE('',*,*,#11206,.T.);
#15355=ORIENTED_EDGE('',*,*,#11207,.T.);
#15356=ORIENTED_EDGE('',*,*,#11203,.F.);
#15357=ORIENTED_EDGE('',*,*,#11208,.F.);
#15358=ORIENTED_EDGE('',*,*,#11209,.T.);
#15359=ORIENTED_EDGE('',*,*,#11210,.T.);
#15360=ORIENTED_EDGE('',*,*,#11206,.F.);
#15361=ORIENTED_EDGE('',*,*,#11211,.F.);
#15362=ORIENTED_EDGE('',*,*,#11212,.T.);
#15363=ORIENTED_EDGE('',*,*,#11213,.T.);
#15364=ORIENTED_EDGE('',*,*,#11209,.F.);
#15365=ORIENTED_EDGE('',*,*,#11214,.F.);
#15366=ORIENTED_EDGE('',*,*,#11215,.T.);
#15367=ORIENTED_EDGE('',*,*,#11216,.T.);
#15368=ORIENTED_EDGE('',*,*,#11212,.F.);
#15369=ORIENTED_EDGE('',*,*,#11217,.T.);
#15370=ORIENTED_EDGE('',*,*,#11218,.T.);
#15371=ORIENTED_EDGE('',*,*,#11219,.T.);
#15372=ORIENTED_EDGE('',*,*,#10839,.F.);
#15373=ORIENTED_EDGE('',*,*,#11220,.T.);
#15374=ORIENTED_EDGE('',*,*,#11221,.T.);
#15375=ORIENTED_EDGE('',*,*,#11222,.F.);
#15376=ORIENTED_EDGE('',*,*,#11218,.F.);
#15377=ORIENTED_EDGE('',*,*,#11223,.T.);
#15378=ORIENTED_EDGE('',*,*,#11224,.T.);
#15379=ORIENTED_EDGE('',*,*,#11225,.F.);
#15380=ORIENTED_EDGE('',*,*,#11221,.F.);
#15381=ORIENTED_EDGE('',*,*,#11226,.T.);
#15382=ORIENTED_EDGE('',*,*,#11227,.T.);
#15383=ORIENTED_EDGE('',*,*,#11228,.F.);
#15384=ORIENTED_EDGE('',*,*,#11224,.F.);
#15385=ORIENTED_EDGE('',*,*,#11229,.F.);
#15386=ORIENTED_EDGE('',*,*,#11162,.T.);
#15387=ORIENTED_EDGE('',*,*,#11230,.F.);
#15388=ORIENTED_EDGE('',*,*,#11227,.F.);
#15389=ORIENTED_EDGE('',*,*,#11231,.T.);
#15390=ORIENTED_EDGE('',*,*,#11232,.T.);
#15391=ORIENTED_EDGE('',*,*,#11233,.F.);
#15392=ORIENTED_EDGE('',*,*,#11232,.F.);
#15393=ORIENTED_EDGE('',*,*,#11234,.T.);
#15394=ORIENTED_EDGE('',*,*,#11235,.T.);
#15395=ORIENTED_EDGE('',*,*,#11236,.T.);
#15396=ORIENTED_EDGE('',*,*,#11215,.F.);
#15397=ORIENTED_EDGE('',*,*,#11237,.F.);
#15398=ORIENTED_EDGE('',*,*,#10853,.T.);
#15399=ORIENTED_EDGE('',*,*,#11238,.F.);
#15400=ORIENTED_EDGE('',*,*,#11239,.F.);
#15401=ORIENTED_EDGE('',*,*,#11240,.T.);
#15402=ORIENTED_EDGE('',*,*,#11239,.T.);
#15403=ORIENTED_EDGE('',*,*,#11241,.F.);
#15404=ORIENTED_EDGE('',*,*,#11242,.F.);
#15405=ORIENTED_EDGE('',*,*,#11243,.T.);
#15406=ORIENTED_EDGE('',*,*,#11242,.T.);
#15407=ORIENTED_EDGE('',*,*,#11244,.F.);
#15408=ORIENTED_EDGE('',*,*,#11245,.F.);
#15409=ORIENTED_EDGE('',*,*,#11246,.T.);
#15410=ORIENTED_EDGE('',*,*,#11245,.T.);
#15411=ORIENTED_EDGE('',*,*,#11247,.F.);
#15412=ORIENTED_EDGE('',*,*,#11248,.F.);
#15413=ORIENTED_EDGE('',*,*,#11249,.T.);
#15414=ORIENTED_EDGE('',*,*,#11248,.T.);
#15415=ORIENTED_EDGE('',*,*,#11250,.F.);
#15416=ORIENTED_EDGE('',*,*,#11251,.F.);
#15417=ORIENTED_EDGE('',*,*,#11252,.T.);
#15418=ORIENTED_EDGE('',*,*,#11251,.T.);
#15419=ORIENTED_EDGE('',*,*,#11253,.F.);
#15420=ORIENTED_EDGE('',*,*,#11254,.F.);
#15421=ORIENTED_EDGE('',*,*,#11255,.T.);
#15422=ORIENTED_EDGE('',*,*,#11254,.T.);
#15423=ORIENTED_EDGE('',*,*,#11256,.F.);
#15424=ORIENTED_EDGE('',*,*,#11235,.F.);
#15425=ORIENTED_EDGE('',*,*,#11257,.T.);
#15426=ORIENTED_EDGE('',*,*,#11258,.T.);
#15427=ORIENTED_EDGE('',*,*,#11259,.F.);
#15428=ORIENTED_EDGE('',*,*,#11260,.F.);
#15429=ORIENTED_EDGE('',*,*,#11261,.T.);
#15430=ORIENTED_EDGE('',*,*,#11262,.T.);
#15431=ORIENTED_EDGE('',*,*,#11263,.F.);
#15432=ORIENTED_EDGE('',*,*,#11258,.F.);
#15433=ORIENTED_EDGE('',*,*,#11264,.T.);
#15434=ORIENTED_EDGE('',*,*,#11265,.T.);
#15435=ORIENTED_EDGE('',*,*,#11266,.F.);
#15436=ORIENTED_EDGE('',*,*,#11262,.F.);
#15437=ORIENTED_EDGE('',*,*,#11267,.T.);
#15438=ORIENTED_EDGE('',*,*,#11268,.T.);
#15439=ORIENTED_EDGE('',*,*,#11269,.F.);
#15440=ORIENTED_EDGE('',*,*,#11270,.F.);
#15441=ORIENTED_EDGE('',*,*,#11271,.T.);
#15442=ORIENTED_EDGE('',*,*,#11270,.T.);
#15443=ORIENTED_EDGE('',*,*,#11272,.F.);
#15444=ORIENTED_EDGE('',*,*,#11273,.F.);
#15445=ORIENTED_EDGE('',*,*,#11274,.T.);
#15446=ORIENTED_EDGE('',*,*,#11273,.T.);
#15447=ORIENTED_EDGE('',*,*,#11275,.F.);
#15448=ORIENTED_EDGE('',*,*,#11276,.F.);
#15449=ORIENTED_EDGE('',*,*,#11277,.T.);
#15450=ORIENTED_EDGE('',*,*,#11276,.T.);
#15451=ORIENTED_EDGE('',*,*,#11278,.F.);
#15452=ORIENTED_EDGE('',*,*,#11279,.F.);
#15453=ORIENTED_EDGE('',*,*,#11280,.T.);
#15454=ORIENTED_EDGE('',*,*,#11279,.T.);
#15455=ORIENTED_EDGE('',*,*,#11281,.F.);
#15456=ORIENTED_EDGE('',*,*,#11282,.F.);
#15457=ORIENTED_EDGE('',*,*,#11283,.T.);
#15458=ORIENTED_EDGE('',*,*,#11282,.T.);
#15459=ORIENTED_EDGE('',*,*,#11284,.F.);
#15460=ORIENTED_EDGE('',*,*,#11285,.F.);
#15461=ORIENTED_EDGE('',*,*,#11286,.F.);
#15462=ORIENTED_EDGE('',*,*,#11125,.T.);
#15463=ORIENTED_EDGE('',*,*,#11287,.T.);
#15464=ORIENTED_EDGE('',*,*,#11288,.F.);
#15465=ORIENTED_EDGE('',*,*,#11289,.F.);
#15466=ORIENTED_EDGE('',*,*,#11288,.T.);
#15467=ORIENTED_EDGE('',*,*,#11290,.T.);
#15468=ORIENTED_EDGE('',*,*,#11291,.F.);
#15469=ORIENTED_EDGE('',*,*,#11292,.F.);
#15470=ORIENTED_EDGE('',*,*,#11291,.T.);
#15471=ORIENTED_EDGE('',*,*,#11293,.T.);
#15472=ORIENTED_EDGE('',*,*,#11294,.F.);
#15473=ORIENTED_EDGE('',*,*,#11295,.F.);
#15474=ORIENTED_EDGE('',*,*,#11294,.T.);
#15475=ORIENTED_EDGE('',*,*,#11296,.T.);
#15476=ORIENTED_EDGE('',*,*,#11297,.F.);
#15477=ORIENTED_EDGE('',*,*,#11298,.F.);
#15478=ORIENTED_EDGE('',*,*,#11285,.T.);
#15479=ORIENTED_EDGE('',*,*,#11299,.F.);
#15480=ORIENTED_EDGE('',*,*,#11300,.F.);
#15481=ORIENTED_EDGE('',*,*,#11301,.T.);
#15482=ORIENTED_EDGE('',*,*,#11302,.T.);
#15483=ORIENTED_EDGE('',*,*,#11303,.T.);
#15484=ORIENTED_EDGE('',*,*,#11133,.F.);
#15485=ORIENTED_EDGE('',*,*,#11304,.F.);
#15486=ORIENTED_EDGE('',*,*,#11305,.T.);
#15487=ORIENTED_EDGE('',*,*,#11306,.T.);
#15488=ORIENTED_EDGE('',*,*,#11302,.F.);
#15489=ORIENTED_EDGE('',*,*,#11307,.F.);
#15490=ORIENTED_EDGE('',*,*,#11308,.T.);
#15491=ORIENTED_EDGE('',*,*,#11309,.T.);
#15492=ORIENTED_EDGE('',*,*,#11305,.F.);
#15493=ORIENTED_EDGE('',*,*,#11310,.F.);
#15494=ORIENTED_EDGE('',*,*,#11311,.T.);
#15495=ORIENTED_EDGE('',*,*,#11312,.T.);
#15496=ORIENTED_EDGE('',*,*,#11308,.F.);
#15497=ORIENTED_EDGE('',*,*,#11313,.F.);
#15498=ORIENTED_EDGE('',*,*,#11314,.T.);
#15499=ORIENTED_EDGE('',*,*,#11315,.T.);
#15500=ORIENTED_EDGE('',*,*,#11311,.F.);
#15501=ORIENTED_EDGE('',*,*,#11316,.F.);
#15502=ORIENTED_EDGE('',*,*,#11317,.T.);
#15503=ORIENTED_EDGE('',*,*,#11318,.T.);
#15504=ORIENTED_EDGE('',*,*,#11314,.F.);
#15505=ORIENTED_EDGE('',*,*,#11319,.F.);
#15506=ORIENTED_EDGE('',*,*,#11300,.T.);
#15507=ORIENTED_EDGE('',*,*,#11320,.T.);
#15508=ORIENTED_EDGE('',*,*,#11317,.F.);
#15509=ORIENTED_EDGE('',*,*,#11321,.F.);
#15510=ORIENTED_EDGE('',*,*,#11322,.T.);
#15511=ORIENTED_EDGE('',*,*,#11323,.T.);
#15512=ORIENTED_EDGE('',*,*,#11324,.F.);
#15513=ORIENTED_EDGE('',*,*,#11325,.F.);
#15514=ORIENTED_EDGE('',*,*,#11324,.T.);
#15515=ORIENTED_EDGE('',*,*,#11326,.T.);
#15516=ORIENTED_EDGE('',*,*,#11327,.F.);
#15517=ORIENTED_EDGE('',*,*,#11328,.F.);
#15518=ORIENTED_EDGE('',*,*,#11327,.T.);
#15519=ORIENTED_EDGE('',*,*,#11329,.T.);
#15520=ORIENTED_EDGE('',*,*,#11330,.F.);
#15521=ORIENTED_EDGE('',*,*,#11331,.T.);
#15522=ORIENTED_EDGE('',*,*,#11330,.T.);
#15523=ORIENTED_EDGE('',*,*,#11332,.T.);
#15524=ORIENTED_EDGE('',*,*,#11265,.F.);
#15525=ORIENTED_EDGE('',*,*,#11333,.F.);
#15526=ORIENTED_EDGE('',*,*,#11334,.T.);
#15527=ORIENTED_EDGE('',*,*,#11335,.T.);
#15528=ORIENTED_EDGE('',*,*,#11336,.F.);
#15529=ORIENTED_EDGE('',*,*,#11337,.F.);
#15530=ORIENTED_EDGE('',*,*,#11338,.T.);
#15531=ORIENTED_EDGE('',*,*,#11339,.T.);
#15532=ORIENTED_EDGE('',*,*,#11334,.F.);
#15533=ORIENTED_EDGE('',*,*,#11340,.F.);
#15534=ORIENTED_EDGE('',*,*,#11341,.T.);
#15535=ORIENTED_EDGE('',*,*,#11342,.T.);
#15536=ORIENTED_EDGE('',*,*,#11338,.F.);
#15537=ORIENTED_EDGE('',*,*,#11343,.F.);
#15538=ORIENTED_EDGE('',*,*,#11344,.T.);
#15539=ORIENTED_EDGE('',*,*,#11345,.T.);
#15540=ORIENTED_EDGE('',*,*,#11341,.F.);
#15541=ORIENTED_EDGE('',*,*,#11346,.F.);
#15542=ORIENTED_EDGE('',*,*,#11347,.T.);
#15543=ORIENTED_EDGE('',*,*,#11348,.T.);
#15544=ORIENTED_EDGE('',*,*,#11344,.F.);
#15545=ORIENTED_EDGE('',*,*,#11349,.F.);
#15546=ORIENTED_EDGE('',*,*,#11350,.T.);
#15547=ORIENTED_EDGE('',*,*,#11351,.T.);
#15548=ORIENTED_EDGE('',*,*,#11347,.F.);
#15549=ORIENTED_EDGE('',*,*,#11352,.T.);
#15550=ORIENTED_EDGE('',*,*,#11353,.T.);
#15551=ORIENTED_EDGE('',*,*,#11354,.T.);
#15552=ORIENTED_EDGE('',*,*,#11187,.F.);
#15553=ORIENTED_EDGE('',*,*,#11355,.T.);
#15554=ORIENTED_EDGE('',*,*,#11356,.T.);
#15555=ORIENTED_EDGE('',*,*,#11357,.F.);
#15556=ORIENTED_EDGE('',*,*,#11353,.F.);
#15557=ORIENTED_EDGE('',*,*,#11358,.T.);
#15558=ORIENTED_EDGE('',*,*,#11359,.T.);
#15559=ORIENTED_EDGE('',*,*,#11360,.F.);
#15560=ORIENTED_EDGE('',*,*,#11356,.F.);
#15561=ORIENTED_EDGE('',*,*,#11361,.T.);
#15562=ORIENTED_EDGE('',*,*,#11362,.T.);
#15563=ORIENTED_EDGE('',*,*,#11363,.F.);
#15564=ORIENTED_EDGE('',*,*,#11359,.F.);
#15565=ORIENTED_EDGE('',*,*,#11364,.F.);
#15566=ORIENTED_EDGE('',*,*,#11297,.T.);
#15567=ORIENTED_EDGE('',*,*,#11365,.F.);
#15568=ORIENTED_EDGE('',*,*,#11362,.F.);
#15569=ORIENTED_EDGE('',*,*,#11366,.T.);
#15570=ORIENTED_EDGE('',*,*,#11367,.T.);
#15571=ORIENTED_EDGE('',*,*,#11368,.F.);
#15572=ORIENTED_EDGE('',*,*,#11367,.F.);
#15573=ORIENTED_EDGE('',*,*,#11369,.T.);
#15574=ORIENTED_EDGE('',*,*,#11370,.T.);
#15575=ORIENTED_EDGE('',*,*,#11371,.T.);
#15576=ORIENTED_EDGE('',*,*,#11350,.F.);
#15577=ORIENTED_EDGE('',*,*,#11372,.F.);
#15578=ORIENTED_EDGE('',*,*,#11201,.T.);
#15579=ORIENTED_EDGE('',*,*,#11373,.F.);
#15580=ORIENTED_EDGE('',*,*,#11374,.F.);
#15581=ORIENTED_EDGE('',*,*,#11375,.T.);
#15582=ORIENTED_EDGE('',*,*,#11374,.T.);
#15583=ORIENTED_EDGE('',*,*,#11376,.F.);
#15584=ORIENTED_EDGE('',*,*,#11377,.F.);
#15585=ORIENTED_EDGE('',*,*,#11378,.T.);
#15586=ORIENTED_EDGE('',*,*,#11377,.T.);
#15587=ORIENTED_EDGE('',*,*,#11379,.F.);
#15588=ORIENTED_EDGE('',*,*,#11380,.F.);
#15589=ORIENTED_EDGE('',*,*,#11381,.T.);
#15590=ORIENTED_EDGE('',*,*,#11380,.T.);
#15591=ORIENTED_EDGE('',*,*,#11382,.F.);
#15592=ORIENTED_EDGE('',*,*,#11383,.F.);
#15593=ORIENTED_EDGE('',*,*,#11384,.T.);
#15594=ORIENTED_EDGE('',*,*,#11383,.T.);
#15595=ORIENTED_EDGE('',*,*,#11385,.F.);
#15596=ORIENTED_EDGE('',*,*,#11386,.F.);
#15597=ORIENTED_EDGE('',*,*,#11387,.T.);
#15598=ORIENTED_EDGE('',*,*,#11386,.T.);
#15599=ORIENTED_EDGE('',*,*,#11388,.F.);
#15600=ORIENTED_EDGE('',*,*,#11389,.F.);
#15601=ORIENTED_EDGE('',*,*,#11390,.T.);
#15602=ORIENTED_EDGE('',*,*,#11389,.T.);
#15603=ORIENTED_EDGE('',*,*,#11391,.F.);
#15604=ORIENTED_EDGE('',*,*,#11370,.F.);
#15605=ORIENTED_EDGE('',*,*,#11392,.F.);
#15606=ORIENTED_EDGE('',*,*,#11393,.T.);
#15607=ORIENTED_EDGE('',*,*,#11394,.T.);
#15608=ORIENTED_EDGE('',*,*,#11395,.F.);
#15609=ORIENTED_EDGE('',*,*,#11396,.F.);
#15610=ORIENTED_EDGE('',*,*,#11395,.T.);
#15611=ORIENTED_EDGE('',*,*,#11397,.T.);
#15612=ORIENTED_EDGE('',*,*,#11398,.F.);
#15613=ORIENTED_EDGE('',*,*,#11399,.F.);
#15614=ORIENTED_EDGE('',*,*,#11398,.T.);
#15615=ORIENTED_EDGE('',*,*,#11400,.T.);
#15616=ORIENTED_EDGE('',*,*,#11401,.F.);
#15617=ORIENTED_EDGE('',*,*,#11402,.F.);
#15618=ORIENTED_EDGE('',*,*,#11401,.T.);
#15619=ORIENTED_EDGE('',*,*,#11403,.T.);
#15620=ORIENTED_EDGE('',*,*,#11404,.F.);
#15621=ORIENTED_EDGE('',*,*,#11405,.F.);
#15622=ORIENTED_EDGE('',*,*,#11406,.T.);
#15623=ORIENTED_EDGE('',*,*,#11407,.T.);
#15624=ORIENTED_EDGE('',*,*,#11408,.F.);
#15625=ORIENTED_EDGE('',*,*,#11409,.F.);
#15626=ORIENTED_EDGE('',*,*,#11408,.T.);
#15627=ORIENTED_EDGE('',*,*,#11410,.T.);
#15628=ORIENTED_EDGE('',*,*,#11411,.F.);
#15629=ORIENTED_EDGE('',*,*,#11412,.F.);
#15630=ORIENTED_EDGE('',*,*,#11411,.T.);
#15631=ORIENTED_EDGE('',*,*,#11413,.T.);
#15632=ORIENTED_EDGE('',*,*,#11414,.F.);
#15633=ORIENTED_EDGE('',*,*,#11415,.F.);
#15634=ORIENTED_EDGE('',*,*,#11414,.T.);
#15635=ORIENTED_EDGE('',*,*,#11416,.T.);
#15636=ORIENTED_EDGE('',*,*,#11417,.F.);
#15637=ORIENTED_EDGE('',*,*,#11418,.F.);
#15638=ORIENTED_EDGE('',*,*,#11417,.T.);
#15639=ORIENTED_EDGE('',*,*,#11419,.T.);
#15640=ORIENTED_EDGE('',*,*,#11420,.F.);
#15641=ORIENTED_EDGE('',*,*,#11421,.F.);
#15642=ORIENTED_EDGE('',*,*,#11420,.T.);
#15643=ORIENTED_EDGE('',*,*,#11422,.T.);
#15644=ORIENTED_EDGE('',*,*,#11423,.F.);
#15645=ORIENTED_EDGE('',*,*,#11424,.T.);
#15646=ORIENTED_EDGE('',*,*,#11423,.T.);
#15647=ORIENTED_EDGE('',*,*,#11425,.T.);
#15648=ORIENTED_EDGE('',*,*,#11268,.F.);
#15649=ORIENTED_EDGE('',*,*,#11426,.F.);
#15650=ORIENTED_EDGE('',*,*,#11260,.T.);
#15651=ORIENTED_EDGE('',*,*,#11427,.F.);
#15652=ORIENTED_EDGE('',*,*,#11428,.F.);
#15653=ORIENTED_EDGE('',*,*,#11429,.F.);
#15654=ORIENTED_EDGE('',*,*,#11428,.T.);
#15655=ORIENTED_EDGE('',*,*,#11430,.T.);
#15656=ORIENTED_EDGE('',*,*,#11431,.F.);
#15657=ORIENTED_EDGE('',*,*,#11432,.F.);
#15658=ORIENTED_EDGE('',*,*,#11431,.T.);
#15659=ORIENTED_EDGE('',*,*,#11433,.T.);
#15660=ORIENTED_EDGE('',*,*,#11434,.F.);
#15661=ORIENTED_EDGE('',*,*,#11435,.F.);
#15662=ORIENTED_EDGE('',*,*,#11434,.T.);
#15663=ORIENTED_EDGE('',*,*,#11436,.T.);
#15664=ORIENTED_EDGE('',*,*,#11437,.F.);
#15665=ORIENTED_EDGE('',*,*,#11438,.F.);
#15666=ORIENTED_EDGE('',*,*,#11439,.T.);
#15667=ORIENTED_EDGE('',*,*,#11440,.T.);
#15668=ORIENTED_EDGE('',*,*,#11393,.F.);
#15669=ORIENTED_EDGE('',*,*,#11441,.F.);
#15670=ORIENTED_EDGE('',*,*,#11442,.T.);
#15671=ORIENTED_EDGE('',*,*,#11443,.T.);
#15672=ORIENTED_EDGE('',*,*,#11439,.F.);
#15673=ORIENTED_EDGE('',*,*,#11444,.F.);
#15674=ORIENTED_EDGE('',*,*,#11445,.T.);
#15675=ORIENTED_EDGE('',*,*,#11446,.T.);
#15676=ORIENTED_EDGE('',*,*,#11442,.F.);
#15677=ORIENTED_EDGE('',*,*,#11447,.F.);
#15678=ORIENTED_EDGE('',*,*,#11404,.T.);
#15679=ORIENTED_EDGE('',*,*,#11448,.T.);
#15680=ORIENTED_EDGE('',*,*,#11445,.F.);
#15681=ORIENTED_EDGE('',*,*,#11449,.F.);
#15682=ORIENTED_EDGE('',*,*,#11450,.T.);
#15683=ORIENTED_EDGE('',*,*,#11451,.T.);
#15684=ORIENTED_EDGE('',*,*,#11406,.F.);
#15685=ORIENTED_EDGE('',*,*,#11452,.F.);
#15686=ORIENTED_EDGE('',*,*,#11453,.T.);
#15687=ORIENTED_EDGE('',*,*,#11454,.T.);
#15688=ORIENTED_EDGE('',*,*,#11450,.F.);
#15689=ORIENTED_EDGE('',*,*,#11455,.F.);
#15690=ORIENTED_EDGE('',*,*,#11456,.T.);
#15691=ORIENTED_EDGE('',*,*,#11457,.T.);
#15692=ORIENTED_EDGE('',*,*,#11453,.F.);
#15693=ORIENTED_EDGE('',*,*,#11458,.F.);
#15694=ORIENTED_EDGE('',*,*,#11459,.T.);
#15695=ORIENTED_EDGE('',*,*,#11460,.T.);
#15696=ORIENTED_EDGE('',*,*,#11456,.F.);
#15697=ORIENTED_EDGE('',*,*,#11461,.F.);
#15698=ORIENTED_EDGE('',*,*,#11462,.T.);
#15699=ORIENTED_EDGE('',*,*,#11463,.T.);
#15700=ORIENTED_EDGE('',*,*,#11459,.F.);
#15701=ORIENTED_EDGE('',*,*,#11464,.F.);
#15702=ORIENTED_EDGE('',*,*,#11465,.T.);
#15703=ORIENTED_EDGE('',*,*,#11466,.T.);
#15704=ORIENTED_EDGE('',*,*,#11462,.F.);
#15705=ORIENTED_EDGE('',*,*,#11467,.F.);
#15706=ORIENTED_EDGE('',*,*,#11468,.T.);
#15707=ORIENTED_EDGE('',*,*,#11469,.T.);
#15708=ORIENTED_EDGE('',*,*,#11465,.F.);
#15709=ORIENTED_EDGE('',*,*,#11470,.F.);
#15710=ORIENTED_EDGE('',*,*,#11471,.T.);
#15711=ORIENTED_EDGE('',*,*,#11472,.T.);
#15712=ORIENTED_EDGE('',*,*,#11468,.F.);
#15713=ORIENTED_EDGE('',*,*,#11473,.F.);
#15714=ORIENTED_EDGE('',*,*,#11474,.T.);
#15715=ORIENTED_EDGE('',*,*,#11475,.T.);
#15716=ORIENTED_EDGE('',*,*,#11471,.F.);
#15717=ORIENTED_EDGE('',*,*,#11476,.F.);
#15718=ORIENTED_EDGE('',*,*,#11477,.T.);
#15719=ORIENTED_EDGE('',*,*,#11478,.T.);
#15720=ORIENTED_EDGE('',*,*,#11474,.F.);
#15721=ORIENTED_EDGE('',*,*,#11479,.F.);
#15722=ORIENTED_EDGE('',*,*,#11480,.T.);
#15723=ORIENTED_EDGE('',*,*,#11481,.T.);
#15724=ORIENTED_EDGE('',*,*,#11477,.F.);
#15725=ORIENTED_EDGE('',*,*,#11482,.F.);
#15726=ORIENTED_EDGE('',*,*,#11483,.T.);
#15727=ORIENTED_EDGE('',*,*,#11484,.T.);
#15728=ORIENTED_EDGE('',*,*,#11480,.F.);
#15729=ORIENTED_EDGE('',*,*,#11485,.F.);
#15730=ORIENTED_EDGE('',*,*,#11486,.T.);
#15731=ORIENTED_EDGE('',*,*,#11487,.T.);
#15732=ORIENTED_EDGE('',*,*,#11483,.F.);
#15733=ORIENTED_EDGE('',*,*,#11488,.F.);
#15734=ORIENTED_EDGE('',*,*,#11489,.T.);
#15735=ORIENTED_EDGE('',*,*,#11490,.T.);
#15736=ORIENTED_EDGE('',*,*,#11486,.F.);
#15737=ORIENTED_EDGE('',*,*,#11491,.F.);
#15738=ORIENTED_EDGE('',*,*,#11492,.T.);
#15739=ORIENTED_EDGE('',*,*,#11493,.T.);
#15740=ORIENTED_EDGE('',*,*,#11489,.F.);
#15741=ORIENTED_EDGE('',*,*,#11494,.F.);
#15742=ORIENTED_EDGE('',*,*,#11495,.T.);
#15743=ORIENTED_EDGE('',*,*,#11496,.T.);
#15744=ORIENTED_EDGE('',*,*,#11492,.F.);
#15745=ORIENTED_EDGE('',*,*,#11166,.F.);
#15746=ORIENTED_EDGE('',*,*,#10788,.F.);
#15747=ORIENTED_EDGE('',*,*,#10792,.F.);
#15748=ORIENTED_EDGE('',*,*,#10795,.F.);
#15749=ORIENTED_EDGE('',*,*,#10798,.F.);
#15750=ORIENTED_EDGE('',*,*,#10801,.F.);
#15751=ORIENTED_EDGE('',*,*,#10804,.F.);
#15752=ORIENTED_EDGE('',*,*,#10817,.T.);
#15753=ORIENTED_EDGE('',*,*,#10836,.T.);
#15754=ORIENTED_EDGE('',*,*,#10833,.T.);
#15755=ORIENTED_EDGE('',*,*,#10830,.T.);
#15756=ORIENTED_EDGE('',*,*,#10827,.T.);
#15757=ORIENTED_EDGE('',*,*,#10824,.T.);
#15758=ORIENTED_EDGE('',*,*,#10820,.T.);
#15759=ORIENTED_EDGE('',*,*,#11042,.T.);
#15760=ORIENTED_EDGE('',*,*,#11039,.F.);
#15761=ORIENTED_EDGE('',*,*,#11036,.F.);
#15762=ORIENTED_EDGE('',*,*,#11033,.F.);
#15763=ORIENTED_EDGE('',*,*,#11030,.F.);
#15764=ORIENTED_EDGE('',*,*,#11027,.F.);
#15765=ORIENTED_EDGE('',*,*,#11023,.F.);
#15766=ORIENTED_EDGE('',*,*,#11075,.F.);
#15767=ORIENTED_EDGE('',*,*,#11078,.F.);
#15768=ORIENTED_EDGE('',*,*,#11081,.F.);
#15769=ORIENTED_EDGE('',*,*,#11084,.F.);
#15770=ORIENTED_EDGE('',*,*,#11087,.F.);
#15771=ORIENTED_EDGE('',*,*,#11090,.F.);
#15772=ORIENTED_EDGE('',*,*,#11093,.F.);
#15773=ORIENTED_EDGE('',*,*,#11096,.F.);
#15774=ORIENTED_EDGE('',*,*,#11099,.F.);
#15775=ORIENTED_EDGE('',*,*,#11102,.F.);
#15776=ORIENTED_EDGE('',*,*,#11105,.F.);
#15777=ORIENTED_EDGE('',*,*,#11108,.F.);
#15778=ORIENTED_EDGE('',*,*,#11111,.F.);
#15779=ORIENTED_EDGE('',*,*,#11114,.F.);
#15780=ORIENTED_EDGE('',*,*,#11117,.F.);
#15781=ORIENTED_EDGE('',*,*,#11120,.F.);
#15782=ORIENTED_EDGE('',*,*,#11061,.F.);
#15783=ORIENTED_EDGE('',*,*,#11007,.T.);
#15784=ORIENTED_EDGE('',*,*,#11004,.T.);
#15785=ORIENTED_EDGE('',*,*,#11001,.T.);
#15786=ORIENTED_EDGE('',*,*,#10998,.T.);
#15787=ORIENTED_EDGE('',*,*,#10995,.T.);
#15788=ORIENTED_EDGE('',*,*,#10992,.T.);
#15789=ORIENTED_EDGE('',*,*,#10989,.T.);
#15790=ORIENTED_EDGE('',*,*,#10986,.T.);
#15791=ORIENTED_EDGE('',*,*,#10983,.T.);
#15792=ORIENTED_EDGE('',*,*,#10980,.T.);
#15793=ORIENTED_EDGE('',*,*,#10977,.T.);
#15794=ORIENTED_EDGE('',*,*,#10974,.T.);
#15795=ORIENTED_EDGE('',*,*,#10971,.T.);
#15796=ORIENTED_EDGE('',*,*,#10968,.T.);
#15797=ORIENTED_EDGE('',*,*,#10965,.T.);
#15798=ORIENTED_EDGE('',*,*,#10962,.T.);
#15799=ORIENTED_EDGE('',*,*,#10918,.T.);
#15800=ORIENTED_EDGE('',*,*,#10922,.T.);
#15801=ORIENTED_EDGE('',*,*,#10925,.T.);
#15802=ORIENTED_EDGE('',*,*,#10928,.T.);
#15803=ORIENTED_EDGE('',*,*,#10931,.T.);
#15804=ORIENTED_EDGE('',*,*,#10934,.T.);
#15805=ORIENTED_EDGE('',*,*,#10937,.F.);
#15806=ORIENTED_EDGE('',*,*,#10887,.F.);
#15807=ORIENTED_EDGE('',*,*,#10891,.F.);
#15808=ORIENTED_EDGE('',*,*,#10894,.F.);
#15809=ORIENTED_EDGE('',*,*,#10897,.F.);
#15810=ORIENTED_EDGE('',*,*,#10900,.F.);
#15811=ORIENTED_EDGE('',*,*,#10903,.F.);
#15812=ORIENTED_EDGE('',*,*,#10884,.F.);
#15813=ORIENTED_EDGE('',*,*,#10866,.T.);
#15814=ORIENTED_EDGE('',*,*,#10863,.T.);
#15815=ORIENTED_EDGE('',*,*,#10860,.T.);
#15816=ORIENTED_EDGE('',*,*,#10857,.T.);
#15817=ORIENTED_EDGE('',*,*,#10854,.T.);
#15818=ORIENTED_EDGE('',*,*,#10850,.T.);
#15819=ORIENTED_EDGE('',*,*,#11237,.T.);
#15820=ORIENTED_EDGE('',*,*,#11240,.F.);
#15821=ORIENTED_EDGE('',*,*,#11243,.F.);
#15822=ORIENTED_EDGE('',*,*,#11246,.F.);
#15823=ORIENTED_EDGE('',*,*,#11249,.F.);
#15824=ORIENTED_EDGE('',*,*,#11252,.F.);
#15825=ORIENTED_EDGE('',*,*,#11255,.F.);
#15826=ORIENTED_EDGE('',*,*,#11234,.F.);
#15827=ORIENTED_EDGE('',*,*,#11214,.T.);
#15828=ORIENTED_EDGE('',*,*,#11211,.T.);
#15829=ORIENTED_EDGE('',*,*,#11208,.T.);
#15830=ORIENTED_EDGE('',*,*,#11205,.T.);
#15831=ORIENTED_EDGE('',*,*,#11202,.T.);
#15832=ORIENTED_EDGE('',*,*,#11198,.T.);
#15833=ORIENTED_EDGE('',*,*,#11372,.T.);
#15834=ORIENTED_EDGE('',*,*,#11375,.F.);
#15835=ORIENTED_EDGE('',*,*,#11378,.F.);
#15836=ORIENTED_EDGE('',*,*,#11381,.F.);
#15837=ORIENTED_EDGE('',*,*,#11384,.F.);
#15838=ORIENTED_EDGE('',*,*,#11387,.F.);
#15839=ORIENTED_EDGE('',*,*,#11390,.F.);
#15840=ORIENTED_EDGE('',*,*,#11369,.F.);
#15841=ORIENTED_EDGE('',*,*,#11349,.T.);
#15842=ORIENTED_EDGE('',*,*,#11346,.T.);
#15843=ORIENTED_EDGE('',*,*,#11343,.T.);
#15844=ORIENTED_EDGE('',*,*,#11340,.T.);
#15845=ORIENTED_EDGE('',*,*,#11337,.T.);
#15846=ORIENTED_EDGE('',*,*,#11333,.T.);
#15847=ORIENTED_EDGE('',*,*,#11497,.T.);
#15848=ORIENTED_EDGE('',*,*,#11498,.F.);
#15849=ORIENTED_EDGE('',*,*,#11499,.F.);
#15850=ORIENTED_EDGE('',*,*,#11500,.F.);
#15851=ORIENTED_EDGE('',*,*,#11501,.F.);
#15852=ORIENTED_EDGE('',*,*,#11502,.F.);
#15853=ORIENTED_EDGE('',*,*,#11503,.F.);
#15854=ORIENTED_EDGE('',*,*,#11504,.F.);
#15855=ORIENTED_EDGE('',*,*,#11505,.F.);
#15856=ORIENTED_EDGE('',*,*,#11506,.F.);
#15857=ORIENTED_EDGE('',*,*,#11507,.F.);
#15858=ORIENTED_EDGE('',*,*,#11508,.F.);
#15859=ORIENTED_EDGE('',*,*,#11509,.F.);
#15860=ORIENTED_EDGE('',*,*,#11510,.F.);
#15861=ORIENTED_EDGE('',*,*,#11511,.F.);
#15862=ORIENTED_EDGE('',*,*,#11512,.F.);
#15863=ORIENTED_EDGE('',*,*,#11513,.F.);
#15864=ORIENTED_EDGE('',*,*,#11514,.F.);
#15865=ORIENTED_EDGE('',*,*,#11515,.F.);
#15866=ORIENTED_EDGE('',*,*,#11516,.F.);
#15867=ORIENTED_EDGE('',*,*,#11517,.F.);
#15868=ORIENTED_EDGE('',*,*,#11518,.F.);
#15869=ORIENTED_EDGE('',*,*,#11519,.F.);
#15870=ORIENTED_EDGE('',*,*,#11520,.F.);
#15871=ORIENTED_EDGE('',*,*,#11494,.T.);
#15872=ORIENTED_EDGE('',*,*,#11491,.T.);
#15873=ORIENTED_EDGE('',*,*,#11488,.T.);
#15874=ORIENTED_EDGE('',*,*,#11485,.T.);
#15875=ORIENTED_EDGE('',*,*,#11482,.T.);
#15876=ORIENTED_EDGE('',*,*,#11479,.T.);
#15877=ORIENTED_EDGE('',*,*,#11476,.T.);
#15878=ORIENTED_EDGE('',*,*,#11473,.T.);
#15879=ORIENTED_EDGE('',*,*,#11470,.T.);
#15880=ORIENTED_EDGE('',*,*,#11467,.T.);
#15881=ORIENTED_EDGE('',*,*,#11464,.T.);
#15882=ORIENTED_EDGE('',*,*,#11461,.T.);
#15883=ORIENTED_EDGE('',*,*,#11458,.T.);
#15884=ORIENTED_EDGE('',*,*,#11455,.T.);
#15885=ORIENTED_EDGE('',*,*,#11452,.T.);
#15886=ORIENTED_EDGE('',*,*,#11449,.T.);
#15887=ORIENTED_EDGE('',*,*,#11405,.T.);
#15888=ORIENTED_EDGE('',*,*,#11409,.T.);
#15889=ORIENTED_EDGE('',*,*,#11412,.T.);
#15890=ORIENTED_EDGE('',*,*,#11415,.T.);
#15891=ORIENTED_EDGE('',*,*,#11418,.T.);
#15892=ORIENTED_EDGE('',*,*,#11421,.T.);
#15893=ORIENTED_EDGE('',*,*,#11424,.F.);
#15894=ORIENTED_EDGE('',*,*,#11267,.F.);
#15895=ORIENTED_EDGE('',*,*,#11271,.F.);
#15896=ORIENTED_EDGE('',*,*,#11274,.F.);
#15897=ORIENTED_EDGE('',*,*,#11277,.F.);
#15898=ORIENTED_EDGE('',*,*,#11280,.F.);
#15899=ORIENTED_EDGE('',*,*,#11283,.F.);
#15900=ORIENTED_EDGE('',*,*,#11298,.T.);
#15901=ORIENTED_EDGE('',*,*,#11319,.T.);
#15902=ORIENTED_EDGE('',*,*,#11316,.T.);
#15903=ORIENTED_EDGE('',*,*,#11313,.T.);
#15904=ORIENTED_EDGE('',*,*,#11310,.T.);
#15905=ORIENTED_EDGE('',*,*,#11307,.T.);
#15906=ORIENTED_EDGE('',*,*,#11304,.T.);
#15907=ORIENTED_EDGE('',*,*,#11301,.F.);
#15908=ORIENTED_EDGE('',*,*,#11132,.F.);
#15909=ORIENTED_EDGE('',*,*,#11136,.F.);
#15910=ORIENTED_EDGE('',*,*,#11139,.F.);
#15911=ORIENTED_EDGE('',*,*,#11142,.F.);
#15912=ORIENTED_EDGE('',*,*,#11145,.F.);
#15913=ORIENTED_EDGE('',*,*,#11148,.F.);
#15914=ORIENTED_EDGE('',*,*,#11163,.T.);
#15915=ORIENTED_EDGE('',*,*,#11184,.T.);
#15916=ORIENTED_EDGE('',*,*,#11181,.T.);
#15917=ORIENTED_EDGE('',*,*,#11178,.T.);
#15918=ORIENTED_EDGE('',*,*,#11175,.T.);
#15919=ORIENTED_EDGE('',*,*,#11172,.T.);
#15920=ORIENTED_EDGE('',*,*,#11169,.T.);
#15921=ORIENTED_EDGE('',*,*,#11151,.T.);
#15922=ORIENTED_EDGE('',*,*,#11154,.T.);
#15923=ORIENTED_EDGE('',*,*,#11157,.T.);
#15924=ORIENTED_EDGE('',*,*,#11160,.T.);
#15925=ORIENTED_EDGE('',*,*,#11229,.T.);
#15926=ORIENTED_EDGE('',*,*,#11226,.F.);
#15927=ORIENTED_EDGE('',*,*,#11223,.F.);
#15928=ORIENTED_EDGE('',*,*,#11220,.F.);
#15929=ORIENTED_EDGE('',*,*,#11217,.F.);
#15930=ORIENTED_EDGE('',*,*,#10838,.T.);
#15931=ORIENTED_EDGE('',*,*,#10842,.T.);
#15932=ORIENTED_EDGE('',*,*,#10845,.T.);
#15933=ORIENTED_EDGE('',*,*,#10848,.F.);
#15934=ORIENTED_EDGE('',*,*,#10785,.F.);
#15935=ORIENTED_EDGE('',*,*,#10782,.F.);
#15936=ORIENTED_EDGE('',*,*,#10778,.F.);
#15937=ORIENTED_EDGE('',*,*,#11060,.T.);
#15938=ORIENTED_EDGE('',*,*,#11020,.F.);
#15939=ORIENTED_EDGE('',*,*,#11017,.F.);
#15940=ORIENTED_EDGE('',*,*,#11014,.F.);
#15941=ORIENTED_EDGE('',*,*,#11010,.F.);
#15942=ORIENTED_EDGE('',*,*,#11064,.F.);
#15943=ORIENTED_EDGE('',*,*,#11067,.F.);
#15944=ORIENTED_EDGE('',*,*,#11070,.F.);
#15945=ORIENTED_EDGE('',*,*,#11073,.F.);
#15946=ORIENTED_EDGE('',*,*,#10915,.T.);
#15947=ORIENTED_EDGE('',*,*,#10960,.T.);
#15948=ORIENTED_EDGE('',*,*,#10957,.T.);
#15949=ORIENTED_EDGE('',*,*,#10954,.T.);
#15950=ORIENTED_EDGE('',*,*,#10951,.T.);
#15951=ORIENTED_EDGE('',*,*,#10905,.T.);
#15952=ORIENTED_EDGE('',*,*,#10909,.T.);
#15953=ORIENTED_EDGE('',*,*,#10912,.T.);
#15954=ORIENTED_EDGE('',*,*,#11044,.F.);
#15955=ORIENTED_EDGE('',*,*,#10807,.T.);
#15956=ORIENTED_EDGE('',*,*,#10811,.T.);
#15957=ORIENTED_EDGE('',*,*,#10814,.T.);
#15958=ORIENTED_EDGE('',*,*,#10879,.T.);
#15959=ORIENTED_EDGE('',*,*,#10876,.F.);
#15960=ORIENTED_EDGE('',*,*,#10873,.F.);
#15961=ORIENTED_EDGE('',*,*,#10869,.F.);
#15962=ORIENTED_EDGE('',*,*,#10939,.T.);
#15963=ORIENTED_EDGE('',*,*,#10942,.T.);
#15964=ORIENTED_EDGE('',*,*,#10945,.T.);
#15965=ORIENTED_EDGE('',*,*,#10948,.T.);
#15966=ORIENTED_EDGE('',*,*,#11056,.T.);
#15967=ORIENTED_EDGE('',*,*,#11053,.F.);
#15968=ORIENTED_EDGE('',*,*,#11050,.F.);
#15969=ORIENTED_EDGE('',*,*,#11047,.F.);
#15970=ORIENTED_EDGE('',*,*,#10883,.T.);
#15971=ORIENTED_EDGE('',*,*,#11286,.T.);
#15972=ORIENTED_EDGE('',*,*,#11289,.T.);
#15973=ORIENTED_EDGE('',*,*,#11292,.T.);
#15974=ORIENTED_EDGE('',*,*,#11295,.T.);
#15975=ORIENTED_EDGE('',*,*,#11364,.T.);
#15976=ORIENTED_EDGE('',*,*,#11361,.F.);
#15977=ORIENTED_EDGE('',*,*,#11358,.F.);
#15978=ORIENTED_EDGE('',*,*,#11355,.F.);
#15979=ORIENTED_EDGE('',*,*,#11352,.F.);
#15980=ORIENTED_EDGE('',*,*,#11186,.T.);
#15981=ORIENTED_EDGE('',*,*,#11190,.T.);
#15982=ORIENTED_EDGE('',*,*,#11193,.T.);
#15983=ORIENTED_EDGE('',*,*,#11196,.F.);
#15984=ORIENTED_EDGE('',*,*,#11129,.F.);
#15985=ORIENTED_EDGE('',*,*,#11126,.F.);
#15986=ORIENTED_EDGE('',*,*,#11122,.F.);
#15987=ORIENTED_EDGE('',*,*,#11233,.T.);
#15988=ORIENTED_EDGE('',*,*,#11426,.T.);
#15989=ORIENTED_EDGE('',*,*,#11429,.T.);
#15990=ORIENTED_EDGE('',*,*,#11432,.T.);
#15991=ORIENTED_EDGE('',*,*,#11435,.T.);
#15992=ORIENTED_EDGE('',*,*,#11521,.T.);
#15993=ORIENTED_EDGE('',*,*,#11522,.F.);
#15994=ORIENTED_EDGE('',*,*,#11523,.F.);
#15995=ORIENTED_EDGE('',*,*,#11524,.F.);
#15996=ORIENTED_EDGE('',*,*,#11525,.F.);
#15997=ORIENTED_EDGE('',*,*,#11321,.T.);
#15998=ORIENTED_EDGE('',*,*,#11325,.T.);
#15999=ORIENTED_EDGE('',*,*,#11328,.T.);
#16000=ORIENTED_EDGE('',*,*,#11331,.F.);
#16001=ORIENTED_EDGE('',*,*,#11264,.F.);
#16002=ORIENTED_EDGE('',*,*,#11261,.F.);
#16003=ORIENTED_EDGE('',*,*,#11257,.F.);
#16004=ORIENTED_EDGE('',*,*,#11368,.T.);
#16005=ORIENTED_EDGE('',*,*,#11402,.T.);
#16006=ORIENTED_EDGE('',*,*,#11447,.T.);
#16007=ORIENTED_EDGE('',*,*,#11444,.T.);
#16008=ORIENTED_EDGE('',*,*,#11441,.T.);
#16009=ORIENTED_EDGE('',*,*,#11438,.T.);
#16010=ORIENTED_EDGE('',*,*,#11392,.T.);
#16011=ORIENTED_EDGE('',*,*,#11396,.T.);
#16012=ORIENTED_EDGE('',*,*,#11399,.T.);
#16013=ORIENTED_EDGE('',*,*,#11526,.F.);
#16014=ORIENTED_EDGE('',*,*,#11527,.F.);
#16015=ORIENTED_EDGE('',*,*,#11528,.F.);
#16016=ORIENTED_EDGE('',*,*,#11529,.F.);
#16017=ORIENTED_EDGE('',*,*,#11530,.F.);
#16018=ORIENTED_EDGE('',*,*,#11531,.F.);
#16019=ORIENTED_EDGE('',*,*,#11532,.F.);
#16020=ORIENTED_EDGE('',*,*,#11533,.F.);
#16021=ORIENTED_EDGE('',*,*,#11534,.T.);
#16022=ORIENTED_EDGE('',*,*,#11529,.T.);
#16023=ORIENTED_EDGE('',*,*,#11535,.T.);
#16024=ORIENTED_EDGE('',*,*,#11536,.F.);
#16025=ORIENTED_EDGE('',*,*,#11537,.F.);
#16026=ORIENTED_EDGE('',*,*,#11528,.T.);
#16027=ORIENTED_EDGE('',*,*,#11538,.T.);
#16028=ORIENTED_EDGE('',*,*,#11539,.F.);
#16029=ORIENTED_EDGE('',*,*,#11535,.F.);
#16030=ORIENTED_EDGE('',*,*,#11527,.T.);
#16031=ORIENTED_EDGE('',*,*,#11540,.T.);
#16032=ORIENTED_EDGE('',*,*,#11541,.F.);
#16033=ORIENTED_EDGE('',*,*,#11538,.F.);
#16034=ORIENTED_EDGE('',*,*,#11526,.T.);
#16035=ORIENTED_EDGE('',*,*,#11542,.T.);
#16036=ORIENTED_EDGE('',*,*,#11543,.F.);
#16037=ORIENTED_EDGE('',*,*,#11540,.F.);
#16038=ORIENTED_EDGE('',*,*,#11503,.T.);
#16039=ORIENTED_EDGE('',*,*,#11544,.T.);
#16040=ORIENTED_EDGE('',*,*,#11545,.F.);
#16041=ORIENTED_EDGE('',*,*,#11546,.F.);
#16042=ORIENTED_EDGE('',*,*,#11502,.T.);
#16043=ORIENTED_EDGE('',*,*,#11547,.T.);
#16044=ORIENTED_EDGE('',*,*,#11548,.F.);
#16045=ORIENTED_EDGE('',*,*,#11544,.F.);
#16046=ORIENTED_EDGE('',*,*,#11501,.T.);
#16047=ORIENTED_EDGE('',*,*,#11549,.T.);
#16048=ORIENTED_EDGE('',*,*,#11550,.F.);
#16049=ORIENTED_EDGE('',*,*,#11547,.F.);
#16050=ORIENTED_EDGE('',*,*,#11500,.T.);
#16051=ORIENTED_EDGE('',*,*,#11551,.T.);
#16052=ORIENTED_EDGE('',*,*,#11552,.F.);
#16053=ORIENTED_EDGE('',*,*,#11549,.F.);
#16054=ORIENTED_EDGE('',*,*,#11499,.T.);
#16055=ORIENTED_EDGE('',*,*,#11553,.T.);
#16056=ORIENTED_EDGE('',*,*,#11554,.F.);
#16057=ORIENTED_EDGE('',*,*,#11551,.F.);
#16058=ORIENTED_EDGE('',*,*,#11498,.T.);
#16059=ORIENTED_EDGE('',*,*,#11555,.T.);
#16060=ORIENTED_EDGE('',*,*,#11556,.F.);
#16061=ORIENTED_EDGE('',*,*,#11553,.F.);
#16062=ORIENTED_EDGE('',*,*,#11497,.F.);
#16063=ORIENTED_EDGE('',*,*,#11336,.T.);
#16064=ORIENTED_EDGE('',*,*,#11557,.F.);
#16065=ORIENTED_EDGE('',*,*,#11555,.F.);
#16066=ORIENTED_EDGE('',*,*,#11525,.T.);
#16067=ORIENTED_EDGE('',*,*,#11558,.T.);
#16068=ORIENTED_EDGE('',*,*,#11559,.T.);
#16069=ORIENTED_EDGE('',*,*,#11322,.F.);
#16070=ORIENTED_EDGE('',*,*,#11524,.T.);
#16071=ORIENTED_EDGE('',*,*,#11560,.T.);
#16072=ORIENTED_EDGE('',*,*,#11561,.F.);
#16073=ORIENTED_EDGE('',*,*,#11558,.F.);
#16074=ORIENTED_EDGE('',*,*,#11523,.T.);
#16075=ORIENTED_EDGE('',*,*,#11562,.T.);
#16076=ORIENTED_EDGE('',*,*,#11563,.F.);
#16077=ORIENTED_EDGE('',*,*,#11560,.F.);
#16078=ORIENTED_EDGE('',*,*,#11522,.T.);
#16079=ORIENTED_EDGE('',*,*,#11564,.T.);
#16080=ORIENTED_EDGE('',*,*,#11565,.F.);
#16081=ORIENTED_EDGE('',*,*,#11562,.F.);
#16082=ORIENTED_EDGE('',*,*,#11521,.F.);
#16083=ORIENTED_EDGE('',*,*,#11437,.T.);
#16084=ORIENTED_EDGE('',*,*,#11566,.F.);
#16085=ORIENTED_EDGE('',*,*,#11564,.F.);
#16086=ORIENTED_EDGE('',*,*,#11567,.F.);
#16087=ORIENTED_EDGE('',*,*,#11568,.T.);
#16088=ORIENTED_EDGE('',*,*,#11534,.F.);
#16089=ORIENTED_EDGE('',*,*,#11568,.F.);
#16090=ORIENTED_EDGE('',*,*,#11520,.T.);
#16091=ORIENTED_EDGE('',*,*,#11569,.T.);
#16092=ORIENTED_EDGE('',*,*,#11570,.T.);
#16093=ORIENTED_EDGE('',*,*,#11495,.F.);
#16094=ORIENTED_EDGE('',*,*,#11530,.T.);
#16095=ORIENTED_EDGE('',*,*,#11537,.T.);
#16096=ORIENTED_EDGE('',*,*,#11571,.F.);
#16097=ORIENTED_EDGE('',*,*,#11572,.F.);
#16098=ORIENTED_EDGE('',*,*,#11531,.T.);
#16099=ORIENTED_EDGE('',*,*,#11572,.T.);
#16100=ORIENTED_EDGE('',*,*,#11573,.F.);
#16101=ORIENTED_EDGE('',*,*,#11574,.F.);
#16102=ORIENTED_EDGE('',*,*,#11532,.T.);
#16103=ORIENTED_EDGE('',*,*,#11574,.T.);
#16104=ORIENTED_EDGE('',*,*,#11575,.F.);
#16105=ORIENTED_EDGE('',*,*,#11576,.F.);
#16106=ORIENTED_EDGE('',*,*,#11533,.T.);
#16107=ORIENTED_EDGE('',*,*,#11576,.T.);
#16108=ORIENTED_EDGE('',*,*,#11577,.F.);
#16109=ORIENTED_EDGE('',*,*,#11542,.F.);
#16110=ORIENTED_EDGE('',*,*,#11504,.T.);
#16111=ORIENTED_EDGE('',*,*,#11546,.T.);
#16112=ORIENTED_EDGE('',*,*,#11578,.F.);
#16113=ORIENTED_EDGE('',*,*,#11579,.F.);
#16114=ORIENTED_EDGE('',*,*,#11505,.T.);
#16115=ORIENTED_EDGE('',*,*,#11579,.T.);
#16116=ORIENTED_EDGE('',*,*,#11580,.F.);
#16117=ORIENTED_EDGE('',*,*,#11581,.F.);
#16118=ORIENTED_EDGE('',*,*,#11506,.T.);
#16119=ORIENTED_EDGE('',*,*,#11581,.T.);
#16120=ORIENTED_EDGE('',*,*,#11582,.F.);
#16121=ORIENTED_EDGE('',*,*,#11583,.F.);
#16122=ORIENTED_EDGE('',*,*,#11507,.T.);
#16123=ORIENTED_EDGE('',*,*,#11583,.T.);
#16124=ORIENTED_EDGE('',*,*,#11584,.F.);
#16125=ORIENTED_EDGE('',*,*,#11585,.F.);
#16126=ORIENTED_EDGE('',*,*,#11508,.T.);
#16127=ORIENTED_EDGE('',*,*,#11585,.T.);
#16128=ORIENTED_EDGE('',*,*,#11586,.F.);
#16129=ORIENTED_EDGE('',*,*,#11587,.F.);
#16130=ORIENTED_EDGE('',*,*,#11509,.T.);
#16131=ORIENTED_EDGE('',*,*,#11587,.T.);
#16132=ORIENTED_EDGE('',*,*,#11588,.F.);
#16133=ORIENTED_EDGE('',*,*,#11589,.F.);
#16134=ORIENTED_EDGE('',*,*,#11510,.T.);
#16135=ORIENTED_EDGE('',*,*,#11589,.T.);
#16136=ORIENTED_EDGE('',*,*,#11590,.F.);
#16137=ORIENTED_EDGE('',*,*,#11591,.F.);
#16138=ORIENTED_EDGE('',*,*,#11511,.T.);
#16139=ORIENTED_EDGE('',*,*,#11591,.T.);
#16140=ORIENTED_EDGE('',*,*,#11592,.F.);
#16141=ORIENTED_EDGE('',*,*,#11593,.F.);
#16142=ORIENTED_EDGE('',*,*,#11512,.T.);
#16143=ORIENTED_EDGE('',*,*,#11593,.T.);
#16144=ORIENTED_EDGE('',*,*,#11594,.F.);
#16145=ORIENTED_EDGE('',*,*,#11595,.F.);
#16146=ORIENTED_EDGE('',*,*,#11513,.T.);
#16147=ORIENTED_EDGE('',*,*,#11595,.T.);
#16148=ORIENTED_EDGE('',*,*,#11596,.F.);
#16149=ORIENTED_EDGE('',*,*,#11597,.F.);
#16150=ORIENTED_EDGE('',*,*,#11514,.T.);
#16151=ORIENTED_EDGE('',*,*,#11597,.T.);
#16152=ORIENTED_EDGE('',*,*,#11598,.F.);
#16153=ORIENTED_EDGE('',*,*,#11599,.F.);
#16154=ORIENTED_EDGE('',*,*,#11515,.T.);
#16155=ORIENTED_EDGE('',*,*,#11599,.T.);
#16156=ORIENTED_EDGE('',*,*,#11600,.F.);
#16157=ORIENTED_EDGE('',*,*,#11601,.F.);
#16158=ORIENTED_EDGE('',*,*,#11516,.T.);
#16159=ORIENTED_EDGE('',*,*,#11601,.T.);
#16160=ORIENTED_EDGE('',*,*,#11602,.F.);
#16161=ORIENTED_EDGE('',*,*,#11603,.F.);
#16162=ORIENTED_EDGE('',*,*,#11517,.T.);
#16163=ORIENTED_EDGE('',*,*,#11603,.T.);
#16164=ORIENTED_EDGE('',*,*,#11604,.F.);
#16165=ORIENTED_EDGE('',*,*,#11605,.F.);
#16166=ORIENTED_EDGE('',*,*,#11518,.T.);
#16167=ORIENTED_EDGE('',*,*,#11605,.T.);
#16168=ORIENTED_EDGE('',*,*,#11606,.F.);
#16169=ORIENTED_EDGE('',*,*,#11607,.F.);
#16170=ORIENTED_EDGE('',*,*,#11519,.T.);
#16171=ORIENTED_EDGE('',*,*,#11607,.T.);
#16172=ORIENTED_EDGE('',*,*,#11608,.F.);
#16173=ORIENTED_EDGE('',*,*,#11569,.F.);
#16174=ORIENTED_EDGE('',*,*,#11168,.F.);
#16175=ORIENTED_EDGE('',*,*,#11171,.F.);
#16176=ORIENTED_EDGE('',*,*,#11174,.F.);
#16177=ORIENTED_EDGE('',*,*,#11177,.F.);
#16178=ORIENTED_EDGE('',*,*,#11180,.F.);
#16179=ORIENTED_EDGE('',*,*,#11183,.F.);
#16180=ORIENTED_EDGE('',*,*,#11185,.F.);
#16181=ORIENTED_EDGE('',*,*,#11164,.T.);
#16182=ORIENTED_EDGE('',*,*,#11149,.T.);
#16183=ORIENTED_EDGE('',*,*,#11146,.T.);
#16184=ORIENTED_EDGE('',*,*,#11143,.T.);
#16185=ORIENTED_EDGE('',*,*,#11140,.T.);
#16186=ORIENTED_EDGE('',*,*,#11137,.T.);
#16187=ORIENTED_EDGE('',*,*,#11134,.T.);
#16188=ORIENTED_EDGE('',*,*,#11303,.F.);
#16189=ORIENTED_EDGE('',*,*,#11306,.F.);
#16190=ORIENTED_EDGE('',*,*,#11309,.F.);
#16191=ORIENTED_EDGE('',*,*,#11312,.F.);
#16192=ORIENTED_EDGE('',*,*,#11315,.F.);
#16193=ORIENTED_EDGE('',*,*,#11318,.F.);
#16194=ORIENTED_EDGE('',*,*,#11320,.F.);
#16195=ORIENTED_EDGE('',*,*,#11299,.T.);
#16196=ORIENTED_EDGE('',*,*,#11284,.T.);
#16197=ORIENTED_EDGE('',*,*,#11281,.T.);
#16198=ORIENTED_EDGE('',*,*,#11278,.T.);
#16199=ORIENTED_EDGE('',*,*,#11275,.T.);
#16200=ORIENTED_EDGE('',*,*,#11272,.T.);
#16201=ORIENTED_EDGE('',*,*,#11269,.T.);
#16202=ORIENTED_EDGE('',*,*,#11425,.F.);
#16203=ORIENTED_EDGE('',*,*,#11422,.F.);
#16204=ORIENTED_EDGE('',*,*,#11419,.F.);
#16205=ORIENTED_EDGE('',*,*,#11416,.F.);
#16206=ORIENTED_EDGE('',*,*,#11413,.F.);
#16207=ORIENTED_EDGE('',*,*,#11410,.F.);
#16208=ORIENTED_EDGE('',*,*,#11407,.F.);
#16209=ORIENTED_EDGE('',*,*,#11451,.F.);
#16210=ORIENTED_EDGE('',*,*,#11454,.F.);
#16211=ORIENTED_EDGE('',*,*,#11457,.F.);
#16212=ORIENTED_EDGE('',*,*,#11460,.F.);
#16213=ORIENTED_EDGE('',*,*,#11463,.F.);
#16214=ORIENTED_EDGE('',*,*,#11466,.F.);
#16215=ORIENTED_EDGE('',*,*,#11469,.F.);
#16216=ORIENTED_EDGE('',*,*,#11472,.F.);
#16217=ORIENTED_EDGE('',*,*,#11475,.F.);
#16218=ORIENTED_EDGE('',*,*,#11478,.F.);
#16219=ORIENTED_EDGE('',*,*,#11481,.F.);
#16220=ORIENTED_EDGE('',*,*,#11484,.F.);
#16221=ORIENTED_EDGE('',*,*,#11487,.F.);
#16222=ORIENTED_EDGE('',*,*,#11490,.F.);
#16223=ORIENTED_EDGE('',*,*,#11493,.F.);
#16224=ORIENTED_EDGE('',*,*,#11496,.F.);
#16225=ORIENTED_EDGE('',*,*,#11570,.F.);
#16226=ORIENTED_EDGE('',*,*,#11608,.T.);
#16227=ORIENTED_EDGE('',*,*,#11606,.T.);
#16228=ORIENTED_EDGE('',*,*,#11604,.T.);
#16229=ORIENTED_EDGE('',*,*,#11602,.T.);
#16230=ORIENTED_EDGE('',*,*,#11600,.T.);
#16231=ORIENTED_EDGE('',*,*,#11598,.T.);
#16232=ORIENTED_EDGE('',*,*,#11596,.T.);
#16233=ORIENTED_EDGE('',*,*,#11594,.T.);
#16234=ORIENTED_EDGE('',*,*,#11592,.T.);
#16235=ORIENTED_EDGE('',*,*,#11590,.T.);
#16236=ORIENTED_EDGE('',*,*,#11588,.T.);
#16237=ORIENTED_EDGE('',*,*,#11586,.T.);
#16238=ORIENTED_EDGE('',*,*,#11584,.T.);
#16239=ORIENTED_EDGE('',*,*,#11582,.T.);
#16240=ORIENTED_EDGE('',*,*,#11580,.T.);
#16241=ORIENTED_EDGE('',*,*,#11578,.T.);
#16242=ORIENTED_EDGE('',*,*,#11545,.T.);
#16243=ORIENTED_EDGE('',*,*,#11548,.T.);
#16244=ORIENTED_EDGE('',*,*,#11550,.T.);
#16245=ORIENTED_EDGE('',*,*,#11552,.T.);
#16246=ORIENTED_EDGE('',*,*,#11554,.T.);
#16247=ORIENTED_EDGE('',*,*,#11556,.T.);
#16248=ORIENTED_EDGE('',*,*,#11557,.T.);
#16249=ORIENTED_EDGE('',*,*,#11335,.F.);
#16250=ORIENTED_EDGE('',*,*,#11339,.F.);
#16251=ORIENTED_EDGE('',*,*,#11342,.F.);
#16252=ORIENTED_EDGE('',*,*,#11345,.F.);
#16253=ORIENTED_EDGE('',*,*,#11348,.F.);
#16254=ORIENTED_EDGE('',*,*,#11351,.F.);
#16255=ORIENTED_EDGE('',*,*,#11371,.F.);
#16256=ORIENTED_EDGE('',*,*,#11391,.T.);
#16257=ORIENTED_EDGE('',*,*,#11388,.T.);
#16258=ORIENTED_EDGE('',*,*,#11385,.T.);
#16259=ORIENTED_EDGE('',*,*,#11382,.T.);
#16260=ORIENTED_EDGE('',*,*,#11379,.T.);
#16261=ORIENTED_EDGE('',*,*,#11376,.T.);
#16262=ORIENTED_EDGE('',*,*,#11373,.T.);
#16263=ORIENTED_EDGE('',*,*,#11200,.F.);
#16264=ORIENTED_EDGE('',*,*,#11204,.F.);
#16265=ORIENTED_EDGE('',*,*,#11207,.F.);
#16266=ORIENTED_EDGE('',*,*,#11210,.F.);
#16267=ORIENTED_EDGE('',*,*,#11213,.F.);
#16268=ORIENTED_EDGE('',*,*,#11216,.F.);
#16269=ORIENTED_EDGE('',*,*,#11236,.F.);
#16270=ORIENTED_EDGE('',*,*,#11256,.T.);
#16271=ORIENTED_EDGE('',*,*,#11253,.T.);
#16272=ORIENTED_EDGE('',*,*,#11250,.T.);
#16273=ORIENTED_EDGE('',*,*,#11247,.T.);
#16274=ORIENTED_EDGE('',*,*,#11244,.T.);
#16275=ORIENTED_EDGE('',*,*,#11241,.T.);
#16276=ORIENTED_EDGE('',*,*,#11238,.T.);
#16277=ORIENTED_EDGE('',*,*,#10852,.F.);
#16278=ORIENTED_EDGE('',*,*,#10856,.F.);
#16279=ORIENTED_EDGE('',*,*,#10859,.F.);
#16280=ORIENTED_EDGE('',*,*,#10862,.F.);
#16281=ORIENTED_EDGE('',*,*,#10865,.F.);
#16282=ORIENTED_EDGE('',*,*,#10868,.F.);
#16283=ORIENTED_EDGE('',*,*,#10886,.F.);
#16284=ORIENTED_EDGE('',*,*,#10904,.T.);
#16285=ORIENTED_EDGE('',*,*,#10901,.T.);
#16286=ORIENTED_EDGE('',*,*,#10898,.T.);
#16287=ORIENTED_EDGE('',*,*,#10895,.T.);
#16288=ORIENTED_EDGE('',*,*,#10892,.T.);
#16289=ORIENTED_EDGE('',*,*,#10889,.T.);
#16290=ORIENTED_EDGE('',*,*,#10938,.F.);
#16291=ORIENTED_EDGE('',*,*,#10935,.F.);
#16292=ORIENTED_EDGE('',*,*,#10932,.F.);
#16293=ORIENTED_EDGE('',*,*,#10929,.F.);
#16294=ORIENTED_EDGE('',*,*,#10926,.F.);
#16295=ORIENTED_EDGE('',*,*,#10923,.F.);
#16296=ORIENTED_EDGE('',*,*,#10920,.F.);
#16297=ORIENTED_EDGE('',*,*,#10964,.F.);
#16298=ORIENTED_EDGE('',*,*,#10967,.F.);
#16299=ORIENTED_EDGE('',*,*,#10970,.F.);
#16300=ORIENTED_EDGE('',*,*,#10973,.F.);
#16301=ORIENTED_EDGE('',*,*,#10976,.F.);
#16302=ORIENTED_EDGE('',*,*,#10979,.F.);
#16303=ORIENTED_EDGE('',*,*,#10982,.F.);
#16304=ORIENTED_EDGE('',*,*,#10985,.F.);
#16305=ORIENTED_EDGE('',*,*,#10988,.F.);
#16306=ORIENTED_EDGE('',*,*,#10991,.F.);
#16307=ORIENTED_EDGE('',*,*,#10994,.F.);
#16308=ORIENTED_EDGE('',*,*,#10997,.F.);
#16309=ORIENTED_EDGE('',*,*,#11000,.F.);
#16310=ORIENTED_EDGE('',*,*,#11003,.F.);
#16311=ORIENTED_EDGE('',*,*,#11006,.F.);
#16312=ORIENTED_EDGE('',*,*,#11009,.F.);
#16313=ORIENTED_EDGE('',*,*,#11063,.F.);
#16314=ORIENTED_EDGE('',*,*,#11121,.T.);
#16315=ORIENTED_EDGE('',*,*,#11118,.T.);
#16316=ORIENTED_EDGE('',*,*,#11115,.T.);
#16317=ORIENTED_EDGE('',*,*,#11112,.T.);
#16318=ORIENTED_EDGE('',*,*,#11109,.T.);
#16319=ORIENTED_EDGE('',*,*,#11106,.T.);
#16320=ORIENTED_EDGE('',*,*,#11103,.T.);
#16321=ORIENTED_EDGE('',*,*,#11100,.T.);
#16322=ORIENTED_EDGE('',*,*,#11097,.T.);
#16323=ORIENTED_EDGE('',*,*,#11094,.T.);
#16324=ORIENTED_EDGE('',*,*,#11091,.T.);
#16325=ORIENTED_EDGE('',*,*,#11088,.T.);
#16326=ORIENTED_EDGE('',*,*,#11085,.T.);
#16327=ORIENTED_EDGE('',*,*,#11082,.T.);
#16328=ORIENTED_EDGE('',*,*,#11079,.T.);
#16329=ORIENTED_EDGE('',*,*,#11076,.T.);
#16330=ORIENTED_EDGE('',*,*,#11025,.T.);
#16331=ORIENTED_EDGE('',*,*,#11029,.T.);
#16332=ORIENTED_EDGE('',*,*,#11032,.T.);
#16333=ORIENTED_EDGE('',*,*,#11035,.T.);
#16334=ORIENTED_EDGE('',*,*,#11038,.T.);
#16335=ORIENTED_EDGE('',*,*,#11041,.T.);
#16336=ORIENTED_EDGE('',*,*,#11043,.T.);
#16337=ORIENTED_EDGE('',*,*,#10822,.F.);
#16338=ORIENTED_EDGE('',*,*,#10826,.F.);
#16339=ORIENTED_EDGE('',*,*,#10829,.F.);
#16340=ORIENTED_EDGE('',*,*,#10832,.F.);
#16341=ORIENTED_EDGE('',*,*,#10835,.F.);
#16342=ORIENTED_EDGE('',*,*,#10837,.F.);
#16343=ORIENTED_EDGE('',*,*,#10818,.T.);
#16344=ORIENTED_EDGE('',*,*,#10805,.T.);
#16345=ORIENTED_EDGE('',*,*,#10802,.T.);
#16346=ORIENTED_EDGE('',*,*,#10799,.T.);
#16347=ORIENTED_EDGE('',*,*,#10796,.T.);
#16348=ORIENTED_EDGE('',*,*,#10793,.T.);
#16349=ORIENTED_EDGE('',*,*,#10790,.T.);
#16350=ORIENTED_EDGE('',*,*,#11022,.T.);
#16351=ORIENTED_EDGE('',*,*,#11074,.T.);
#16352=ORIENTED_EDGE('',*,*,#11071,.T.);
#16353=ORIENTED_EDGE('',*,*,#11068,.T.);
#16354=ORIENTED_EDGE('',*,*,#11065,.T.);
#16355=ORIENTED_EDGE('',*,*,#11012,.T.);
#16356=ORIENTED_EDGE('',*,*,#11016,.T.);
#16357=ORIENTED_EDGE('',*,*,#11019,.T.);
#16358=ORIENTED_EDGE('',*,*,#10916,.F.);
#16359=ORIENTED_EDGE('',*,*,#10913,.F.);
#16360=ORIENTED_EDGE('',*,*,#10910,.F.);
#16361=ORIENTED_EDGE('',*,*,#10907,.F.);
#16362=ORIENTED_EDGE('',*,*,#10953,.F.);
#16363=ORIENTED_EDGE('',*,*,#10956,.F.);
#16364=ORIENTED_EDGE('',*,*,#10959,.F.);
#16365=ORIENTED_EDGE('',*,*,#10961,.F.);
#16366=ORIENTED_EDGE('',*,*,#11058,.T.);
#16367=ORIENTED_EDGE('',*,*,#10881,.F.);
#16368=ORIENTED_EDGE('',*,*,#11046,.F.);
#16369=ORIENTED_EDGE('',*,*,#11049,.T.);
#16370=ORIENTED_EDGE('',*,*,#11052,.T.);
#16371=ORIENTED_EDGE('',*,*,#11055,.T.);
#16372=ORIENTED_EDGE('',*,*,#11057,.T.);
#16373=ORIENTED_EDGE('',*,*,#10949,.F.);
#16374=ORIENTED_EDGE('',*,*,#10946,.F.);
#16375=ORIENTED_EDGE('',*,*,#10943,.F.);
#16376=ORIENTED_EDGE('',*,*,#10940,.T.);
#16377=ORIENTED_EDGE('',*,*,#10871,.T.);
#16378=ORIENTED_EDGE('',*,*,#10875,.T.);
#16379=ORIENTED_EDGE('',*,*,#10878,.T.);
#16380=ORIENTED_EDGE('',*,*,#10880,.T.);
#16381=ORIENTED_EDGE('',*,*,#10815,.F.);
#16382=ORIENTED_EDGE('',*,*,#10812,.F.);
#16383=ORIENTED_EDGE('',*,*,#10809,.F.);
#16384=ORIENTED_EDGE('',*,*,#11152,.F.);
#16385=ORIENTED_EDGE('',*,*,#10780,.T.);
#16386=ORIENTED_EDGE('',*,*,#10784,.T.);
#16387=ORIENTED_EDGE('',*,*,#10787,.T.);
#16388=ORIENTED_EDGE('',*,*,#10849,.F.);
#16389=ORIENTED_EDGE('',*,*,#10846,.F.);
#16390=ORIENTED_EDGE('',*,*,#10843,.F.);
#16391=ORIENTED_EDGE('',*,*,#10840,.F.);
#16392=ORIENTED_EDGE('',*,*,#11219,.F.);
#16393=ORIENTED_EDGE('',*,*,#11222,.T.);
#16394=ORIENTED_EDGE('',*,*,#11225,.T.);
#16395=ORIENTED_EDGE('',*,*,#11228,.T.);
#16396=ORIENTED_EDGE('',*,*,#11230,.T.);
#16397=ORIENTED_EDGE('',*,*,#11161,.F.);
#16398=ORIENTED_EDGE('',*,*,#11158,.F.);
#16399=ORIENTED_EDGE('',*,*,#11155,.F.);
#16400=ORIENTED_EDGE('',*,*,#11231,.F.);
#16401=ORIENTED_EDGE('',*,*,#11287,.F.);
#16402=ORIENTED_EDGE('',*,*,#11124,.T.);
#16403=ORIENTED_EDGE('',*,*,#11128,.T.);
#16404=ORIENTED_EDGE('',*,*,#11131,.T.);
#16405=ORIENTED_EDGE('',*,*,#11197,.F.);
#16406=ORIENTED_EDGE('',*,*,#11194,.F.);
#16407=ORIENTED_EDGE('',*,*,#11191,.F.);
#16408=ORIENTED_EDGE('',*,*,#11188,.F.);
#16409=ORIENTED_EDGE('',*,*,#11354,.F.);
#16410=ORIENTED_EDGE('',*,*,#11357,.T.);
#16411=ORIENTED_EDGE('',*,*,#11360,.T.);
#16412=ORIENTED_EDGE('',*,*,#11363,.T.);
#16413=ORIENTED_EDGE('',*,*,#11365,.T.);
#16414=ORIENTED_EDGE('',*,*,#11296,.F.);
#16415=ORIENTED_EDGE('',*,*,#11293,.F.);
#16416=ORIENTED_EDGE('',*,*,#11290,.F.);
#16417=ORIENTED_EDGE('',*,*,#11366,.F.);
#16418=ORIENTED_EDGE('',*,*,#11567,.T.);
#16419=ORIENTED_EDGE('',*,*,#11403,.F.);
#16420=ORIENTED_EDGE('',*,*,#11400,.F.);
#16421=ORIENTED_EDGE('',*,*,#11397,.F.);
#16422=ORIENTED_EDGE('',*,*,#11394,.F.);
#16423=ORIENTED_EDGE('',*,*,#11440,.F.);
#16424=ORIENTED_EDGE('',*,*,#11443,.F.);
#16425=ORIENTED_EDGE('',*,*,#11446,.F.);
#16426=ORIENTED_EDGE('',*,*,#11448,.F.);
#16427=ORIENTED_EDGE('',*,*,#11543,.T.);
#16428=ORIENTED_EDGE('',*,*,#11577,.T.);
#16429=ORIENTED_EDGE('',*,*,#11575,.T.);
#16430=ORIENTED_EDGE('',*,*,#11573,.T.);
#16431=ORIENTED_EDGE('',*,*,#11571,.T.);
#16432=ORIENTED_EDGE('',*,*,#11536,.T.);
#16433=ORIENTED_EDGE('',*,*,#11539,.T.);
#16434=ORIENTED_EDGE('',*,*,#11541,.T.);
#16435=ORIENTED_EDGE('',*,*,#11427,.T.);
#16436=ORIENTED_EDGE('',*,*,#11259,.T.);
#16437=ORIENTED_EDGE('',*,*,#11263,.T.);
#16438=ORIENTED_EDGE('',*,*,#11266,.T.);
#16439=ORIENTED_EDGE('',*,*,#11332,.F.);
#16440=ORIENTED_EDGE('',*,*,#11329,.F.);
#16441=ORIENTED_EDGE('',*,*,#11326,.F.);
#16442=ORIENTED_EDGE('',*,*,#11323,.F.);
#16443=ORIENTED_EDGE('',*,*,#11559,.F.);
#16444=ORIENTED_EDGE('',*,*,#11561,.T.);
#16445=ORIENTED_EDGE('',*,*,#11563,.T.);
#16446=ORIENTED_EDGE('',*,*,#11565,.T.);
#16447=ORIENTED_EDGE('',*,*,#11566,.T.);
#16448=ORIENTED_EDGE('',*,*,#11436,.F.);
#16449=ORIENTED_EDGE('',*,*,#11433,.F.);
#16450=ORIENTED_EDGE('',*,*,#11430,.F.);
#18735=PLANE('',#21081);
#18736=PLANE('',#21082);
#18737=PLANE('',#21083);
#18738=PLANE('',#21084);
#18739=PLANE('',#21085);
#18740=PLANE('',#21086);
#18741=PLANE('',#21087);
#18742=PLANE('',#21088);
#18743=PLANE('',#21089);
#18744=PLANE('',#21090);
#18745=PLANE('',#21091);
#18746=PLANE('',#21092);
#18747=PLANE('',#21093);
#18748=PLANE('',#21094);
#18749=PLANE('',#21095);
#18750=PLANE('',#21096);
#18751=PLANE('',#21097);
#18752=PLANE('',#21098);
#18753=PLANE('',#21099);
#18754=PLANE('',#21100);
#18755=PLANE('',#21101);
#18756=PLANE('',#21102);
#18757=PLANE('',#21103);
#18758=PLANE('',#21104);
#18759=PLANE('',#21105);
#18760=PLANE('',#21106);
#18761=PLANE('',#21107);
#18762=PLANE('',#21108);
#18763=PLANE('',#21109);
#18764=PLANE('',#21110);
#18765=PLANE('',#21111);
#18766=PLANE('',#21112);
#18767=PLANE('',#21113);
#18768=PLANE('',#21117);
#18769=PLANE('',#21118);
#18770=PLANE('',#21119);
#18771=PLANE('',#21120);
#18772=PLANE('',#21121);
#18773=PLANE('',#21122);
#18774=PLANE('',#21123);
#18775=PLANE('',#21124);
#18776=PLANE('',#21128);
#18777=PLANE('',#21132);
#18778=PLANE('',#21133);
#18779=PLANE('',#21134);
#18780=PLANE('',#21135);
#18781=PLANE('',#21136);
#18782=PLANE('',#21137);
#18783=PLANE('',#21138);
#18784=PLANE('',#21139);
#18785=PLANE('',#21140);
#18786=PLANE('',#21141);
#18787=PLANE('',#21142);
#18788=PLANE('',#21146);
#18789=PLANE('',#21150);
#18790=PLANE('',#21151);
#18791=PLANE('',#21152);
#18792=PLANE('',#21153);
#18793=PLANE('',#21154);
#18794=PLANE('',#21155);
#18795=PLANE('',#21156);
#18796=PLANE('',#21157);
#18797=PLANE('',#21158);
#18798=PLANE('',#21162);
#18799=PLANE('',#21163);
#18800=PLANE('',#21164);
#18801=PLANE('',#21165);
#18802=PLANE('',#21166);
#18803=PLANE('',#21167);
#18804=PLANE('',#21168);
#18805=PLANE('',#21169);
#18806=PLANE('',#21173);
#18807=PLANE('',#21177);
#18808=PLANE('',#21178);
#18809=PLANE('',#21179);
#18810=PLANE('',#21180);
#18811=PLANE('',#21181);
#18812=PLANE('',#21182);
#18813=PLANE('',#21183);
#18814=PLANE('',#21184);
#18815=PLANE('',#21185);
#18816=PLANE('',#21186);
#18817=PLANE('',#21187);
#18818=PLANE('',#21188);
#18819=PLANE('',#21192);
#18820=PLANE('',#21196);
#18821=PLANE('',#21200);
#18822=PLANE('',#21201);
#18823=PLANE('',#21202);
#18824=PLANE('',#21203);
#18825=PLANE('',#21204);
#18826=PLANE('',#21205);
#18827=PLANE('',#21206);
#18828=PLANE('',#21207);
#18829=PLANE('',#21208);
#18830=PLANE('',#21212);
#18831=PLANE('',#21213);
#18832=PLANE('',#21214);
#18833=PLANE('',#21215);
#18834=PLANE('',#21216);
#18835=PLANE('',#21217);
#18836=PLANE('',#21218);
#18837=PLANE('',#21219);
#18838=PLANE('',#21220);
#18839=PLANE('',#21221);
#18840=PLANE('',#21222);
#18841=PLANE('',#21223);
#18842=PLANE('',#21224);
#18843=PLANE('',#21225);
#18844=PLANE('',#21226);
#18845=PLANE('',#21227);
#18846=PLANE('',#21228);
#18847=PLANE('',#21229);
#18848=PLANE('',#21230);
#18849=PLANE('',#21231);
#18850=PLANE('',#21232);
#18851=PLANE('',#21233);
#18852=PLANE('',#21234);
#18853=PLANE('',#21235);
#18854=PLANE('',#21236);
#18855=PLANE('',#21237);
#18856=PLANE('',#21238);
#18857=PLANE('',#21239);
#18858=PLANE('',#21240);
#18859=PLANE('',#21241);
#18860=PLANE('',#21242);
#18861=PLANE('',#21243);
#18862=PLANE('',#21244);
#18863=PLANE('',#21245);
#18864=PLANE('',#21246);
#18865=PLANE('',#21247);
#18866=PLANE('',#21248);
#18867=PLANE('',#21249);
#18868=PLANE('',#21250);
#18869=PLANE('',#21251);
#18870=PLANE('',#21252);
#18871=PLANE('',#21253);
#18872=PLANE('',#21254);
#18873=PLANE('',#21258);
#18874=PLANE('',#21259);
#18875=PLANE('',#21260);
#18876=PLANE('',#21261);
#18877=PLANE('',#21262);
#18878=PLANE('',#21263);
#18879=PLANE('',#21264);
#18880=PLANE('',#21265);
#18881=PLANE('',#21266);
#18882=PLANE('',#21267);
#18883=PLANE('',#21268);
#18884=PLANE('',#21269);
#18885=PLANE('',#21270);
#18886=PLANE('',#21271);
#18887=PLANE('',#21272);
#18888=PLANE('',#21273);
#18889=PLANE('',#21274);
#18890=PLANE('',#21275);
#18891=PLANE('',#21276);
#18892=PLANE('',#21277);
#18893=PLANE('',#21278);
#18894=PLANE('',#21279);
#18895=PLANE('',#21280);
#18896=PLANE('',#21281);
#18897=PLANE('',#21282);
#18898=PLANE('',#21283);
#18899=PLANE('',#21284);
#18900=PLANE('',#21285);
#18901=PLANE('',#21286);
#18902=PLANE('',#21287);
#18903=PLANE('',#21288);
#18904=PLANE('',#21289);
#18905=PLANE('',#21290);
#18906=PLANE('',#21291);
#18907=PLANE('',#21292);
#18908=PLANE('',#21293);
#18909=PLANE('',#21294);
#18910=PLANE('',#21295);
#18911=PLANE('',#21296);
#18912=PLANE('',#21297);
#18913=PLANE('',#21298);
#18914=PLANE('',#21299);
#18915=PLANE('',#21300);
#18916=PLANE('',#21301);
#18917=PLANE('',#21305);
#18918=PLANE('',#21306);
#18919=PLANE('',#21307);
#18920=PLANE('',#21308);
#18921=PLANE('',#21309);
#18922=PLANE('',#21310);
#18923=PLANE('',#21311);
#18924=PLANE('',#21312);
#18925=PLANE('',#21313);
#18926=PLANE('',#21317);
#18927=PLANE('',#21321);
#18928=PLANE('',#21322);
#18929=PLANE('',#21323);
#18930=PLANE('',#21324);
#18931=PLANE('',#21325);
#18932=PLANE('',#21326);
#18933=PLANE('',#21327);
#18934=PLANE('',#21328);
#18935=PLANE('',#21329);
#18936=PLANE('',#21330);
#18937=PLANE('',#21331);
#18938=PLANE('',#21335);
#18939=PLANE('',#21339);
#18940=PLANE('',#21340);
#18941=PLANE('',#21341);
#18942=PLANE('',#21342);
#18943=PLANE('',#21343);
#18944=PLANE('',#21344);
#18945=PLANE('',#21345);
#18946=PLANE('',#21346);
#18947=PLANE('',#21347);
#18948=PLANE('',#21351);
#18949=PLANE('',#21352);
#18950=PLANE('',#21353);
#18951=PLANE('',#21354);
#18952=PLANE('',#21355);
#18953=PLANE('',#21356);
#18954=PLANE('',#21357);
#18955=PLANE('',#21358);
#18956=PLANE('',#21365);
#18957=PLANE('',#21368);
#18958=PLANE('',#21371);
#18959=PLANE('',#21372);
#18960=PLANE('',#21373);
#18961=PLANE('',#21374);
#18962=PLANE('',#21375);
#18963=PLANE('',#21376);
#18964=PLANE('',#21377);
#18965=PLANE('',#21378);
#18966=PLANE('',#21379);
#18967=PLANE('',#21380);
#18968=PLANE('',#21381);
#18969=PLANE('',#21382);
#18970=PLANE('',#21385);
#18971=PLANE('',#21388);
#18972=PLANE('',#21391);
#18973=PLANE('',#21392);
#18974=PLANE('',#21393);
#18975=PLANE('',#21394);
#18976=PLANE('',#21395);
#18977=PLANE('',#21396);
#18978=PLANE('',#21397);
#18979=PLANE('',#21398);
#18980=PLANE('',#21399);
#18981=PLANE('',#21402);
#18982=PLANE('',#21403);
#18983=PLANE('',#21404);
#18984=PLANE('',#21405);
#18985=PLANE('',#21406);
#18986=PLANE('',#21407);
#18987=PLANE('',#21408);
#18988=PLANE('',#21409);
#19463=ADVANCED_FACE('',(#1606),#18735,.T.);
#19464=ADVANCED_FACE('',(#1607),#18736,.T.);
#19465=ADVANCED_FACE('',(#1608),#18737,.T.);
#19466=ADVANCED_FACE('',(#1609),#18738,.T.);
#19467=ADVANCED_FACE('',(#1610),#18739,.T.);
#19468=ADVANCED_FACE('',(#1611),#18740,.T.);
#19469=ADVANCED_FACE('',(#1612),#18741,.T.);
#19470=ADVANCED_FACE('',(#1613),#18742,.T.);
#19471=ADVANCED_FACE('',(#1614),#18743,.T.);
#19472=ADVANCED_FACE('',(#1615),#18744,.F.);
#19473=ADVANCED_FACE('',(#1616),#18745,.F.);
#19474=ADVANCED_FACE('',(#1617),#18746,.F.);
#19475=ADVANCED_FACE('',(#1618),#18747,.F.);
#19476=ADVANCED_FACE('',(#1619),#18748,.F.);
#19477=ADVANCED_FACE('',(#1620),#18749,.F.);
#19478=ADVANCED_FACE('',(#1621),#18750,.F.);
#19479=ADVANCED_FACE('',(#1622),#18751,.F.);
#19480=ADVANCED_FACE('',(#1623),#18752,.F.);
#19481=ADVANCED_FACE('',(#1624),#18753,.F.);
#19482=ADVANCED_FACE('',(#1625),#18754,.F.);
#19483=ADVANCED_FACE('',(#1626),#18755,.F.);
#19484=ADVANCED_FACE('',(#1627),#18756,.F.);
#19485=ADVANCED_FACE('',(#1628),#18757,.F.);
#19486=ADVANCED_FACE('',(#1629),#18758,.F.);
#19487=ADVANCED_FACE('',(#1630),#18759,.F.);
#19488=ADVANCED_FACE('',(#1631),#18760,.F.);
#19489=ADVANCED_FACE('',(#1632),#18761,.F.);
#19490=ADVANCED_FACE('',(#1633),#18762,.F.);
#19491=ADVANCED_FACE('',(#1634),#18763,.F.);
#19492=ADVANCED_FACE('',(#1635),#18764,.T.);
#19493=ADVANCED_FACE('',(#1636),#18765,.T.);
#19494=ADVANCED_FACE('',(#1637),#18766,.T.);
#19495=ADVANCED_FACE('',(#1638),#18767,.T.);
#19496=ADVANCED_FACE('',(#1639),#897,.F.);
#19497=ADVANCED_FACE('',(#1640),#18768,.T.);
#19498=ADVANCED_FACE('',(#1641),#18769,.T.);
#19499=ADVANCED_FACE('',(#1642),#18770,.T.);
#19500=ADVANCED_FACE('',(#1643),#18771,.T.);
#19501=ADVANCED_FACE('',(#1644),#18772,.T.);
#19502=ADVANCED_FACE('',(#1645),#18773,.T.);
#19503=ADVANCED_FACE('',(#1646),#18774,.T.);
#19504=ADVANCED_FACE('',(#1647),#18775,.F.);
#19505=ADVANCED_FACE('',(#1648),#898,.F.);
#19506=ADVANCED_FACE('',(#1649),#18776,.F.);
#19507=ADVANCED_FACE('',(#1650),#899,.F.);
#19508=ADVANCED_FACE('',(#1651),#18777,.F.);
#19509=ADVANCED_FACE('',(#1652),#18778,.F.);
#19510=ADVANCED_FACE('',(#1653),#18779,.F.);
#19511=ADVANCED_FACE('',(#1654),#18780,.F.);
#19512=ADVANCED_FACE('',(#1655),#18781,.F.);
#19513=ADVANCED_FACE('',(#1656),#18782,.F.);
#19514=ADVANCED_FACE('',(#1657),#18783,.F.);
#19515=ADVANCED_FACE('',(#1658),#18784,.F.);
#19516=ADVANCED_FACE('',(#1659),#18785,.F.);
#19517=ADVANCED_FACE('',(#1660),#18786,.F.);
#19518=ADVANCED_FACE('',(#1661),#18787,.F.);
#19519=ADVANCED_FACE('',(#1662),#900,.F.);
#19520=ADVANCED_FACE('',(#1663),#18788,.F.);
#19521=ADVANCED_FACE('',(#1664),#901,.F.);
#19522=ADVANCED_FACE('',(#1665),#18789,.F.);
#19523=ADVANCED_FACE('',(#1666),#18790,.F.);
#19524=ADVANCED_FACE('',(#1667),#18791,.F.);
#19525=ADVANCED_FACE('',(#1668),#18792,.F.);
#19526=ADVANCED_FACE('',(#1669),#18793,.F.);
#19527=ADVANCED_FACE('',(#1670),#18794,.F.);
#19528=ADVANCED_FACE('',(#1671),#18795,.F.);
#19529=ADVANCED_FACE('',(#1672),#18796,.F.);
#19530=ADVANCED_FACE('',(#1673),#18797,.F.);
#19531=ADVANCED_FACE('',(#1674),#902,.T.);
#19532=ADVANCED_FACE('',(#1675),#18798,.F.);
#19533=ADVANCED_FACE('',(#1676),#18799,.F.);
#19534=ADVANCED_FACE('',(#1677),#18800,.F.);
#19535=ADVANCED_FACE('',(#1678),#18801,.F.);
#19536=ADVANCED_FACE('',(#1679),#18802,.F.);
#19537=ADVANCED_FACE('',(#1680),#18803,.F.);
#19538=ADVANCED_FACE('',(#1681),#18804,.F.);
#19539=ADVANCED_FACE('',(#1682),#18805,.T.);
#19540=ADVANCED_FACE('',(#1683),#903,.F.);
#19541=ADVANCED_FACE('',(#1684),#18806,.T.);
#19542=ADVANCED_FACE('',(#1685),#904,.F.);
#19543=ADVANCED_FACE('',(#1686),#18807,.T.);
#19544=ADVANCED_FACE('',(#1687),#18808,.T.);
#19545=ADVANCED_FACE('',(#1688),#18809,.T.);
#19546=ADVANCED_FACE('',(#1689),#18810,.T.);
#19547=ADVANCED_FACE('',(#1690),#18811,.T.);
#19548=ADVANCED_FACE('',(#1691),#18812,.T.);
#19549=ADVANCED_FACE('',(#1692),#18813,.T.);
#19550=ADVANCED_FACE('',(#1693),#18814,.T.);
#19551=ADVANCED_FACE('',(#1694),#18815,.T.);
#19552=ADVANCED_FACE('',(#1695),#18816,.T.);
#19553=ADVANCED_FACE('',(#1696),#18817,.T.);
#19554=ADVANCED_FACE('',(#1697),#18818,.T.);
#19555=ADVANCED_FACE('',(#1698),#905,.F.);
#19556=ADVANCED_FACE('',(#1699),#18819,.T.);
#19557=ADVANCED_FACE('',(#1700),#906,.F.);
#19558=ADVANCED_FACE('',(#1701),#18820,.T.);
#19559=ADVANCED_FACE('',(#1702),#907,.F.);
#19560=ADVANCED_FACE('',(#1703),#18821,.T.);
#19561=ADVANCED_FACE('',(#1704),#18822,.T.);
#19562=ADVANCED_FACE('',(#1705),#18823,.T.);
#19563=ADVANCED_FACE('',(#1706),#18824,.T.);
#19564=ADVANCED_FACE('',(#1707),#18825,.T.);
#19565=ADVANCED_FACE('',(#1708),#18826,.T.);
#19566=ADVANCED_FACE('',(#1709),#18827,.T.);
#19567=ADVANCED_FACE('',(#1710),#18828,.T.);
#19568=ADVANCED_FACE('',(#1711),#18829,.T.);
#19569=ADVANCED_FACE('',(#1712),#908,.T.);
#19570=ADVANCED_FACE('',(#1713),#18830,.T.);
#19571=ADVANCED_FACE('',(#1714),#18831,.T.);
#19572=ADVANCED_FACE('',(#1715),#18832,.T.);
#19573=ADVANCED_FACE('',(#1716),#18833,.T.);
#19574=ADVANCED_FACE('',(#1717),#18834,.T.);
#19575=ADVANCED_FACE('',(#1718),#18835,.T.);
#19576=ADVANCED_FACE('',(#1719),#18836,.T.);
#19577=ADVANCED_FACE('',(#1720),#18837,.T.);
#19578=ADVANCED_FACE('',(#1721),#18838,.T.);
#19579=ADVANCED_FACE('',(#1722),#18839,.T.);
#19580=ADVANCED_FACE('',(#1723),#18840,.T.);
#19581=ADVANCED_FACE('',(#1724),#18841,.T.);
#19582=ADVANCED_FACE('',(#1725),#18842,.T.);
#19583=ADVANCED_FACE('',(#1726),#18843,.T.);
#19584=ADVANCED_FACE('',(#1727),#18844,.T.);
#19585=ADVANCED_FACE('',(#1728),#18845,.T.);
#19586=ADVANCED_FACE('',(#1729),#18846,.F.);
#19587=ADVANCED_FACE('',(#1730),#18847,.F.);
#19588=ADVANCED_FACE('',(#1731),#18848,.F.);
#19589=ADVANCED_FACE('',(#1732),#18849,.F.);
#19590=ADVANCED_FACE('',(#1733),#18850,.F.);
#19591=ADVANCED_FACE('',(#1734),#18851,.F.);
#19592=ADVANCED_FACE('',(#1735),#18852,.F.);
#19593=ADVANCED_FACE('',(#1736),#18853,.F.);
#19594=ADVANCED_FACE('',(#1737),#18854,.F.);
#19595=ADVANCED_FACE('',(#1738),#18855,.F.);
#19596=ADVANCED_FACE('',(#1739),#18856,.F.);
#19597=ADVANCED_FACE('',(#1740),#18857,.F.);
#19598=ADVANCED_FACE('',(#1741),#18858,.F.);
#19599=ADVANCED_FACE('',(#1742),#18859,.F.);
#19600=ADVANCED_FACE('',(#1743),#18860,.F.);
#19601=ADVANCED_FACE('',(#1744),#18861,.F.);
#19602=ADVANCED_FACE('',(#1745),#18862,.F.);
#19603=ADVANCED_FACE('',(#1746),#18863,.F.);
#19604=ADVANCED_FACE('',(#1747),#18864,.F.);
#19605=ADVANCED_FACE('',(#1748),#18865,.F.);
#19606=ADVANCED_FACE('',(#1749),#18866,.F.);
#19607=ADVANCED_FACE('',(#1750),#18867,.F.);
#19608=ADVANCED_FACE('',(#1751),#18868,.T.);
#19609=ADVANCED_FACE('',(#1752),#18869,.T.);
#19610=ADVANCED_FACE('',(#1753),#18870,.T.);
#19611=ADVANCED_FACE('',(#1754),#18871,.T.);
#19612=ADVANCED_FACE('',(#1755),#18872,.T.);
#19613=ADVANCED_FACE('',(#1756),#909,.F.);
#19614=ADVANCED_FACE('',(#1757),#18873,.T.);
#19615=ADVANCED_FACE('',(#1758),#18874,.T.);
#19616=ADVANCED_FACE('',(#1759),#18875,.T.);
#19617=ADVANCED_FACE('',(#1760),#18876,.T.);
#19618=ADVANCED_FACE('',(#1761),#18877,.T.);
#19619=ADVANCED_FACE('',(#1762),#18878,.T.);
#19620=ADVANCED_FACE('',(#1763),#18879,.T.);
#19621=ADVANCED_FACE('',(#1764),#18880,.T.);
#19622=ADVANCED_FACE('',(#1765),#18881,.T.);
#19623=ADVANCED_FACE('',(#1766),#18882,.T.);
#19624=ADVANCED_FACE('',(#1767),#18883,.T.);
#19625=ADVANCED_FACE('',(#1768),#18884,.T.);
#19626=ADVANCED_FACE('',(#1769),#18885,.T.);
#19627=ADVANCED_FACE('',(#1770),#18886,.T.);
#19628=ADVANCED_FACE('',(#1771),#18887,.T.);
#19629=ADVANCED_FACE('',(#1772),#18888,.T.);
#19630=ADVANCED_FACE('',(#1773),#18889,.T.);
#19631=ADVANCED_FACE('',(#1774),#18890,.F.);
#19632=ADVANCED_FACE('',(#1775),#18891,.F.);
#19633=ADVANCED_FACE('',(#1776),#18892,.F.);
#19634=ADVANCED_FACE('',(#1777),#18893,.F.);
#19635=ADVANCED_FACE('',(#1778),#18894,.F.);
#19636=ADVANCED_FACE('',(#1779),#18895,.F.);
#19637=ADVANCED_FACE('',(#1780),#18896,.F.);
#19638=ADVANCED_FACE('',(#1781),#18897,.F.);
#19639=ADVANCED_FACE('',(#1782),#18898,.F.);
#19640=ADVANCED_FACE('',(#1783),#18899,.F.);
#19641=ADVANCED_FACE('',(#1784),#18900,.F.);
#19642=ADVANCED_FACE('',(#1785),#18901,.F.);
#19643=ADVANCED_FACE('',(#1786),#18902,.F.);
#19644=ADVANCED_FACE('',(#1787),#18903,.F.);
#19645=ADVANCED_FACE('',(#1788),#18904,.F.);
#19646=ADVANCED_FACE('',(#1789),#18905,.F.);
#19647=ADVANCED_FACE('',(#1790),#18906,.F.);
#19648=ADVANCED_FACE('',(#1791),#18907,.F.);
#19649=ADVANCED_FACE('',(#1792),#18908,.F.);
#19650=ADVANCED_FACE('',(#1793),#18909,.F.);
#19651=ADVANCED_FACE('',(#1794),#18910,.F.);
#19652=ADVANCED_FACE('',(#1795),#18911,.F.);
#19653=ADVANCED_FACE('',(#1796),#18912,.T.);
#19654=ADVANCED_FACE('',(#1797),#18913,.T.);
#19655=ADVANCED_FACE('',(#1798),#18914,.T.);
#19656=ADVANCED_FACE('',(#1799),#18915,.T.);
#19657=ADVANCED_FACE('',(#1800),#18916,.T.);
#19658=ADVANCED_FACE('',(#1801),#910,.F.);
#19659=ADVANCED_FACE('',(#1802),#18917,.T.);
#19660=ADVANCED_FACE('',(#1803),#18918,.T.);
#19661=ADVANCED_FACE('',(#1804),#18919,.T.);
#19662=ADVANCED_FACE('',(#1805),#18920,.T.);
#19663=ADVANCED_FACE('',(#1806),#18921,.T.);
#19664=ADVANCED_FACE('',(#1807),#18922,.T.);
#19665=ADVANCED_FACE('',(#1808),#18923,.T.);
#19666=ADVANCED_FACE('',(#1809),#18924,.T.);
#19667=ADVANCED_FACE('',(#1810),#18925,.F.);
#19668=ADVANCED_FACE('',(#1811),#911,.F.);
#19669=ADVANCED_FACE('',(#1812),#18926,.F.);
#19670=ADVANCED_FACE('',(#1813),#912,.F.);
#19671=ADVANCED_FACE('',(#1814),#18927,.F.);
#19672=ADVANCED_FACE('',(#1815),#18928,.F.);
#19673=ADVANCED_FACE('',(#1816),#18929,.F.);
#19674=ADVANCED_FACE('',(#1817),#18930,.F.);
#19675=ADVANCED_FACE('',(#1818),#18931,.F.);
#19676=ADVANCED_FACE('',(#1819),#18932,.F.);
#19677=ADVANCED_FACE('',(#1820),#18933,.F.);
#19678=ADVANCED_FACE('',(#1821),#18934,.F.);
#19679=ADVANCED_FACE('',(#1822),#18935,.F.);
#19680=ADVANCED_FACE('',(#1823),#18936,.F.);
#19681=ADVANCED_FACE('',(#1824),#18937,.F.);
#19682=ADVANCED_FACE('',(#1825),#913,.F.);
#19683=ADVANCED_FACE('',(#1826),#18938,.F.);
#19684=ADVANCED_FACE('',(#1827),#914,.F.);
#19685=ADVANCED_FACE('',(#1828),#18939,.F.);
#19686=ADVANCED_FACE('',(#1829),#18940,.F.);
#19687=ADVANCED_FACE('',(#1830),#18941,.F.);
#19688=ADVANCED_FACE('',(#1831),#18942,.F.);
#19689=ADVANCED_FACE('',(#1832),#18943,.F.);
#19690=ADVANCED_FACE('',(#1833),#18944,.F.);
#19691=ADVANCED_FACE('',(#1834),#18945,.F.);
#19692=ADVANCED_FACE('',(#1835),#18946,.F.);
#19693=ADVANCED_FACE('',(#1836),#18947,.F.);
#19694=ADVANCED_FACE('',(#1837),#915,.T.);
#19695=ADVANCED_FACE('',(#1838),#18948,.F.);
#19696=ADVANCED_FACE('',(#1839),#18949,.F.);
#19697=ADVANCED_FACE('',(#1840),#18950,.F.);
#19698=ADVANCED_FACE('',(#1841),#18951,.F.);
#19699=ADVANCED_FACE('',(#1842),#18952,.F.);
#19700=ADVANCED_FACE('',(#1843),#18953,.F.);
#19701=ADVANCED_FACE('',(#1844),#18954,.F.);
#19702=ADVANCED_FACE('',(#1845,#659,#660,#661,#662,#663,#664,#665,#666,
#667,#668,#669,#670,#671),#18955,.F.);
#19703=ADVANCED_FACE('',(#1846),#18956,.T.);
#19704=ADVANCED_FACE('',(#1847),#916,.F.);
#19705=ADVANCED_FACE('',(#1848),#18957,.T.);
#19706=ADVANCED_FACE('',(#1849),#917,.F.);
#19707=ADVANCED_FACE('',(#1850),#18958,.T.);
#19708=ADVANCED_FACE('',(#1851),#18959,.T.);
#19709=ADVANCED_FACE('',(#1852),#18960,.T.);
#19710=ADVANCED_FACE('',(#1853),#18961,.T.);
#19711=ADVANCED_FACE('',(#1854),#18962,.T.);
#19712=ADVANCED_FACE('',(#1855),#18963,.T.);
#19713=ADVANCED_FACE('',(#1856),#18964,.T.);
#19714=ADVANCED_FACE('',(#1857),#18965,.T.);
#19715=ADVANCED_FACE('',(#1858),#18966,.T.);
#19716=ADVANCED_FACE('',(#1859),#18967,.T.);
#19717=ADVANCED_FACE('',(#1860),#18968,.T.);
#19718=ADVANCED_FACE('',(#1861),#18969,.T.);
#19719=ADVANCED_FACE('',(#1862),#918,.F.);
#19720=ADVANCED_FACE('',(#1863),#18970,.T.);
#19721=ADVANCED_FACE('',(#1864),#919,.F.);
#19722=ADVANCED_FACE('',(#1865),#18971,.T.);
#19723=ADVANCED_FACE('',(#1866),#920,.F.);
#19724=ADVANCED_FACE('',(#1867),#18972,.T.);
#19725=ADVANCED_FACE('',(#1868),#18973,.T.);
#19726=ADVANCED_FACE('',(#1869),#18974,.T.);
#19727=ADVANCED_FACE('',(#1870),#18975,.T.);
#19728=ADVANCED_FACE('',(#1871),#18976,.T.);
#19729=ADVANCED_FACE('',(#1872),#18977,.T.);
#19730=ADVANCED_FACE('',(#1873),#18978,.T.);
#19731=ADVANCED_FACE('',(#1874),#18979,.T.);
#19732=ADVANCED_FACE('',(#1875),#18980,.T.);
#19733=ADVANCED_FACE('',(#1876),#921,.T.);
#19734=ADVANCED_FACE('',(#1877),#18981,.T.);
#19735=ADVANCED_FACE('',(#1878),#18982,.T.);
#19736=ADVANCED_FACE('',(#1879),#18983,.T.);
#19737=ADVANCED_FACE('',(#1880),#18984,.T.);
#19738=ADVANCED_FACE('',(#1881),#18985,.T.);
#19739=ADVANCED_FACE('',(#1882),#18986,.T.);
#19740=ADVANCED_FACE('',(#1883),#18987,.T.);
#19741=ADVANCED_FACE('',(#1884,#672,#673,#674,#675,#676,#677,#678,#679,
#680,#681,#682,#683,#684),#18988,.T.);
#20126=CLOSED_SHELL('',(#19463,#19464,#19465,#19466,#19467,#19468,#19469,
#19470,#19471,#19472,#19473,#19474,#19475,#19476,#19477,#19478,#19479,#19480,
#19481,#19482,#19483,#19484,#19485,#19486,#19487,#19488,#19489,#19490,#19491,
#19492,#19493,#19494,#19495,#19496,#19497,#19498,#19499,#19500,#19501,#19502,
#19503,#19504,#19505,#19506,#19507,#19508,#19509,#19510,#19511,#19512,#19513,
#19514,#19515,#19516,#19517,#19518,#19519,#19520,#19521,#19522,#19523,#19524,
#19525,#19526,#19527,#19528,#19529,#19530,#19531,#19532,#19533,#19534,#19535,
#19536,#19537,#19538,#19539,#19540,#19541,#19542,#19543,#19544,#19545,#19546,
#19547,#19548,#19549,#19550,#19551,#19552,#19553,#19554,#19555,#19556,#19557,
#19558,#19559,#19560,#19561,#19562,#19563,#19564,#19565,#19566,#19567,#19568,
#19569,#19570,#19571,#19572,#19573,#19574,#19575,#19576,#19577,#19578,#19579,
#19580,#19581,#19582,#19583,#19584,#19585,#19586,#19587,#19588,#19589,#19590,
#19591,#19592,#19593,#19594,#19595,#19596,#19597,#19598,#19599,#19600,#19601,
#19602,#19603,#19604,#19605,#19606,#19607,#19608,#19609,#19610,#19611,#19612,
#19613,#19614,#19615,#19616,#19617,#19618,#19619,#19620,#19621,#19622,#19623,
#19624,#19625,#19626,#19627,#19628,#19629,#19630,#19631,#19632,#19633,#19634,
#19635,#19636,#19637,#19638,#19639,#19640,#19641,#19642,#19643,#19644,#19645,
#19646,#19647,#19648,#19649,#19650,#19651,#19652,#19653,#19654,#19655,#19656,
#19657,#19658,#19659,#19660,#19661,#19662,#19663,#19664,#19665,#19666,#19667,
#19668,#19669,#19670,#19671,#19672,#19673,#19674,#19675,#19676,#19677,#19678,
#19679,#19680,#19681,#19682,#19683,#19684,#19685,#19686,#19687,#19688,#19689,
#19690,#19691,#19692,#19693,#19694,#19695,#19696,#19697,#19698,#19699,#19700,
#19701,#19702,#19703,#19704,#19705,#19706,#19707,#19708,#19709,#19710,#19711,
#19712,#19713,#19714,#19715,#19716,#19717,#19718,#19719,#19720,#19721,#19722,
#19723,#19724,#19725,#19726,#19727,#19728,#19729,#19730,#19731,#19732,#19733,
#19734,#19735,#19736,#19737,#19738,#19739,#19740,#19741));
#21080=AXIS2_PLACEMENT_3D('',#29325,#24222,#24223);
#21081=AXIS2_PLACEMENT_3D('',#29326,#24224,#24225);
#21082=AXIS2_PLACEMENT_3D('',#29335,#24230,#24231);
#21083=AXIS2_PLACEMENT_3D('',#29341,#24235,#24236);
#21084=AXIS2_PLACEMENT_3D('',#29347,#24240,#24241);
#21085=AXIS2_PLACEMENT_3D('',#29356,#24246,#24247);
#21086=AXIS2_PLACEMENT_3D('',#29362,#24251,#24252);
#21087=AXIS2_PLACEMENT_3D('',#29368,#24256,#24257);
#21088=AXIS2_PLACEMENT_3D('',#29374,#24261,#24262);
#21089=AXIS2_PLACEMENT_3D('',#29380,#24266,#24267);
#21090=AXIS2_PLACEMENT_3D('',#29386,#24271,#24272);
#21091=AXIS2_PLACEMENT_3D('',#29395,#24277,#24278);
#21092=AXIS2_PLACEMENT_3D('',#29401,#24282,#24283);
#21093=AXIS2_PLACEMENT_3D('',#29407,#24287,#24288);
#21094=AXIS2_PLACEMENT_3D('',#29413,#24292,#24293);
#21095=AXIS2_PLACEMENT_3D('',#29422,#24298,#24299);
#21096=AXIS2_PLACEMENT_3D('',#29428,#24303,#24304);
#21097=AXIS2_PLACEMENT_3D('',#29434,#24308,#24309);
#21098=AXIS2_PLACEMENT_3D('',#29440,#24313,#24314);
#21099=AXIS2_PLACEMENT_3D('',#29446,#24318,#24319);
#21100=AXIS2_PLACEMENT_3D('',#29449,#24322,#24323);
#21101=AXIS2_PLACEMENT_3D('',#29458,#24328,#24329);
#21102=AXIS2_PLACEMENT_3D('',#29464,#24333,#24334);
#21103=AXIS2_PLACEMENT_3D('',#29470,#24338,#24339);
#21104=AXIS2_PLACEMENT_3D('',#29473,#24342,#24343);
#21105=AXIS2_PLACEMENT_3D('',#29482,#24348,#24349);
#21106=AXIS2_PLACEMENT_3D('',#29488,#24353,#24354);
#21107=AXIS2_PLACEMENT_3D('',#29494,#24358,#24359);
#21108=AXIS2_PLACEMENT_3D('',#29500,#24363,#24364);
#21109=AXIS2_PLACEMENT_3D('',#29506,#24368,#24369);
#21110=AXIS2_PLACEMENT_3D('',#29512,#24373,#24374);
#21111=AXIS2_PLACEMENT_3D('',#29521,#24379,#24380);
#21112=AXIS2_PLACEMENT_3D('',#29527,#24384,#24385);
#21113=AXIS2_PLACEMENT_3D('',#29533,#24389,#24390);
#21114=AXIS2_PLACEMENT_3D('',#29536,#24393,#24394);
#21115=AXIS2_PLACEMENT_3D('',#29538,#24395,#24396);
#21116=AXIS2_PLACEMENT_3D('',#29541,#24398,#24399);
#21117=AXIS2_PLACEMENT_3D('',#29542,#24400,#24401);
#21118=AXIS2_PLACEMENT_3D('',#29548,#24405,#24406);
#21119=AXIS2_PLACEMENT_3D('',#29557,#24411,#24412);
#21120=AXIS2_PLACEMENT_3D('',#29563,#24416,#24417);
#21121=AXIS2_PLACEMENT_3D('',#29569,#24421,#24422);
#21122=AXIS2_PLACEMENT_3D('',#29575,#24426,#24427);
#21123=AXIS2_PLACEMENT_3D('',#29581,#24431,#24432);
#21124=AXIS2_PLACEMENT_3D('',#29584,#24435,#24436);
#21125=AXIS2_PLACEMENT_3D('',#29593,#24441,#24442);
#21126=AXIS2_PLACEMENT_3D('',#29595,#24443,#24444);
#21127=AXIS2_PLACEMENT_3D('',#29597,#24445,#24446);
#21128=AXIS2_PLACEMENT_3D('',#29599,#24448,#24449);
#21129=AXIS2_PLACEMENT_3D('',#29605,#24453,#24454);
#21130=AXIS2_PLACEMENT_3D('',#29607,#24455,#24456);
#21131=AXIS2_PLACEMENT_3D('',#29609,#24457,#24458);
#21132=AXIS2_PLACEMENT_3D('',#29611,#24460,#24461);
#21133=AXIS2_PLACEMENT_3D('',#29620,#24466,#24467);
#21134=AXIS2_PLACEMENT_3D('',#29626,#24471,#24472);
#21135=AXIS2_PLACEMENT_3D('',#29632,#24476,#24477);
#21136=AXIS2_PLACEMENT_3D('',#29638,#24481,#24482);
#21137=AXIS2_PLACEMENT_3D('',#29644,#24486,#24487);
#21138=AXIS2_PLACEMENT_3D('',#29650,#24491,#24492);
#21139=AXIS2_PLACEMENT_3D('',#29653,#24495,#24496);
#21140=AXIS2_PLACEMENT_3D('',#29659,#24500,#24501);
#21141=AXIS2_PLACEMENT_3D('',#29665,#24505,#24506);
#21142=AXIS2_PLACEMENT_3D('',#29671,#24510,#24511);
#21143=AXIS2_PLACEMENT_3D('',#29677,#24515,#24516);
#21144=AXIS2_PLACEMENT_3D('',#29679,#24517,#24518);
#21145=AXIS2_PLACEMENT_3D('',#29682,#24520,#24521);
#21146=AXIS2_PLACEMENT_3D('',#29683,#24522,#24523);
#21147=AXIS2_PLACEMENT_3D('',#29689,#24527,#24528);
#21148=AXIS2_PLACEMENT_3D('',#29691,#24529,#24530);
#21149=AXIS2_PLACEMENT_3D('',#29694,#24532,#24533);
#21150=AXIS2_PLACEMENT_3D('',#29695,#24534,#24535);
#21151=AXIS2_PLACEMENT_3D('',#29698,#24538,#24539);
#21152=AXIS2_PLACEMENT_3D('',#29704,#24543,#24544);
#21153=AXIS2_PLACEMENT_3D('',#29710,#24548,#24549);
#21154=AXIS2_PLACEMENT_3D('',#29716,#24553,#24554);
#21155=AXIS2_PLACEMENT_3D('',#29722,#24558,#24559);
#21156=AXIS2_PLACEMENT_3D('',#29728,#24563,#24564);
#21157=AXIS2_PLACEMENT_3D('',#29734,#24568,#24569);
#21158=AXIS2_PLACEMENT_3D('',#29740,#24573,#24574);
#21159=AXIS2_PLACEMENT_3D('',#29746,#24578,#24579);
#21160=AXIS2_PLACEMENT_3D('',#29748,#24580,#24581);
#21161=AXIS2_PLACEMENT_3D('',#29751,#24583,#24584);
#21162=AXIS2_PLACEMENT_3D('',#29752,#24585,#24586);
#21163=AXIS2_PLACEMENT_3D('',#29758,#24590,#24591);
#21164=AXIS2_PLACEMENT_3D('',#29764,#24595,#24596);
#21165=AXIS2_PLACEMENT_3D('',#29770,#24600,#24601);
#21166=AXIS2_PLACEMENT_3D('',#29776,#24605,#24606);
#21167=AXIS2_PLACEMENT_3D('',#29782,#24610,#24611);
#21168=AXIS2_PLACEMENT_3D('',#29788,#24615,#24616);
#21169=AXIS2_PLACEMENT_3D('',#29794,#24620,#24621);
#21170=AXIS2_PLACEMENT_3D('',#29803,#24626,#24627);
#21171=AXIS2_PLACEMENT_3D('',#29805,#24628,#24629);
#21172=AXIS2_PLACEMENT_3D('',#29808,#24631,#24632);
#21173=AXIS2_PLACEMENT_3D('',#29809,#24633,#24634);
#21174=AXIS2_PLACEMENT_3D('',#29815,#24638,#24639);
#21175=AXIS2_PLACEMENT_3D('',#29817,#24640,#24641);
#21176=AXIS2_PLACEMENT_3D('',#29820,#24643,#24644);
#21177=AXIS2_PLACEMENT_3D('',#29821,#24645,#24646);
#21178=AXIS2_PLACEMENT_3D('',#29830,#24651,#24652);
#21179=AXIS2_PLACEMENT_3D('',#29836,#24656,#24657);
#21180=AXIS2_PLACEMENT_3D('',#29842,#24661,#24662);
#21181=AXIS2_PLACEMENT_3D('',#29848,#24666,#24667);
#21182=AXIS2_PLACEMENT_3D('',#29854,#24671,#24672);
#21183=AXIS2_PLACEMENT_3D('',#29860,#24676,#24677);
#21184=AXIS2_PLACEMENT_3D('',#29863,#24680,#24681);
#21185=AXIS2_PLACEMENT_3D('',#29869,#24685,#24686);
#21186=AXIS2_PLACEMENT_3D('',#29875,#24690,#24691);
#21187=AXIS2_PLACEMENT_3D('',#29881,#24695,#24696);
#21188=AXIS2_PLACEMENT_3D('',#29887,#24700,#24701);
#21189=AXIS2_PLACEMENT_3D('',#29890,#24704,#24705);
#21190=AXIS2_PLACEMENT_3D('',#29892,#24706,#24707);
#21191=AXIS2_PLACEMENT_3D('',#29895,#24709,#24710);
#21192=AXIS2_PLACEMENT_3D('',#29896,#24711,#24712);
#21193=AXIS2_PLACEMENT_3D('',#29902,#24716,#24717);
#21194=AXIS2_PLACEMENT_3D('',#29904,#24718,#24719);
#21195=AXIS2_PLACEMENT_3D('',#29906,#24720,#24721);
#21196=AXIS2_PLACEMENT_3D('',#29908,#24723,#24724);
#21197=AXIS2_PLACEMENT_3D('',#29914,#24728,#24729);
#21198=AXIS2_PLACEMENT_3D('',#29916,#24730,#24731);
#21199=AXIS2_PLACEMENT_3D('',#29918,#24732,#24733);
#21200=AXIS2_PLACEMENT_3D('',#29920,#24735,#24736);
#21201=AXIS2_PLACEMENT_3D('',#29923,#24739,#24740);
#21202=AXIS2_PLACEMENT_3D('',#29929,#24744,#24745);
#21203=AXIS2_PLACEMENT_3D('',#29935,#24749,#24750);
#21204=AXIS2_PLACEMENT_3D('',#29941,#24754,#24755);
#21205=AXIS2_PLACEMENT_3D('',#29947,#24759,#24760);
#21206=AXIS2_PLACEMENT_3D('',#29953,#24764,#24765);
#21207=AXIS2_PLACEMENT_3D('',#29959,#24769,#24770);
#21208=AXIS2_PLACEMENT_3D('',#29965,#24774,#24775);
#21209=AXIS2_PLACEMENT_3D('',#29971,#24779,#24780);
#21210=AXIS2_PLACEMENT_3D('',#29973,#24781,#24782);
#21211=AXIS2_PLACEMENT_3D('',#29975,#24783,#24784);
#21212=AXIS2_PLACEMENT_3D('',#29977,#24786,#24787);
#21213=AXIS2_PLACEMENT_3D('',#29983,#24791,#24792);
#21214=AXIS2_PLACEMENT_3D('',#29989,#24796,#24797);
#21215=AXIS2_PLACEMENT_3D('',#29995,#24801,#24802);
#21216=AXIS2_PLACEMENT_3D('',#30001,#24806,#24807);
#21217=AXIS2_PLACEMENT_3D('',#30007,#24811,#24812);
#21218=AXIS2_PLACEMENT_3D('',#30013,#24816,#24817);
#21219=AXIS2_PLACEMENT_3D('',#30016,#24820,#24821);
#21220=AXIS2_PLACEMENT_3D('',#30025,#24826,#24827);
#21221=AXIS2_PLACEMENT_3D('',#30031,#24831,#24832);
#21222=AXIS2_PLACEMENT_3D('',#30037,#24836,#24837);
#21223=AXIS2_PLACEMENT_3D('',#30046,#24842,#24843);
#21224=AXIS2_PLACEMENT_3D('',#30052,#24847,#24848);
#21225=AXIS2_PLACEMENT_3D('',#30058,#24852,#24853);
#21226=AXIS2_PLACEMENT_3D('',#30064,#24857,#24858);
#21227=AXIS2_PLACEMENT_3D('',#30070,#24862,#24863);
#21228=AXIS2_PLACEMENT_3D('',#30076,#24867,#24868);
#21229=AXIS2_PLACEMENT_3D('',#30082,#24872,#24873);
#21230=AXIS2_PLACEMENT_3D('',#30088,#24877,#24878);
#21231=AXIS2_PLACEMENT_3D('',#30094,#24882,#24883);
#21232=AXIS2_PLACEMENT_3D('',#30100,#24887,#24888);
#21233=AXIS2_PLACEMENT_3D('',#30106,#24892,#24893);
#21234=AXIS2_PLACEMENT_3D('',#30112,#24897,#24898);
#21235=AXIS2_PLACEMENT_3D('',#30118,#24902,#24903);
#21236=AXIS2_PLACEMENT_3D('',#30124,#24907,#24908);
#21237=AXIS2_PLACEMENT_3D('',#30130,#24912,#24913);
#21238=AXIS2_PLACEMENT_3D('',#30136,#24917,#24918);
#21239=AXIS2_PLACEMENT_3D('',#30142,#24922,#24923);
#21240=AXIS2_PLACEMENT_3D('',#30145,#24926,#24927);
#21241=AXIS2_PLACEMENT_3D('',#30154,#24932,#24933);
#21242=AXIS2_PLACEMENT_3D('',#30160,#24937,#24938);
#21243=AXIS2_PLACEMENT_3D('',#30166,#24942,#24943);
#21244=AXIS2_PLACEMENT_3D('',#30169,#24946,#24947);
#21245=AXIS2_PLACEMENT_3D('',#30178,#24952,#24953);
#21246=AXIS2_PLACEMENT_3D('',#30184,#24957,#24958);
#21247=AXIS2_PLACEMENT_3D('',#30190,#24962,#24963);
#21248=AXIS2_PLACEMENT_3D('',#30196,#24967,#24968);
#21249=AXIS2_PLACEMENT_3D('',#30202,#24972,#24973);
#21250=AXIS2_PLACEMENT_3D('',#30208,#24977,#24978);
#21251=AXIS2_PLACEMENT_3D('',#30214,#24982,#24983);
#21252=AXIS2_PLACEMENT_3D('',#30220,#24987,#24988);
#21253=AXIS2_PLACEMENT_3D('',#30226,#24992,#24993);
#21254=AXIS2_PLACEMENT_3D('',#30232,#24997,#24998);
#21255=AXIS2_PLACEMENT_3D('',#30235,#25001,#25002);
#21256=AXIS2_PLACEMENT_3D('',#30237,#25003,#25004);
#21257=AXIS2_PLACEMENT_3D('',#30240,#25006,#25007);
#21258=AXIS2_PLACEMENT_3D('',#30241,#25008,#25009);
#21259=AXIS2_PLACEMENT_3D('',#30247,#25013,#25014);
#21260=AXIS2_PLACEMENT_3D('',#30253,#25018,#25019);
#21261=AXIS2_PLACEMENT_3D('',#30259,#25023,#25024);
#21262=AXIS2_PLACEMENT_3D('',#30265,#25028,#25029);
#21263=AXIS2_PLACEMENT_3D('',#30271,#25033,#25034);
#21264=AXIS2_PLACEMENT_3D('',#30277,#25038,#25039);
#21265=AXIS2_PLACEMENT_3D('',#30283,#25043,#25044);
#21266=AXIS2_PLACEMENT_3D('',#30286,#25047,#25048);
#21267=AXIS2_PLACEMENT_3D('',#30295,#25053,#25054);
#21268=AXIS2_PLACEMENT_3D('',#30301,#25058,#25059);
#21269=AXIS2_PLACEMENT_3D('',#30307,#25063,#25064);
#21270=AXIS2_PLACEMENT_3D('',#30316,#25069,#25070);
#21271=AXIS2_PLACEMENT_3D('',#30322,#25074,#25075);
#21272=AXIS2_PLACEMENT_3D('',#30328,#25079,#25080);
#21273=AXIS2_PLACEMENT_3D('',#30334,#25084,#25085);
#21274=AXIS2_PLACEMENT_3D('',#30340,#25089,#25090);
#21275=AXIS2_PLACEMENT_3D('',#30346,#25094,#25095);
#21276=AXIS2_PLACEMENT_3D('',#30352,#25099,#25100);
#21277=AXIS2_PLACEMENT_3D('',#30358,#25104,#25105);
#21278=AXIS2_PLACEMENT_3D('',#30364,#25109,#25110);
#21279=AXIS2_PLACEMENT_3D('',#30370,#25114,#25115);
#21280=AXIS2_PLACEMENT_3D('',#30376,#25119,#25120);
#21281=AXIS2_PLACEMENT_3D('',#30382,#25124,#25125);
#21282=AXIS2_PLACEMENT_3D('',#30388,#25129,#25130);
#21283=AXIS2_PLACEMENT_3D('',#30394,#25134,#25135);
#21284=AXIS2_PLACEMENT_3D('',#30400,#25139,#25140);
#21285=AXIS2_PLACEMENT_3D('',#30406,#25144,#25145);
#21286=AXIS2_PLACEMENT_3D('',#30412,#25149,#25150);
#21287=AXIS2_PLACEMENT_3D('',#30415,#25153,#25154);
#21288=AXIS2_PLACEMENT_3D('',#30424,#25159,#25160);
#21289=AXIS2_PLACEMENT_3D('',#30430,#25164,#25165);
#21290=AXIS2_PLACEMENT_3D('',#30436,#25169,#25170);
#21291=AXIS2_PLACEMENT_3D('',#30439,#25173,#25174);
#21292=AXIS2_PLACEMENT_3D('',#30448,#25179,#25180);
#21293=AXIS2_PLACEMENT_3D('',#30454,#25184,#25185);
#21294=AXIS2_PLACEMENT_3D('',#30460,#25189,#25190);
#21295=AXIS2_PLACEMENT_3D('',#30466,#25194,#25195);
#21296=AXIS2_PLACEMENT_3D('',#30472,#25199,#25200);
#21297=AXIS2_PLACEMENT_3D('',#30478,#25204,#25205);
#21298=AXIS2_PLACEMENT_3D('',#30484,#25209,#25210);
#21299=AXIS2_PLACEMENT_3D('',#30490,#25214,#25215);
#21300=AXIS2_PLACEMENT_3D('',#30496,#25219,#25220);
#21301=AXIS2_PLACEMENT_3D('',#30502,#25224,#25225);
#21302=AXIS2_PLACEMENT_3D('',#30505,#25228,#25229);
#21303=AXIS2_PLACEMENT_3D('',#30507,#25230,#25231);
#21304=AXIS2_PLACEMENT_3D('',#30510,#25233,#25234);
#21305=AXIS2_PLACEMENT_3D('',#30511,#25235,#25236);
#21306=AXIS2_PLACEMENT_3D('',#30517,#25240,#25241);
#21307=AXIS2_PLACEMENT_3D('',#30523,#25245,#25246);
#21308=AXIS2_PLACEMENT_3D('',#30529,#25250,#25251);
#21309=AXIS2_PLACEMENT_3D('',#30535,#25255,#25256);
#21310=AXIS2_PLACEMENT_3D('',#30541,#25260,#25261);
#21311=AXIS2_PLACEMENT_3D('',#30547,#25265,#25266);
#21312=AXIS2_PLACEMENT_3D('',#30553,#25270,#25271);
#21313=AXIS2_PLACEMENT_3D('',#30556,#25274,#25275);
#21314=AXIS2_PLACEMENT_3D('',#30565,#25280,#25281);
#21315=AXIS2_PLACEMENT_3D('',#30567,#25282,#25283);
#21316=AXIS2_PLACEMENT_3D('',#30569,#25284,#25285);
#21317=AXIS2_PLACEMENT_3D('',#30571,#25287,#25288);
#21318=AXIS2_PLACEMENT_3D('',#30577,#25292,#25293);
#21319=AXIS2_PLACEMENT_3D('',#30579,#25294,#25295);
#21320=AXIS2_PLACEMENT_3D('',#30581,#25296,#25297);
#21321=AXIS2_PLACEMENT_3D('',#30583,#25299,#25300);
#21322=AXIS2_PLACEMENT_3D('',#30592,#25305,#25306);
#21323=AXIS2_PLACEMENT_3D('',#30598,#25310,#25311);
#21324=AXIS2_PLACEMENT_3D('',#30604,#25315,#25316);
#21325=AXIS2_PLACEMENT_3D('',#30610,#25320,#25321);
#21326=AXIS2_PLACEMENT_3D('',#30616,#25325,#25326);
#21327=AXIS2_PLACEMENT_3D('',#30622,#25330,#25331);
#21328=AXIS2_PLACEMENT_3D('',#30625,#25334,#25335);
#21329=AXIS2_PLACEMENT_3D('',#30631,#25339,#25340);
#21330=AXIS2_PLACEMENT_3D('',#30637,#25344,#25345);
#21331=AXIS2_PLACEMENT_3D('',#30643,#25349,#25350);
#21332=AXIS2_PLACEMENT_3D('',#30649,#25354,#25355);
#21333=AXIS2_PLACEMENT_3D('',#30651,#25356,#25357);
#21334=AXIS2_PLACEMENT_3D('',#30654,#25359,#25360);
#21335=AXIS2_PLACEMENT_3D('',#30655,#25361,#25362);
#21336=AXIS2_PLACEMENT_3D('',#30661,#25366,#25367);
#21337=AXIS2_PLACEMENT_3D('',#30663,#25368,#25369);
#21338=AXIS2_PLACEMENT_3D('',#30666,#25371,#25372);
#21339=AXIS2_PLACEMENT_3D('',#30667,#25373,#25374);
#21340=AXIS2_PLACEMENT_3D('',#30670,#25377,#25378);
#21341=AXIS2_PLACEMENT_3D('',#30676,#25382,#25383);
#21342=AXIS2_PLACEMENT_3D('',#30682,#25387,#25388);
#21343=AXIS2_PLACEMENT_3D('',#30688,#25392,#25393);
#21344=AXIS2_PLACEMENT_3D('',#30694,#25397,#25398);
#21345=AXIS2_PLACEMENT_3D('',#30700,#25402,#25403);
#21346=AXIS2_PLACEMENT_3D('',#30706,#25407,#25408);
#21347=AXIS2_PLACEMENT_3D('',#30712,#25412,#25413);
#21348=AXIS2_PLACEMENT_3D('',#30718,#25417,#25418);
#21349=AXIS2_PLACEMENT_3D('',#30720,#25419,#25420);
#21350=AXIS2_PLACEMENT_3D('',#30723,#25422,#25423);
#21351=AXIS2_PLACEMENT_3D('',#30724,#25424,#25425);
#21352=AXIS2_PLACEMENT_3D('',#30730,#25429,#25430);
#21353=AXIS2_PLACEMENT_3D('',#30736,#25434,#25435);
#21354=AXIS2_PLACEMENT_3D('',#30742,#25439,#25440);
#21355=AXIS2_PLACEMENT_3D('',#30748,#25444,#25445);
#21356=AXIS2_PLACEMENT_3D('',#30754,#25449,#25450);
#21357=AXIS2_PLACEMENT_3D('',#30760,#25454,#25455);
#21358=AXIS2_PLACEMENT_3D('',#30766,#25459,#25460);
#21359=AXIS2_PLACEMENT_3D('',#30798,#25476,#25477);
#21360=AXIS2_PLACEMENT_3D('',#30825,#25491,#25492);
#21361=AXIS2_PLACEMENT_3D('',#30829,#25494,#25495);
#21362=AXIS2_PLACEMENT_3D('',#30833,#25497,#25498);
#21363=AXIS2_PLACEMENT_3D('',#30837,#25500,#25501);
#21364=AXIS2_PLACEMENT_3D('',#30840,#25503,#25504);
#21365=AXIS2_PLACEMENT_3D('',#30841,#25505,#25506);
#21366=AXIS2_PLACEMENT_3D('',#30847,#25510,#25511);
#21367=AXIS2_PLACEMENT_3D('',#30850,#25513,#25514);
#21368=AXIS2_PLACEMENT_3D('',#30851,#25515,#25516);
#21369=AXIS2_PLACEMENT_3D('',#30855,#25519,#25520);
#21370=AXIS2_PLACEMENT_3D('',#30858,#25522,#25523);
#21371=AXIS2_PLACEMENT_3D('',#30859,#25524,#25525);
#21372=AXIS2_PLACEMENT_3D('',#30865,#25529,#25530);
#21373=AXIS2_PLACEMENT_3D('',#30869,#25533,#25534);
#21374=AXIS2_PLACEMENT_3D('',#30873,#25537,#25538);
#21375=AXIS2_PLACEMENT_3D('',#30877,#25541,#25542);
#21376=AXIS2_PLACEMENT_3D('',#30881,#25545,#25546);
#21377=AXIS2_PLACEMENT_3D('',#30885,#25549,#25550);
#21378=AXIS2_PLACEMENT_3D('',#30887,#25552,#25553);
#21379=AXIS2_PLACEMENT_3D('',#30891,#25556,#25557);
#21380=AXIS2_PLACEMENT_3D('',#30895,#25560,#25561);
#21381=AXIS2_PLACEMENT_3D('',#30899,#25564,#25565);
#21382=AXIS2_PLACEMENT_3D('',#30903,#25568,#25569);
#21383=AXIS2_PLACEMENT_3D('',#30905,#25571,#25572);
#21384=AXIS2_PLACEMENT_3D('',#30907,#25573,#25574);
#21385=AXIS2_PLACEMENT_3D('',#30909,#25576,#25577);
#21386=AXIS2_PLACEMENT_3D('',#30913,#25580,#25581);
#21387=AXIS2_PLACEMENT_3D('',#30915,#25582,#25583);
#21388=AXIS2_PLACEMENT_3D('',#30917,#25585,#25586);
#21389=AXIS2_PLACEMENT_3D('',#30921,#25589,#25590);
#21390=AXIS2_PLACEMENT_3D('',#30923,#25591,#25592);
#21391=AXIS2_PLACEMENT_3D('',#30925,#25594,#25595);
#21392=AXIS2_PLACEMENT_3D('',#30927,#25597,#25598);
#21393=AXIS2_PLACEMENT_3D('',#30931,#25601,#25602);
#21394=AXIS2_PLACEMENT_3D('',#30935,#25605,#25606);
#21395=AXIS2_PLACEMENT_3D('',#30939,#25609,#25610);
#21396=AXIS2_PLACEMENT_3D('',#30943,#25613,#25614);
#21397=AXIS2_PLACEMENT_3D('',#30947,#25617,#25618);
#21398=AXIS2_PLACEMENT_3D('',#30951,#25621,#25622);
#21399=AXIS2_PLACEMENT_3D('',#30955,#25625,#25626);
#21400=AXIS2_PLACEMENT_3D('',#30959,#25629,#25630);
#21401=AXIS2_PLACEMENT_3D('',#30961,#25631,#25632);
#21402=AXIS2_PLACEMENT_3D('',#30963,#25634,#25635);
#21403=AXIS2_PLACEMENT_3D('',#30967,#25638,#25639);
#21404=AXIS2_PLACEMENT_3D('',#30971,#25642,#25643);
#21405=AXIS2_PLACEMENT_3D('',#30975,#25646,#25647);
#21406=AXIS2_PLACEMENT_3D('',#30979,#25650,#25651);
#21407=AXIS2_PLACEMENT_3D('',#30983,#25654,#25655);
#21408=AXIS2_PLACEMENT_3D('',#30987,#25658,#25659);
#21409=AXIS2_PLACEMENT_3D('',#30989,#25661,#25662);
#24222=DIRECTION('axis',(0.,0.,1.));
#24223=DIRECTION('refdir',(1.,0.,0.));
#24224=DIRECTION('center_axis',(-1.,0.,0.));
#24225=DIRECTION('ref_axis',(0.,0.,1.));
#24226=DIRECTION('',(0.,0.,1.));
#24227=DIRECTION('',(0.,1.,0.));
#24228=DIRECTION('',(0.,0.,1.));
#24229=DIRECTION('',(0.,1.,0.));
#24230=DIRECTION('center_axis',(0.,0.,1.));
#24231=DIRECTION('ref_axis',(1.,0.,0.));
#24232=DIRECTION('',(1.,0.,0.));
#24233=DIRECTION('',(0.,1.,0.));
#24234=DIRECTION('',(1.,0.,0.));
#24235=DIRECTION('center_axis',(-0.710721462348357,0.,0.703473526834815));
#24236=DIRECTION('ref_axis',(0.703473526834815,0.,0.710721462348357));
#24237=DIRECTION('',(0.703473526834815,0.,0.710721462348357));
#24238=DIRECTION('',(0.,1.,0.));
#24239=DIRECTION('',(0.703473526834815,0.,0.710721462348357));
#24240=DIRECTION('center_axis',(1.,0.,0.));
#24241=DIRECTION('ref_axis',(0.,0.,-1.));
#24242=DIRECTION('',(0.,0.,-1.));
#24243=DIRECTION('',(0.,1.,0.));
#24244=DIRECTION('',(0.,0.,-1.));
#24245=DIRECTION('',(0.,1.,0.));
#24246=DIRECTION('center_axis',(0.,0.,-1.));
#24247=DIRECTION('ref_axis',(-1.,0.,0.));
#24248=DIRECTION('',(-1.,0.,0.));
#24249=DIRECTION('',(-1.,0.,0.));
#24250=DIRECTION('',(0.,1.,0.));
#24251=DIRECTION('center_axis',(1.,0.,0.));
#24252=DIRECTION('ref_axis',(0.,0.,-1.));
#24253=DIRECTION('',(0.,0.,-1.));
#24254=DIRECTION('',(0.,0.,-1.));
#24255=DIRECTION('',(0.,1.,0.));
#24256=DIRECTION('center_axis',(0.,0.,1.));
#24257=DIRECTION('ref_axis',(1.,0.,0.));
#24258=DIRECTION('',(1.,0.,0.));
#24259=DIRECTION('',(1.,0.,0.));
#24260=DIRECTION('',(0.,1.,0.));
#24261=DIRECTION('center_axis',(1.,0.,0.));
#24262=DIRECTION('ref_axis',(0.,0.,-1.));
#24263=DIRECTION('',(0.,0.,-1.));
#24264=DIRECTION('',(0.,0.,-1.));
#24265=DIRECTION('',(0.,1.,0.));
#24266=DIRECTION('center_axis',(0.710721462348357,0.,-0.703473526834815));
#24267=DIRECTION('ref_axis',(-0.703473526834815,0.,-0.710721462348357));
#24268=DIRECTION('',(-0.703473526834815,0.,-0.710721462348357));
#24269=DIRECTION('',(-0.703473526834815,0.,-0.710721462348357));
#24270=DIRECTION('',(0.,1.,0.));
#24271=DIRECTION('center_axis',(-1.,0.,0.));
#24272=DIRECTION('ref_axis',(0.,0.,1.));
#24273=DIRECTION('',(0.,0.,1.));
#24274=DIRECTION('',(0.,1.,0.));
#24275=DIRECTION('',(0.,0.,1.));
#24276=DIRECTION('',(0.,1.,0.));
#24277=DIRECTION('center_axis',(0.,0.,-1.));
#24278=DIRECTION('ref_axis',(-1.,0.,0.));
#24279=DIRECTION('',(-1.,0.,0.));
#24280=DIRECTION('',(-1.,0.,0.));
#24281=DIRECTION('',(0.,1.,0.));
#24282=DIRECTION('center_axis',(-0.710721462348357,0.,-0.703473526834815));
#24283=DIRECTION('ref_axis',(-0.703473526834815,0.,0.710721462348357));
#24284=DIRECTION('',(-0.703473526834815,0.,0.710721462348357));
#24285=DIRECTION('',(-0.703473526834815,0.,0.710721462348357));
#24286=DIRECTION('',(0.,1.,0.));
#24287=DIRECTION('center_axis',(0.,0.,1.));
#24288=DIRECTION('ref_axis',(1.,0.,0.));
#24289=DIRECTION('',(1.,0.,0.));
#24290=DIRECTION('',(-1.,0.,0.));
#24291=DIRECTION('',(0.,1.,0.));
#24292=DIRECTION('center_axis',(1.,0.,0.));
#24293=DIRECTION('ref_axis',(0.,0.,-1.));
#24294=DIRECTION('',(0.,0.,-1.));
#24295=DIRECTION('',(0.,1.,0.));
#24296=DIRECTION('',(0.,0.,-1.));
#24297=DIRECTION('',(0.,1.,0.));
#24298=DIRECTION('center_axis',(0.,0.,1.));
#24299=DIRECTION('ref_axis',(1.,0.,0.));
#24300=DIRECTION('',(1.,0.,0.));
#24301=DIRECTION('',(0.,1.,0.));
#24302=DIRECTION('',(1.,0.,0.));
#24303=DIRECTION('center_axis',(1.,0.,0.));
#24304=DIRECTION('ref_axis',(0.,0.,-1.));
#24305=DIRECTION('',(0.,0.,-1.));
#24306=DIRECTION('',(0.,1.,0.));
#24307=DIRECTION('',(0.,0.,-1.));
#24308=DIRECTION('center_axis',(0.,0.,-1.));
#24309=DIRECTION('ref_axis',(-1.,0.,0.));
#24310=DIRECTION('',(-1.,0.,0.));
#24311=DIRECTION('',(0.,1.,0.));
#24312=DIRECTION('',(-1.,0.,0.));
#24313=DIRECTION('center_axis',(1.,0.,0.));
#24314=DIRECTION('ref_axis',(0.,0.,-1.));
#24315=DIRECTION('',(0.,0.,-1.));
#24316=DIRECTION('',(0.,1.,0.));
#24317=DIRECTION('',(0.,0.,-1.));
#24318=DIRECTION('center_axis',(0.710721462348357,0.,0.703473526834815));
#24319=DIRECTION('ref_axis',(0.703473526834815,0.,-0.710721462348357));
#24320=DIRECTION('',(0.703473526834815,0.,-0.710721462348357));
#24321=DIRECTION('',(0.703473526834815,0.,-0.710721462348357));
#24322=DIRECTION('center_axis',(1.,0.,0.));
#24323=DIRECTION('ref_axis',(0.,0.,-1.));
#24324=DIRECTION('',(0.,0.,-1.));
#24325=DIRECTION('',(0.,1.,0.));
#24326=DIRECTION('',(0.,0.,-1.));
#24327=DIRECTION('',(0.,1.,0.));
#24328=DIRECTION('center_axis',(0.,0.,1.));
#24329=DIRECTION('ref_axis',(1.,0.,0.));
#24330=DIRECTION('',(1.,0.,0.));
#24331=DIRECTION('',(1.,0.,0.));
#24332=DIRECTION('',(0.,1.,0.));
#24333=DIRECTION('center_axis',(0.710721462348357,0.,0.703473526834815));
#24334=DIRECTION('ref_axis',(0.703473526834815,0.,-0.710721462348357));
#24335=DIRECTION('',(0.703473526834815,0.,-0.710721462348357));
#24336=DIRECTION('',(0.703473526834815,0.,-0.710721462348357));
#24337=DIRECTION('',(0.,1.,0.));
#24338=DIRECTION('center_axis',(1.,0.,0.));
#24339=DIRECTION('ref_axis',(0.,0.,-1.));
#24340=DIRECTION('',(0.,0.,1.));
#24341=DIRECTION('',(0.,0.,-1.));
#24342=DIRECTION('center_axis',(-1.,0.,0.));
#24343=DIRECTION('ref_axis',(0.,0.,1.));
#24344=DIRECTION('',(0.,0.,1.));
#24345=DIRECTION('',(0.,1.,0.));
#24346=DIRECTION('',(0.,0.,1.));
#24347=DIRECTION('',(0.,1.,0.));
#24348=DIRECTION('center_axis',(0.,0.,-1.));
#24349=DIRECTION('ref_axis',(-1.,0.,0.));
#24350=DIRECTION('',(-1.,0.,0.));
#24351=DIRECTION('',(0.,1.,0.));
#24352=DIRECTION('',(-1.,0.,0.));
#24353=DIRECTION('center_axis',(-1.,0.,0.));
#24354=DIRECTION('ref_axis',(0.,0.,1.));
#24355=DIRECTION('',(0.,0.,1.));
#24356=DIRECTION('',(0.,1.,0.));
#24357=DIRECTION('',(0.,0.,1.));
#24358=DIRECTION('center_axis',(0.,0.,1.));
#24359=DIRECTION('ref_axis',(1.,0.,0.));
#24360=DIRECTION('',(1.,0.,0.));
#24361=DIRECTION('',(0.,1.,0.));
#24362=DIRECTION('',(1.,0.,0.));
#24363=DIRECTION('center_axis',(-1.,0.,0.));
#24364=DIRECTION('ref_axis',(0.,0.,1.));
#24365=DIRECTION('',(0.,0.,1.));
#24366=DIRECTION('',(0.,1.,0.));
#24367=DIRECTION('',(0.,0.,1.));
#24368=DIRECTION('center_axis',(-0.710721462348357,0.,-0.703473526834815));
#24369=DIRECTION('ref_axis',(-0.703473526834815,0.,0.710721462348357));
#24370=DIRECTION('',(-0.703473526834815,0.,0.710721462348357));
#24371=DIRECTION('',(0.,1.,0.));
#24372=DIRECTION('',(-0.703473526834815,0.,0.710721462348357));
#24373=DIRECTION('center_axis',(1.,0.,0.));
#24374=DIRECTION('ref_axis',(0.,0.,-1.));
#24375=DIRECTION('',(0.,0.,-1.));
#24376=DIRECTION('',(0.,1.,0.));
#24377=DIRECTION('',(0.,0.,-1.));
#24378=DIRECTION('',(0.,1.,0.));
#24379=DIRECTION('center_axis',(0.,0.,-1.));
#24380=DIRECTION('ref_axis',(-1.,0.,0.));
#24381=DIRECTION('',(-1.,0.,0.));
#24382=DIRECTION('',(0.,1.,0.));
#24383=DIRECTION('',(-1.,0.,0.));
#24384=DIRECTION('center_axis',(0.710721462348357,0.,-0.703473526834815));
#24385=DIRECTION('ref_axis',(-0.703473526834815,0.,-0.710721462348357));
#24386=DIRECTION('',(-0.703473526834815,0.,-0.710721462348357));
#24387=DIRECTION('',(0.,1.,0.));
#24388=DIRECTION('',(-0.703473526834815,0.,-0.710721462348357));
#24389=DIRECTION('center_axis',(1.,0.,0.));
#24390=DIRECTION('ref_axis',(0.,0.,-1.));
#24391=DIRECTION('',(0.,0.,1.));
#24392=DIRECTION('',(0.,0.,-1.));
#24393=DIRECTION('center_axis',(0.,1.,0.));
#24394=DIRECTION('ref_axis',(1.,0.,0.));
#24395=DIRECTION('center_axis',(0.,1.,0.));
#24396=DIRECTION('ref_axis',(1.,0.,0.));
#24397=DIRECTION('',(0.,-1.,0.));
#24398=DIRECTION('center_axis',(0.,1.,0.));
#24399=DIRECTION('ref_axis',(-1.,0.,0.));
#24400=DIRECTION('center_axis',(0.,0.,1.));
#24401=DIRECTION('ref_axis',(1.,0.,0.));
#24402=DIRECTION('',(1.,0.,0.));
#24403=DIRECTION('',(0.,1.,0.));
#24404=DIRECTION('',(-1.,0.,0.));
#24405=DIRECTION('center_axis',(-1.,0.,0.));
#24406=DIRECTION('ref_axis',(0.,0.,1.));
#24407=DIRECTION('',(0.,0.,1.));
#24408=DIRECTION('',(0.,1.,0.));
#24409=DIRECTION('',(0.,0.,1.));
#24410=DIRECTION('',(0.,1.,0.));
#24411=DIRECTION('center_axis',(0.,0.,1.));
#24412=DIRECTION('ref_axis',(1.,0.,0.));
#24413=DIRECTION('',(1.,0.,0.));
#24414=DIRECTION('',(1.,0.,0.));
#24415=DIRECTION('',(0.,1.,0.));
#24416=DIRECTION('center_axis',(-1.,0.,0.));
#24417=DIRECTION('ref_axis',(0.,0.,1.));
#24418=DIRECTION('',(0.,0.,1.));
#24419=DIRECTION('',(0.,0.,1.));
#24420=DIRECTION('',(0.,1.,0.));
#24421=DIRECTION('center_axis',(0.,0.,-1.));
#24422=DIRECTION('ref_axis',(-1.,0.,0.));
#24423=DIRECTION('',(-1.,0.,0.));
#24424=DIRECTION('',(-1.,0.,0.));
#24425=DIRECTION('',(0.,1.,0.));
#24426=DIRECTION('center_axis',(-1.,0.,0.));
#24427=DIRECTION('ref_axis',(0.,0.,1.));
#24428=DIRECTION('',(0.,0.,1.));
#24429=DIRECTION('',(0.,0.,1.));
#24430=DIRECTION('',(0.,1.,0.));
#24431=DIRECTION('center_axis',(-0.710721462348357,0.,0.703473526834815));
#24432=DIRECTION('ref_axis',(0.703473526834815,0.,0.710721462348357));
#24433=DIRECTION('',(0.703473526834815,0.,0.710721462348357));
#24434=DIRECTION('',(0.703473526834815,0.,0.710721462348357));
#24435=DIRECTION('center_axis',(1.22464679914735E-16,0.,-1.));
#24436=DIRECTION('ref_axis',(-1.,0.,-1.22464679914735E-16));
#24437=DIRECTION('',(-1.,0.,-1.22464679914735E-16));
#24438=DIRECTION('',(0.,1.,0.));
#24439=DIRECTION('',(-1.,0.,-1.22464679914735E-16));
#24440=DIRECTION('',(0.,1.,0.));
#24441=DIRECTION('center_axis',(0.,-1.,0.));
#24442=DIRECTION('ref_axis',(-1.,0.,-1.22464679914735E-16));
#24443=DIRECTION('center_axis',(0.,1.,0.));
#24444=DIRECTION('ref_axis',(-1.,0.,-1.22464679914735E-16));
#24445=DIRECTION('center_axis',(0.,1.,0.));
#24446=DIRECTION('ref_axis',(-1.,0.,-1.22464679914735E-16));
#24447=DIRECTION('',(0.,1.,0.));
#24448=DIRECTION('center_axis',(-1.,0.,2.6449522119078E-16));
#24449=DIRECTION('ref_axis',(2.6449522119078E-16,0.,1.));
#24450=DIRECTION('',(2.6449522119078E-16,0.,1.));
#24451=DIRECTION('',(2.6449522119078E-16,0.,1.));
#24452=DIRECTION('',(0.,1.,0.));
#24453=DIRECTION('center_axis',(0.,-1.,0.));
#24454=DIRECTION('ref_axis',(-1.22464679914735E-16,0.,1.));
#24455=DIRECTION('center_axis',(0.,1.,0.));
#24456=DIRECTION('ref_axis',(-1.22464679914735E-16,0.,1.));
#24457=DIRECTION('center_axis',(0.,1.,0.));
#24458=DIRECTION('ref_axis',(-1.22464679914735E-16,0.,1.));
#24459=DIRECTION('',(0.,1.,0.));
#24460=DIRECTION('center_axis',(-0.710721462348357,0.,-0.703473526834815));
#24461=DIRECTION('ref_axis',(-0.703473526834815,0.,0.710721462348357));
#24462=DIRECTION('',(-0.703473526834815,0.,0.710721462348357));
#24463=DIRECTION('',(0.,1.,0.));
#24464=DIRECTION('',(-0.703473526834815,0.,0.710721462348357));
#24465=DIRECTION('',(0.,1.,0.));
#24466=DIRECTION('center_axis',(-1.,0.,-1.22464679914735E-16));
#24467=DIRECTION('ref_axis',(-1.22464679914735E-16,0.,1.));
#24468=DIRECTION('',(-1.22464679914735E-16,0.,1.));
#24469=DIRECTION('',(-1.22464679914735E-16,0.,1.));
#24470=DIRECTION('',(0.,1.,0.));
#24471=DIRECTION('center_axis',(-1.22464679914735E-16,0.,1.));
#24472=DIRECTION('ref_axis',(1.,0.,1.22464679914735E-16));
#24473=DIRECTION('',(1.,0.,1.22464679914735E-16));
#24474=DIRECTION('',(1.,0.,1.22464679914735E-16));
#24475=DIRECTION('',(0.,1.,0.));
#24476=DIRECTION('center_axis',(-1.,0.,-1.22464679914735E-16));
#24477=DIRECTION('ref_axis',(-1.22464679914735E-16,0.,1.));
#24478=DIRECTION('',(-1.22464679914735E-16,0.,1.));
#24479=DIRECTION('',(-1.22464679914735E-16,0.,1.));
#24480=DIRECTION('',(0.,1.,0.));
#24481=DIRECTION('center_axis',(1.22464679914735E-16,0.,-1.));
#24482=DIRECTION('ref_axis',(-1.,0.,-1.22464679914735E-16));
#24483=DIRECTION('',(-1.,0.,-1.22464679914735E-16));
#24484=DIRECTION('',(-1.,0.,-1.22464679914735E-16));
#24485=DIRECTION('',(0.,1.,0.));
#24486=DIRECTION('center_axis',(-1.,0.,-1.22464679914735E-16));
#24487=DIRECTION('ref_axis',(-1.22464679914735E-16,0.,1.));
#24488=DIRECTION('',(-1.22464679914735E-16,0.,1.));
#24489=DIRECTION('',(-1.22464679914735E-16,0.,1.));
#24490=DIRECTION('',(0.,1.,0.));
#24491=DIRECTION('center_axis',(1.22464679914735E-16,0.,-1.));
#24492=DIRECTION('ref_axis',(-1.,0.,-1.22464679914735E-16));
#24493=DIRECTION('',(1.,0.,0.));
#24494=DIRECTION('',(-1.,0.,-1.22464679914735E-16));
#24495=DIRECTION('center_axis',(-1.22464679914735E-16,0.,1.));
#24496=DIRECTION('ref_axis',(1.,0.,1.22464679914735E-16));
#24497=DIRECTION('',(1.,0.,1.22464679914735E-16));
#24498=DIRECTION('',(-1.,0.,0.));
#24499=DIRECTION('',(0.,1.,0.));
#24500=DIRECTION('center_axis',(1.,0.,1.22464679914735E-16));
#24501=DIRECTION('ref_axis',(1.22464679914735E-16,0.,-1.));
#24502=DIRECTION('',(1.22464679914735E-16,0.,-1.));
#24503=DIRECTION('',(1.22464679914735E-16,0.,-1.));
#24504=DIRECTION('',(0.,1.,0.));
#24505=DIRECTION('center_axis',(-1.22464679914735E-16,0.,1.));
#24506=DIRECTION('ref_axis',(1.,0.,1.22464679914735E-16));
#24507=DIRECTION('',(1.,0.,1.22464679914735E-16));
#24508=DIRECTION('',(1.,0.,1.22464679914735E-16));
#24509=DIRECTION('',(0.,1.,0.));
#24510=DIRECTION('center_axis',(0.710721462348357,0.,0.703473526834815));
#24511=DIRECTION('ref_axis',(0.703473526834815,0.,-0.710721462348357));
#24512=DIRECTION('',(0.703473526834815,0.,-0.710721462348357));
#24513=DIRECTION('',(0.703473526834815,0.,-0.710721462348357));
#24514=DIRECTION('',(0.,1.,0.));
#24515=DIRECTION('center_axis',(0.,-1.,0.));
#24516=DIRECTION('ref_axis',(1.22464679914735E-16,0.,-1.));
#24517=DIRECTION('center_axis',(0.,1.,0.));
#24518=DIRECTION('ref_axis',(1.22464679914735E-16,0.,-1.));
#24519=DIRECTION('',(0.,1.,0.));
#24520=DIRECTION('center_axis',(0.,1.,0.));
#24521=DIRECTION('ref_axis',(1.22464679914735E-16,0.,-1.));
#24522=DIRECTION('center_axis',(1.,0.,3.15944630467493E-16));
#24523=DIRECTION('ref_axis',(3.15944630467493E-16,0.,-1.));
#24524=DIRECTION('',(3.15944630467493E-16,0.,-1.));
#24525=DIRECTION('',(0.,1.,0.));
#24526=DIRECTION('',(3.15944630467493E-16,0.,-1.));
#24527=DIRECTION('center_axis',(0.,-1.,0.));
#24528=DIRECTION('ref_axis',(1.,0.,1.78860330739173E-14));
#24529=DIRECTION('center_axis',(0.,1.,0.));
#24530=DIRECTION('ref_axis',(1.,0.,1.78860330739173E-14));
#24531=DIRECTION('',(0.,1.,0.));
#24532=DIRECTION('center_axis',(0.,1.,0.));
#24533=DIRECTION('ref_axis',(1.,0.,1.78860330739173E-14));
#24534=DIRECTION('center_axis',(-1.22464679914735E-16,0.,1.));
#24535=DIRECTION('ref_axis',(1.,0.,1.22464679914735E-16));
#24536=DIRECTION('',(1.,0.,1.22464679914735E-16));
#24537=DIRECTION('',(1.,0.,1.22464679914735E-16));
#24538=DIRECTION('center_axis',(1.22464679914735E-16,0.,-1.));
#24539=DIRECTION('ref_axis',(-1.,0.,-1.22464679914735E-16));
#24540=DIRECTION('',(-1.,0.,-1.22464679914735E-16));
#24541=DIRECTION('',(0.,1.,0.));
#24542=DIRECTION('',(-1.,0.,-1.22464679914735E-16));
#24543=DIRECTION('center_axis',(0.710721462348357,0.,-0.703473526834815));
#24544=DIRECTION('ref_axis',(-0.703473526834815,0.,-0.710721462348357));
#24545=DIRECTION('',(-0.703473526834815,0.,-0.710721462348357));
#24546=DIRECTION('',(0.,1.,0.));
#24547=DIRECTION('',(-0.703473526834815,0.,-0.710721462348357));
#24548=DIRECTION('center_axis',(1.,0.,1.22464679914735E-16));
#24549=DIRECTION('ref_axis',(1.22464679914735E-16,0.,-1.));
#24550=DIRECTION('',(1.22464679914735E-16,0.,-1.));
#24551=DIRECTION('',(0.,1.,0.));
#24552=DIRECTION('',(1.22464679914735E-16,0.,-1.));
#24553=DIRECTION('center_axis',(-1.22464679914735E-16,0.,1.));
#24554=DIRECTION('ref_axis',(1.,0.,1.22464679914735E-16));
#24555=DIRECTION('',(1.,0.,1.22464679914735E-16));
#24556=DIRECTION('',(0.,1.,0.));
#24557=DIRECTION('',(1.,0.,1.22464679914735E-16));
#24558=DIRECTION('center_axis',(1.,0.,1.22464679914735E-16));
#24559=DIRECTION('ref_axis',(1.22464679914735E-16,0.,-1.));
#24560=DIRECTION('',(1.22464679914735E-16,0.,-1.));
#24561=DIRECTION('',(0.,1.,0.));
#24562=DIRECTION('',(1.22464679914735E-16,0.,-1.));
#24563=DIRECTION('center_axis',(1.22464679914735E-16,0.,-1.));
#24564=DIRECTION('ref_axis',(-1.,0.,-1.22464679914735E-16));
#24565=DIRECTION('',(-1.,0.,-1.22464679914735E-16));
#24566=DIRECTION('',(0.,1.,0.));
#24567=DIRECTION('',(-1.,0.,-1.22464679914735E-16));
#24568=DIRECTION('center_axis',(1.,0.,1.22464679914735E-16));
#24569=DIRECTION('ref_axis',(1.22464679914735E-16,0.,-1.));
#24570=DIRECTION('',(1.22464679914735E-16,0.,-1.));
#24571=DIRECTION('',(0.,1.,0.));
#24572=DIRECTION('',(1.22464679914735E-16,0.,-1.));
#24573=DIRECTION('center_axis',(1.22464679914735E-16,0.,-1.));
#24574=DIRECTION('ref_axis',(-1.,0.,-1.22464679914735E-16));
#24575=DIRECTION('',(-1.,0.,-1.22464679914735E-16));
#24576=DIRECTION('',(0.,1.,0.));
#24577=DIRECTION('',(-1.,0.,-1.22464679914735E-16));
#24578=DIRECTION('center_axis',(0.,-1.,0.));
#24579=DIRECTION('ref_axis',(1.,0.,1.22464679914735E-16));
#24580=DIRECTION('center_axis',(0.,-1.,0.));
#24581=DIRECTION('ref_axis',(1.,0.,1.22464679914735E-16));
#24582=DIRECTION('',(0.,1.,0.));
#24583=DIRECTION('center_axis',(0.,-1.,0.));
#24584=DIRECTION('ref_axis',(1.,0.,1.22464679914735E-16));
#24585=DIRECTION('center_axis',(-1.,0.,-1.22464679914735E-16));
#24586=DIRECTION('ref_axis',(-1.22464679914735E-16,0.,1.));
#24587=DIRECTION('',(-1.22464679914735E-16,0.,1.));
#24588=DIRECTION('',(0.,1.,0.));
#24589=DIRECTION('',(-1.22464679914735E-16,0.,1.));
#24590=DIRECTION('center_axis',(-1.22464679914735E-16,0.,1.));
#24591=DIRECTION('ref_axis',(1.,0.,1.22464679914735E-16));
#24592=DIRECTION('',(1.,0.,1.22464679914735E-16));
#24593=DIRECTION('',(0.,1.,0.));
#24594=DIRECTION('',(1.,0.,1.22464679914735E-16));
#24595=DIRECTION('center_axis',(-1.,0.,-2.70193671200296E-15));
#24596=DIRECTION('ref_axis',(-2.70193671200296E-15,0.,1.));
#24597=DIRECTION('',(-2.70193671200296E-15,0.,1.));
#24598=DIRECTION('',(0.,1.,0.));
#24599=DIRECTION('',(-2.70193671200296E-15,0.,1.));
#24600=DIRECTION('center_axis',(2.14733784037198E-15,0.,1.));
#24601=DIRECTION('ref_axis',(1.,0.,-2.14733784037198E-15));
#24602=DIRECTION('',(1.,0.,-2.14733784037198E-15));
#24603=DIRECTION('',(0.,1.,0.));
#24604=DIRECTION('',(1.,0.,-2.14733784037198E-15));
#24605=DIRECTION('center_axis',(1.,0.,1.22464679914735E-16));
#24606=DIRECTION('ref_axis',(1.22464679914735E-16,0.,-1.));
#24607=DIRECTION('',(1.22464679914735E-16,0.,-1.));
#24608=DIRECTION('',(0.,1.,0.));
#24609=DIRECTION('',(1.22464679914735E-16,0.,-1.));
#24610=DIRECTION('center_axis',(-1.22464679914735E-16,0.,1.));
#24611=DIRECTION('ref_axis',(1.,0.,1.22464679914735E-16));
#24612=DIRECTION('',(1.,0.,1.22464679914735E-16));
#24613=DIRECTION('',(0.,1.,0.));
#24614=DIRECTION('',(1.,0.,1.22464679914735E-16));
#24615=DIRECTION('center_axis',(-0.710721462348357,0.,0.703473526834815));
#24616=DIRECTION('ref_axis',(0.703473526834815,0.,0.710721462348357));
#24617=DIRECTION('',(0.703473526834815,0.,0.710721462348357));
#24618=DIRECTION('',(0.,1.,0.));
#24619=DIRECTION('',(0.703473526834815,0.,0.710721462348357));
#24620=DIRECTION('center_axis',(1.22464679914735E-16,0.,-1.));
#24621=DIRECTION('ref_axis',(-1.,0.,-1.22464679914735E-16));
#24622=DIRECTION('',(-1.,0.,-1.22464679914735E-16));
#24623=DIRECTION('',(0.,1.,0.));
#24624=DIRECTION('',(-1.,0.,-1.22464679914735E-16));
#24625=DIRECTION('',(0.,1.,0.));
#24626=DIRECTION('center_axis',(0.,1.,0.));
#24627=DIRECTION('ref_axis',(-1.,0.,-1.22464679914735E-16));
#24628=DIRECTION('center_axis',(0.,-1.,0.));
#24629=DIRECTION('ref_axis',(-1.,0.,-1.22464679914735E-16));
#24630=DIRECTION('',(0.,1.,0.));
#24631=DIRECTION('center_axis',(0.,-1.,0.));
#24632=DIRECTION('ref_axis',(-1.,0.,-1.22464679914735E-16));
#24633=DIRECTION('center_axis',(1.,0.,5.0942458102025E-16));
#24634=DIRECTION('ref_axis',(5.0942458102025E-16,0.,-1.));
#24635=DIRECTION('',(5.0942458102025E-16,0.,-1.));
#24636=DIRECTION('',(0.,1.,0.));
#24637=DIRECTION('',(5.0942458102025E-16,0.,-1.));
#24638=DIRECTION('center_axis',(0.,1.,0.));
#24639=DIRECTION('ref_axis',(1.22464679914735E-16,0.,-1.));
#24640=DIRECTION('center_axis',(0.,-1.,0.));
#24641=DIRECTION('ref_axis',(1.22464679914735E-16,0.,-1.));
#24642=DIRECTION('',(0.,1.,0.));
#24643=DIRECTION('center_axis',(0.,-1.,0.));
#24644=DIRECTION('ref_axis',(1.22464679914735E-16,0.,-1.));
#24645=DIRECTION('center_axis',(0.710721462348357,0.,-0.703473526834815));
#24646=DIRECTION('ref_axis',(-0.703473526834815,0.,-0.710721462348357));
#24647=DIRECTION('',(-0.703473526834815,0.,-0.710721462348357));
#24648=DIRECTION('',(0.,1.,0.));
#24649=DIRECTION('',(-0.703473526834815,0.,-0.710721462348357));
#24650=DIRECTION('',(0.,1.,0.));
#24651=DIRECTION('center_axis',(1.,0.,1.22464679914735E-16));
#24652=DIRECTION('ref_axis',(1.22464679914735E-16,0.,-1.));
#24653=DIRECTION('',(1.22464679914735E-16,0.,-1.));
#24654=DIRECTION('',(0.,1.,0.));
#24655=DIRECTION('',(1.22464679914735E-16,0.,-1.));
#24656=DIRECTION('center_axis',(-1.22464679914735E-16,0.,1.));
#24657=DIRECTION('ref_axis',(1.,0.,1.22464679914735E-16));
#24658=DIRECTION('',(1.,0.,1.22464679914735E-16));
#24659=DIRECTION('',(0.,1.,0.));
#24660=DIRECTION('',(1.,0.,1.22464679914735E-16));
#24661=DIRECTION('center_axis',(1.,0.,1.22464679914735E-16));
#24662=DIRECTION('ref_axis',(1.22464679914735E-16,0.,-1.));
#24663=DIRECTION('',(1.22464679914735E-16,0.,-1.));
#24664=DIRECTION('',(0.,1.,0.));
#24665=DIRECTION('',(1.22464679914735E-16,0.,-1.));
#24666=DIRECTION('center_axis',(1.22464679914735E-16,0.,-1.));
#24667=DIRECTION('ref_axis',(-1.,0.,-1.22464679914735E-16));
#24668=DIRECTION('',(-1.,0.,-1.22464679914735E-16));
#24669=DIRECTION('',(0.,1.,0.));
#24670=DIRECTION('',(-1.,0.,-1.22464679914735E-16));
#24671=DIRECTION('center_axis',(1.,0.,1.22464679914735E-16));
#24672=DIRECTION('ref_axis',(1.22464679914735E-16,0.,-1.));
#24673=DIRECTION('',(1.22464679914735E-16,0.,-1.));
#24674=DIRECTION('',(0.,1.,0.));
#24675=DIRECTION('',(1.22464679914735E-16,0.,-1.));
#24676=DIRECTION('center_axis',(1.22464679914735E-16,0.,-1.));
#24677=DIRECTION('ref_axis',(-1.,0.,-1.22464679914735E-16));
#24678=DIRECTION('',(1.,0.,0.));
#24679=DIRECTION('',(-1.,0.,-1.22464679914735E-16));
#24680=DIRECTION('center_axis',(-1.22464679914735E-16,0.,1.));
#24681=DIRECTION('ref_axis',(1.,0.,1.22464679914735E-16));
#24682=DIRECTION('',(1.,0.,1.22464679914735E-16));
#24683=DIRECTION('',(0.,1.,0.));
#24684=DIRECTION('',(-1.,0.,0.));
#24685=DIRECTION('center_axis',(-1.,0.,-1.22464679914735E-16));
#24686=DIRECTION('ref_axis',(-1.22464679914735E-16,0.,1.));
#24687=DIRECTION('',(-1.22464679914735E-16,0.,1.));
#24688=DIRECTION('',(0.,1.,0.));
#24689=DIRECTION('',(-1.22464679914735E-16,0.,1.));
#24690=DIRECTION('center_axis',(-1.22464679914735E-16,0.,1.));
#24691=DIRECTION('ref_axis',(1.,0.,1.22464679914735E-16));
#24692=DIRECTION('',(1.,0.,1.22464679914735E-16));
#24693=DIRECTION('',(0.,1.,0.));
#24694=DIRECTION('',(1.,0.,1.22464679914735E-16));
#24695=DIRECTION('center_axis',(-0.710721462348357,0.,0.703473526834815));
#24696=DIRECTION('ref_axis',(0.703473526834815,0.,0.710721462348357));
#24697=DIRECTION('',(0.703473526834815,0.,0.710721462348357));
#24698=DIRECTION('',(0.,1.,0.));
#24699=DIRECTION('',(0.703473526834815,0.,0.710721462348357));
#24700=DIRECTION('center_axis',(-1.,0.,-1.22464679914735E-16));
#24701=DIRECTION('ref_axis',(-1.22464679914735E-16,0.,1.));
#24702=DIRECTION('',(1.22464679914735E-16,0.,-1.));
#24703=DIRECTION('',(-1.22464679914735E-16,0.,1.));
#24704=DIRECTION('center_axis',(0.,1.,0.));
#24705=DIRECTION('ref_axis',(-1.,0.,-1.22464679914735E-16));
#24706=DIRECTION('center_axis',(0.,-1.,0.));
#24707=DIRECTION('ref_axis',(-1.,0.,-1.22464679914735E-16));
#24708=DIRECTION('',(0.,-1.,0.));
#24709=DIRECTION('center_axis',(0.,1.,0.));
#24710=DIRECTION('ref_axis',(-1.,0.,-1.22464679914735E-16));
#24711=DIRECTION('center_axis',(1.,0.,1.22464679914735E-16));
#24712=DIRECTION('ref_axis',(1.22464679914735E-16,0.,-1.));
#24713=DIRECTION('',(1.22464679914735E-16,0.,-1.));
#24714=DIRECTION('',(0.,1.,0.));
#24715=DIRECTION('',(-1.22464679914735E-16,0.,1.));
#24716=DIRECTION('center_axis',(0.,1.,0.));
#24717=DIRECTION('ref_axis',(-1.22464679914735E-16,0.,1.));
#24718=DIRECTION('center_axis',(0.,-1.,0.));
#24719=DIRECTION('ref_axis',(-1.22464679914735E-16,0.,1.));
#24720=DIRECTION('center_axis',(0.,-1.,0.));
#24721=DIRECTION('ref_axis',(-1.22464679914735E-16,0.,1.));
#24722=DIRECTION('',(0.,1.,0.));
#24723=DIRECTION('center_axis',(-1.,0.,7.10152706380222E-17));
#24724=DIRECTION('ref_axis',(7.10152706380222E-17,0.,1.));
#24725=DIRECTION('',(7.10152706380222E-17,0.,1.));
#24726=DIRECTION('',(7.10152706380222E-17,0.,1.));
#24727=DIRECTION('',(0.,1.,0.));
#24728=DIRECTION('center_axis',(0.,1.,0.));
#24729=DIRECTION('ref_axis',(1.,0.,-1.76411037140878E-14));
#24730=DIRECTION('center_axis',(0.,-1.,0.));
#24731=DIRECTION('ref_axis',(1.,0.,-1.76411037140878E-14));
#24732=DIRECTION('center_axis',(0.,-1.,0.));
#24733=DIRECTION('ref_axis',(1.,0.,-1.76411037140878E-14));
#24734=DIRECTION('',(0.,1.,0.));
#24735=DIRECTION('center_axis',(-1.22464679914735E-16,0.,1.));
#24736=DIRECTION('ref_axis',(1.,0.,1.22464679914735E-16));
#24737=DIRECTION('',(1.,0.,1.22464679914735E-16));
#24738=DIRECTION('',(1.,0.,1.22464679914735E-16));
#24739=DIRECTION('center_axis',(1.22464679914735E-16,0.,-1.));
#24740=DIRECTION('ref_axis',(-1.,0.,-1.22464679914735E-16));
#24741=DIRECTION('',(-1.,0.,-1.22464679914735E-16));
#24742=DIRECTION('',(-1.,0.,-1.22464679914735E-16));
#24743=DIRECTION('',(0.,1.,0.));
#24744=DIRECTION('center_axis',(-0.710721462348357,0.,-0.703473526834815));
#24745=DIRECTION('ref_axis',(-0.703473526834815,0.,0.710721462348357));
#24746=DIRECTION('',(-0.703473526834815,0.,0.710721462348357));
#24747=DIRECTION('',(-0.703473526834815,0.,0.710721462348357));
#24748=DIRECTION('',(0.,1.,0.));
#24749=DIRECTION('center_axis',(-1.,0.,-1.22464679914735E-16));
#24750=DIRECTION('ref_axis',(-1.22464679914735E-16,0.,1.));
#24751=DIRECTION('',(-1.22464679914735E-16,0.,1.));
#24752=DIRECTION('',(-1.22464679914735E-16,0.,1.));
#24753=DIRECTION('',(0.,1.,0.));
#24754=DIRECTION('center_axis',(-1.22464679914735E-16,0.,1.));
#24755=DIRECTION('ref_axis',(1.,0.,1.22464679914735E-16));
#24756=DIRECTION('',(1.,0.,1.22464679914735E-16));
#24757=DIRECTION('',(1.,0.,1.22464679914735E-16));
#24758=DIRECTION('',(0.,1.,0.));
#24759=DIRECTION('center_axis',(-1.,0.,-1.22464679914735E-16));
#24760=DIRECTION('ref_axis',(-1.22464679914735E-16,0.,1.));
#24761=DIRECTION('',(-1.22464679914735E-16,0.,1.));
#24762=DIRECTION('',(-1.22464679914735E-16,0.,1.));
#24763=DIRECTION('',(0.,1.,0.));
#24764=DIRECTION('center_axis',(1.22464679914735E-16,0.,-1.));
#24765=DIRECTION('ref_axis',(-1.,0.,-1.22464679914735E-16));
#24766=DIRECTION('',(-1.,0.,-1.22464679914735E-16));
#24767=DIRECTION('',(-1.,0.,-1.22464679914735E-16));
#24768=DIRECTION('',(0.,1.,0.));
#24769=DIRECTION('center_axis',(-1.,0.,-1.22464679914735E-16));
#24770=DIRECTION('ref_axis',(-1.22464679914735E-16,0.,1.));
#24771=DIRECTION('',(-1.22464679914735E-16,0.,1.));
#24772=DIRECTION('',(-1.22464679914735E-16,0.,1.));
#24773=DIRECTION('',(0.,1.,0.));
#24774=DIRECTION('center_axis',(1.22464679914735E-16,0.,-1.));
#24775=DIRECTION('ref_axis',(-1.,0.,-1.22464679914735E-16));
#24776=DIRECTION('',(-1.,0.,-1.22464679914735E-16));
#24777=DIRECTION('',(-1.,0.,-1.22464679914735E-16));
#24778=DIRECTION('',(0.,1.,0.));
#24779=DIRECTION('center_axis',(0.,1.,0.));
#24780=DIRECTION('ref_axis',(1.,0.,1.22464679914735E-16));
#24781=DIRECTION('center_axis',(0.,1.,0.));
#24782=DIRECTION('ref_axis',(1.,0.,1.22464679914735E-16));
#24783=DIRECTION('center_axis',(0.,1.,0.));
#24784=DIRECTION('ref_axis',(1.,0.,1.22464679914735E-16));
#24785=DIRECTION('',(0.,1.,0.));
#24786=DIRECTION('center_axis',(1.,0.,1.22464679914735E-16));
#24787=DIRECTION('ref_axis',(1.22464679914735E-16,0.,-1.));
#24788=DIRECTION('',(1.22464679914735E-16,0.,-1.));
#24789=DIRECTION('',(1.22464679914735E-16,0.,-1.));
#24790=DIRECTION('',(0.,1.,0.));
#24791=DIRECTION('center_axis',(-1.22464679914735E-16,0.,1.));
#24792=DIRECTION('ref_axis',(1.,0.,1.22464679914735E-16));
#24793=DIRECTION('',(1.,0.,1.22464679914735E-16));
#24794=DIRECTION('',(1.,0.,1.22464679914735E-16));
#24795=DIRECTION('',(0.,1.,0.));
#24796=DIRECTION('center_axis',(1.,0.,-2.45700735217349E-15));
#24797=DIRECTION('ref_axis',(-2.45700735217349E-15,0.,-1.));
#24798=DIRECTION('',(-2.45700735217349E-15,0.,-1.));
#24799=DIRECTION('',(-2.45700735217349E-15,0.,-1.));
#24800=DIRECTION('',(0.,1.,0.));
#24801=DIRECTION('center_axis',(-2.39226720020145E-15,0.,1.));
#24802=DIRECTION('ref_axis',(1.,0.,2.39226720020145E-15));
#24803=DIRECTION('',(1.,0.,2.39226720020145E-15));
#24804=DIRECTION('',(1.,0.,2.39226720020145E-15));
#24805=DIRECTION('',(0.,1.,0.));
#24806=DIRECTION('center_axis',(-1.,0.,-1.22464679914735E-16));
#24807=DIRECTION('ref_axis',(-1.22464679914735E-16,0.,1.));
#24808=DIRECTION('',(-1.22464679914735E-16,0.,1.));
#24809=DIRECTION('',(-1.22464679914735E-16,0.,1.));
#24810=DIRECTION('',(0.,1.,0.));
#24811=DIRECTION('center_axis',(-1.22464679914735E-16,0.,1.));
#24812=DIRECTION('ref_axis',(1.,0.,1.22464679914735E-16));
#24813=DIRECTION('',(1.,0.,1.22464679914735E-16));
#24814=DIRECTION('',(1.,0.,1.22464679914735E-16));
#24815=DIRECTION('',(0.,1.,0.));
#24816=DIRECTION('center_axis',(0.710721462348356,0.,0.703473526834815));
#24817=DIRECTION('ref_axis',(0.703473526834815,0.,-0.710721462348356));
#24818=DIRECTION('',(0.703473526834815,0.,-0.710721462348356));
#24819=DIRECTION('',(0.703473526834815,0.,-0.710721462348356));
#24820=DIRECTION('center_axis',(-1.,0.,0.));
#24821=DIRECTION('ref_axis',(0.,0.,1.));
#24822=DIRECTION('',(0.,0.,1.));
#24823=DIRECTION('',(0.,1.,0.));
#24824=DIRECTION('',(0.,0.,1.));
#24825=DIRECTION('',(0.,1.,0.));
#24826=DIRECTION('center_axis',(0.,0.,1.));
#24827=DIRECTION('ref_axis',(1.,0.,0.));
#24828=DIRECTION('',(1.,0.,0.));
#24829=DIRECTION('',(0.,1.,0.));
#24830=DIRECTION('',(1.,0.,0.));
#24831=DIRECTION('center_axis',(-0.710721462348357,0.,0.703473526834815));
#24832=DIRECTION('ref_axis',(0.703473526834815,0.,0.710721462348357));
#24833=DIRECTION('',(0.703473526834815,0.,0.710721462348357));
#24834=DIRECTION('',(0.,1.,0.));
#24835=DIRECTION('',(0.703473526834815,0.,0.710721462348357));
#24836=DIRECTION('center_axis',(1.,0.,0.));
#24837=DIRECTION('ref_axis',(0.,0.,-1.));
#24838=DIRECTION('',(0.,0.,-1.));
#24839=DIRECTION('',(0.,1.,0.));
#24840=DIRECTION('',(0.,0.,-1.));
#24841=DIRECTION('',(0.,1.,0.));
#24842=DIRECTION('center_axis',(0.,0.,-1.));
#24843=DIRECTION('ref_axis',(-1.,0.,0.));
#24844=DIRECTION('',(-1.,0.,0.));
#24845=DIRECTION('',(-1.,0.,0.));
#24846=DIRECTION('',(0.,1.,0.));
#24847=DIRECTION('center_axis',(1.,0.,0.));
#24848=DIRECTION('ref_axis',(0.,0.,-1.));
#24849=DIRECTION('',(0.,0.,-1.));
#24850=DIRECTION('',(0.,0.,-1.));
#24851=DIRECTION('',(0.,1.,0.));
#24852=DIRECTION('center_axis',(0.,0.,1.));
#24853=DIRECTION('ref_axis',(1.,0.,0.));
#24854=DIRECTION('',(1.,0.,0.));
#24855=DIRECTION('',(1.,0.,0.));
#24856=DIRECTION('',(0.,1.,0.));
#24857=DIRECTION('center_axis',(1.,0.,0.));
#24858=DIRECTION('ref_axis',(0.,0.,-1.));
#24859=DIRECTION('',(0.,0.,-1.));
#24860=DIRECTION('',(0.,0.,-1.));
#24861=DIRECTION('',(0.,1.,0.));
#24862=DIRECTION('center_axis',(0.710721462348357,0.,-0.703473526834815));
#24863=DIRECTION('ref_axis',(-0.703473526834815,0.,-0.710721462348357));
#24864=DIRECTION('',(-0.703473526834815,0.,-0.710721462348357));
#24865=DIRECTION('',(-0.703473526834815,0.,-0.710721462348357));
#24866=DIRECTION('',(0.,1.,0.));
#24867=DIRECTION('center_axis',(0.,0.,-1.));
#24868=DIRECTION('ref_axis',(-1.,0.,0.));
#24869=DIRECTION('',(-1.,0.,0.));
#24870=DIRECTION('',(-1.,0.,0.));
#24871=DIRECTION('',(0.,1.,0.));
#24872=DIRECTION('center_axis',(-1.,0.,0.));
#24873=DIRECTION('ref_axis',(0.,0.,1.));
#24874=DIRECTION('',(0.,0.,1.));
#24875=DIRECTION('',(0.,0.,1.));
#24876=DIRECTION('',(0.,1.,0.));
#24877=DIRECTION('center_axis',(0.,0.,-1.));
#24878=DIRECTION('ref_axis',(-1.,0.,0.));
#24879=DIRECTION('',(-1.,0.,0.));
#24880=DIRECTION('',(-1.,0.,0.));
#24881=DIRECTION('',(0.,1.,0.));
#24882=DIRECTION('center_axis',(-0.710721462348357,0.,-0.703473526834815));
#24883=DIRECTION('ref_axis',(-0.703473526834815,0.,0.710721462348357));
#24884=DIRECTION('',(-0.703473526834815,0.,0.710721462348357));
#24885=DIRECTION('',(-0.703473526834815,0.,0.710721462348357));
#24886=DIRECTION('',(0.,1.,0.));
#24887=DIRECTION('center_axis',(0.,0.,1.));
#24888=DIRECTION('ref_axis',(1.,0.,0.));
#24889=DIRECTION('',(1.,0.,0.));
#24890=DIRECTION('',(-1.,0.,0.));
#24891=DIRECTION('',(0.,1.,0.));
#24892=DIRECTION('center_axis',(0.,0.,1.));
#24893=DIRECTION('ref_axis',(1.,0.,0.));
#24894=DIRECTION('',(-1.,0.,0.));
#24895=DIRECTION('',(0.,1.,0.));
#24896=DIRECTION('',(1.,0.,0.));
#24897=DIRECTION('center_axis',(1.,0.,0.));
#24898=DIRECTION('ref_axis',(0.,0.,-1.));
#24899=DIRECTION('',(0.,0.,-1.));
#24900=DIRECTION('',(0.,1.,0.));
#24901=DIRECTION('',(0.,0.,-1.));
#24902=DIRECTION('center_axis',(0.,0.,1.));
#24903=DIRECTION('ref_axis',(1.,0.,0.));
#24904=DIRECTION('',(1.,0.,0.));
#24905=DIRECTION('',(0.,1.,0.));
#24906=DIRECTION('',(1.,0.,0.));
#24907=DIRECTION('center_axis',(1.,0.,0.));
#24908=DIRECTION('ref_axis',(0.,0.,-1.));
#24909=DIRECTION('',(0.,0.,-1.));
#24910=DIRECTION('',(0.,1.,0.));
#24911=DIRECTION('',(0.,0.,-1.));
#24912=DIRECTION('center_axis',(0.,0.,-1.));
#24913=DIRECTION('ref_axis',(-1.,0.,0.));
#24914=DIRECTION('',(-1.,0.,0.));
#24915=DIRECTION('',(0.,1.,0.));
#24916=DIRECTION('',(-1.,0.,0.));
#24917=DIRECTION('center_axis',(1.,0.,0.));
#24918=DIRECTION('ref_axis',(0.,0.,-1.));
#24919=DIRECTION('',(0.,0.,-1.));
#24920=DIRECTION('',(0.,1.,0.));
#24921=DIRECTION('',(0.,0.,-1.));
#24922=DIRECTION('center_axis',(0.710721462348357,0.,0.703473526834815));
#24923=DIRECTION('ref_axis',(0.703473526834815,0.,-0.710721462348357));
#24924=DIRECTION('',(0.703473526834815,0.,-0.710721462348357));
#24925=DIRECTION('',(0.703473526834815,0.,-0.710721462348357));
#24926=DIRECTION('center_axis',(1.,0.,0.));
#24927=DIRECTION('ref_axis',(0.,0.,-1.));
#24928=DIRECTION('',(0.,0.,-1.));
#24929=DIRECTION('',(0.,1.,0.));
#24930=DIRECTION('',(0.,0.,-1.));
#24931=DIRECTION('',(0.,1.,0.));
#24932=DIRECTION('center_axis',(0.,0.,1.));
#24933=DIRECTION('ref_axis',(1.,0.,0.));
#24934=DIRECTION('',(1.,0.,0.));
#24935=DIRECTION('',(1.,0.,0.));
#24936=DIRECTION('',(0.,1.,0.));
#24937=DIRECTION('center_axis',(0.710721462348357,0.,0.703473526834815));
#24938=DIRECTION('ref_axis',(0.703473526834815,0.,-0.710721462348357));
#24939=DIRECTION('',(0.703473526834815,0.,-0.710721462348357));
#24940=DIRECTION('',(0.703473526834815,0.,-0.710721462348357));
#24941=DIRECTION('',(0.,1.,0.));
#24942=DIRECTION('center_axis',(1.,0.,0.));
#24943=DIRECTION('ref_axis',(0.,0.,-1.));
#24944=DIRECTION('',(0.,0.,1.));
#24945=DIRECTION('',(0.,0.,-1.));
#24946=DIRECTION('center_axis',(-1.,0.,0.));
#24947=DIRECTION('ref_axis',(0.,0.,1.));
#24948=DIRECTION('',(0.,0.,1.));
#24949=DIRECTION('',(0.,1.,0.));
#24950=DIRECTION('',(0.,0.,1.));
#24951=DIRECTION('',(0.,1.,0.));
#24952=DIRECTION('center_axis',(0.,0.,-1.));
#24953=DIRECTION('ref_axis',(-1.,0.,0.));
#24954=DIRECTION('',(-1.,0.,0.));
#24955=DIRECTION('',(0.,1.,0.));
#24956=DIRECTION('',(-1.,0.,0.));
#24957=DIRECTION('center_axis',(-1.,0.,0.));
#24958=DIRECTION('ref_axis',(0.,0.,1.));
#24959=DIRECTION('',(0.,0.,1.));
#24960=DIRECTION('',(0.,1.,0.));
#24961=DIRECTION('',(0.,0.,1.));
#24962=DIRECTION('center_axis',(0.,0.,1.));
#24963=DIRECTION('ref_axis',(1.,0.,0.));
#24964=DIRECTION('',(1.,0.,0.));
#24965=DIRECTION('',(0.,1.,0.));
#24966=DIRECTION('',(1.,0.,0.));
#24967=DIRECTION('center_axis',(-1.,0.,0.));
#24968=DIRECTION('ref_axis',(0.,0.,1.));
#24969=DIRECTION('',(0.,0.,1.));
#24970=DIRECTION('',(0.,1.,0.));
#24971=DIRECTION('',(0.,0.,1.));
#24972=DIRECTION('center_axis',(-0.710721462348357,0.,-0.703473526834815));
#24973=DIRECTION('ref_axis',(-0.703473526834815,0.,0.710721462348357));
#24974=DIRECTION('',(-0.703473526834815,0.,0.710721462348357));
#24975=DIRECTION('',(0.,1.,0.));
#24976=DIRECTION('',(-0.703473526834815,0.,0.710721462348357));
#24977=DIRECTION('center_axis',(0.,0.,-1.));
#24978=DIRECTION('ref_axis',(-1.,0.,0.));
#24979=DIRECTION('',(-1.,0.,0.));
#24980=DIRECTION('',(0.,1.,0.));
#24981=DIRECTION('',(1.,0.,0.));
#24982=DIRECTION('center_axis',(1.,0.,0.));
#24983=DIRECTION('ref_axis',(0.,0.,-1.));
#24984=DIRECTION('',(0.,0.,-1.));
#24985=DIRECTION('',(0.,1.,0.));
#24986=DIRECTION('',(0.,0.,-1.));
#24987=DIRECTION('center_axis',(0.,0.,-1.));
#24988=DIRECTION('ref_axis',(-1.,0.,0.));
#24989=DIRECTION('',(-1.,0.,0.));
#24990=DIRECTION('',(0.,1.,0.));
#24991=DIRECTION('',(-1.,0.,0.));
#24992=DIRECTION('center_axis',(0.710721462348357,0.,-0.703473526834815));
#24993=DIRECTION('ref_axis',(-0.703473526834815,0.,-0.710721462348357));
#24994=DIRECTION('',(-0.703473526834815,0.,-0.710721462348357));
#24995=DIRECTION('',(0.,1.,0.));
#24996=DIRECTION('',(-0.703473526834815,0.,-0.710721462348357));
#24997=DIRECTION('center_axis',(1.,0.,0.));
#24998=DIRECTION('ref_axis',(0.,0.,-1.));
#24999=DIRECTION('',(0.,0.,1.));
#25000=DIRECTION('',(0.,0.,-1.));
#25001=DIRECTION('center_axis',(0.,1.,0.));
#25002=DIRECTION('ref_axis',(1.,0.,0.));
#25003=DIRECTION('center_axis',(0.,1.,0.));
#25004=DIRECTION('ref_axis',(1.,0.,0.));
#25005=DIRECTION('',(0.,-1.,0.));
#25006=DIRECTION('center_axis',(0.,1.,0.));
#25007=DIRECTION('ref_axis',(-1.,0.,0.));
#25008=DIRECTION('center_axis',(0.,0.,1.));
#25009=DIRECTION('ref_axis',(1.,0.,0.));
#25010=DIRECTION('',(1.,0.,0.));
#25011=DIRECTION('',(0.,1.,0.));
#25012=DIRECTION('',(-1.,0.,0.));
#25013=DIRECTION('center_axis',(0.,0.,1.));
#25014=DIRECTION('ref_axis',(1.,0.,0.));
#25015=DIRECTION('',(-1.,0.,0.));
#25016=DIRECTION('',(1.,0.,0.));
#25017=DIRECTION('',(0.,1.,0.));
#25018=DIRECTION('center_axis',(-1.,0.,0.));
#25019=DIRECTION('ref_axis',(0.,0.,1.));
#25020=DIRECTION('',(0.,0.,1.));
#25021=DIRECTION('',(0.,0.,1.));
#25022=DIRECTION('',(0.,1.,0.));
#25023=DIRECTION('center_axis',(0.,0.,1.));
#25024=DIRECTION('ref_axis',(1.,0.,0.));
#25025=DIRECTION('',(1.,0.,0.));
#25026=DIRECTION('',(1.,0.,0.));
#25027=DIRECTION('',(0.,1.,0.));
#25028=DIRECTION('center_axis',(-1.,0.,0.));
#25029=DIRECTION('ref_axis',(0.,0.,1.));
#25030=DIRECTION('',(0.,0.,1.));
#25031=DIRECTION('',(0.,0.,1.));
#25032=DIRECTION('',(0.,1.,0.));
#25033=DIRECTION('center_axis',(0.,0.,-1.));
#25034=DIRECTION('ref_axis',(-1.,0.,0.));
#25035=DIRECTION('',(-1.,0.,0.));
#25036=DIRECTION('',(-1.,0.,0.));
#25037=DIRECTION('',(0.,1.,0.));
#25038=DIRECTION('center_axis',(-1.,0.,0.));
#25039=DIRECTION('ref_axis',(0.,0.,1.));
#25040=DIRECTION('',(0.,0.,1.));
#25041=DIRECTION('',(0.,0.,1.));
#25042=DIRECTION('',(0.,1.,0.));
#25043=DIRECTION('center_axis',(-0.710721462348357,0.,0.703473526834815));
#25044=DIRECTION('ref_axis',(0.703473526834815,0.,0.710721462348357));
#25045=DIRECTION('',(0.703473526834815,0.,0.710721462348357));
#25046=DIRECTION('',(0.703473526834815,0.,0.710721462348357));
#25047=DIRECTION('center_axis',(-1.,0.,0.));
#25048=DIRECTION('ref_axis',(0.,0.,1.));
#25049=DIRECTION('',(0.,0.,1.));
#25050=DIRECTION('',(0.,1.,0.));
#25051=DIRECTION('',(0.,0.,1.));
#25052=DIRECTION('',(0.,1.,0.));
#25053=DIRECTION('center_axis',(0.,0.,1.));
#25054=DIRECTION('ref_axis',(1.,0.,0.));
#25055=DIRECTION('',(1.,0.,0.));
#25056=DIRECTION('',(0.,1.,0.));
#25057=DIRECTION('',(1.,0.,0.));
#25058=DIRECTION('center_axis',(-0.710721462348357,0.,0.703473526834815));
#25059=DIRECTION('ref_axis',(0.703473526834815,0.,0.710721462348357));
#25060=DIRECTION('',(0.703473526834815,0.,0.710721462348357));
#25061=DIRECTION('',(0.,1.,0.));
#25062=DIRECTION('',(0.703473526834815,0.,0.710721462348357));
#25063=DIRECTION('center_axis',(1.,0.,0.));
#25064=DIRECTION('ref_axis',(0.,0.,-1.));
#25065=DIRECTION('',(0.,0.,-1.));
#25066=DIRECTION('',(0.,1.,0.));
#25067=DIRECTION('',(0.,0.,-1.));
#25068=DIRECTION('',(0.,1.,0.));
#25069=DIRECTION('center_axis',(0.,0.,-1.));
#25070=DIRECTION('ref_axis',(-1.,0.,0.));
#25071=DIRECTION('',(-1.,0.,0.));
#25072=DIRECTION('',(-1.,0.,0.));
#25073=DIRECTION('',(0.,1.,0.));
#25074=DIRECTION('center_axis',(1.,0.,0.));
#25075=DIRECTION('ref_axis',(0.,0.,-1.));
#25076=DIRECTION('',(0.,0.,-1.));
#25077=DIRECTION('',(0.,0.,-1.));
#25078=DIRECTION('',(0.,1.,0.));
#25079=DIRECTION('center_axis',(0.,0.,1.));
#25080=DIRECTION('ref_axis',(1.,0.,0.));
#25081=DIRECTION('',(1.,0.,0.));
#25082=DIRECTION('',(1.,0.,0.));
#25083=DIRECTION('',(0.,1.,0.));
#25084=DIRECTION('center_axis',(1.,0.,0.));
#25085=DIRECTION('ref_axis',(0.,0.,-1.));
#25086=DIRECTION('',(0.,0.,-1.));
#25087=DIRECTION('',(0.,0.,-1.));
#25088=DIRECTION('',(0.,1.,0.));
#25089=DIRECTION('center_axis',(0.710721462348357,0.,-0.703473526834815));
#25090=DIRECTION('ref_axis',(-0.703473526834815,0.,-0.710721462348357));
#25091=DIRECTION('',(-0.703473526834815,0.,-0.710721462348357));
#25092=DIRECTION('',(-0.703473526834815,0.,-0.710721462348357));
#25093=DIRECTION('',(0.,1.,0.));
#25094=DIRECTION('center_axis',(0.,0.,-1.));
#25095=DIRECTION('ref_axis',(-1.,0.,0.));
#25096=DIRECTION('',(-1.,0.,0.));
#25097=DIRECTION('',(-1.,0.,0.));
#25098=DIRECTION('',(0.,1.,0.));
#25099=DIRECTION('center_axis',(-1.,0.,0.));
#25100=DIRECTION('ref_axis',(0.,0.,1.));
#25101=DIRECTION('',(0.,0.,1.));
#25102=DIRECTION('',(0.,0.,1.));
#25103=DIRECTION('',(0.,1.,0.));
#25104=DIRECTION('center_axis',(0.,0.,-1.));
#25105=DIRECTION('ref_axis',(-1.,0.,0.));
#25106=DIRECTION('',(-1.,0.,0.));
#25107=DIRECTION('',(-1.,0.,0.));
#25108=DIRECTION('',(0.,1.,0.));
#25109=DIRECTION('center_axis',(-0.710721462348357,0.,-0.703473526834815));
#25110=DIRECTION('ref_axis',(-0.703473526834815,0.,0.710721462348357));
#25111=DIRECTION('',(-0.703473526834815,0.,0.710721462348357));
#25112=DIRECTION('',(-0.703473526834815,0.,0.710721462348357));
#25113=DIRECTION('',(0.,1.,0.));
#25114=DIRECTION('center_axis',(0.,0.,1.));
#25115=DIRECTION('ref_axis',(1.,0.,0.));
#25116=DIRECTION('',(1.,0.,0.));
#25117=DIRECTION('',(-1.,0.,0.));
#25118=DIRECTION('',(0.,1.,0.));
#25119=DIRECTION('center_axis',(0.,0.,1.));
#25120=DIRECTION('ref_axis',(1.,0.,0.));
#25121=DIRECTION('',(-1.,0.,0.));
#25122=DIRECTION('',(0.,1.,0.));
#25123=DIRECTION('',(1.,0.,0.));
#25124=DIRECTION('center_axis',(1.,0.,0.));
#25125=DIRECTION('ref_axis',(0.,0.,-1.));
#25126=DIRECTION('',(0.,0.,-1.));
#25127=DIRECTION('',(0.,1.,0.));
#25128=DIRECTION('',(0.,0.,-1.));
#25129=DIRECTION('center_axis',(0.,0.,1.));
#25130=DIRECTION('ref_axis',(1.,0.,0.));
#25131=DIRECTION('',(1.,0.,0.));
#25132=DIRECTION('',(0.,1.,0.));
#25133=DIRECTION('',(1.,0.,0.));
#25134=DIRECTION('center_axis',(1.,0.,0.));
#25135=DIRECTION('ref_axis',(0.,0.,-1.));
#25136=DIRECTION('',(0.,0.,-1.));
#25137=DIRECTION('',(0.,1.,0.));
#25138=DIRECTION('',(0.,0.,-1.));
#25139=DIRECTION('center_axis',(0.,0.,-1.));
#25140=DIRECTION('ref_axis',(-1.,0.,0.));
#25141=DIRECTION('',(-1.,0.,0.));
#25142=DIRECTION('',(0.,1.,0.));
#25143=DIRECTION('',(-1.,0.,0.));
#25144=DIRECTION('center_axis',(1.,0.,0.));
#25145=DIRECTION('ref_axis',(0.,0.,-1.));
#25146=DIRECTION('',(0.,0.,-1.));
#25147=DIRECTION('',(0.,1.,0.));
#25148=DIRECTION('',(0.,0.,-1.));
#25149=DIRECTION('center_axis',(0.710721462348357,0.,0.703473526834815));
#25150=DIRECTION('ref_axis',(0.703473526834815,0.,-0.710721462348357));
#25151=DIRECTION('',(0.703473526834815,0.,-0.710721462348357));
#25152=DIRECTION('',(0.703473526834815,0.,-0.710721462348357));
#25153=DIRECTION('center_axis',(1.,0.,0.));
#25154=DIRECTION('ref_axis',(0.,0.,-1.));
#25155=DIRECTION('',(0.,0.,-1.));
#25156=DIRECTION('',(0.,1.,0.));
#25157=DIRECTION('',(0.,0.,-1.));
#25158=DIRECTION('',(0.,1.,0.));
#25159=DIRECTION('center_axis',(0.,0.,1.));
#25160=DIRECTION('ref_axis',(1.,0.,0.));
#25161=DIRECTION('',(1.,0.,0.));
#25162=DIRECTION('',(1.,0.,0.));
#25163=DIRECTION('',(0.,1.,0.));
#25164=DIRECTION('center_axis',(0.710721462348357,0.,0.703473526834815));
#25165=DIRECTION('ref_axis',(0.703473526834815,0.,-0.710721462348357));
#25166=DIRECTION('',(0.703473526834815,0.,-0.710721462348357));
#25167=DIRECTION('',(0.703473526834815,0.,-0.710721462348357));
#25168=DIRECTION('',(0.,1.,0.));
#25169=DIRECTION('center_axis',(1.,0.,0.));
#25170=DIRECTION('ref_axis',(0.,0.,-1.));
#25171=DIRECTION('',(0.,0.,1.));
#25172=DIRECTION('',(0.,0.,-1.));
#25173=DIRECTION('center_axis',(-1.,0.,0.));
#25174=DIRECTION('ref_axis',(0.,0.,1.));
#25175=DIRECTION('',(0.,0.,1.));
#25176=DIRECTION('',(0.,1.,0.));
#25177=DIRECTION('',(0.,0.,1.));
#25178=DIRECTION('',(0.,1.,0.));
#25179=DIRECTION('center_axis',(0.,0.,-1.));
#25180=DIRECTION('ref_axis',(-1.,0.,0.));
#25181=DIRECTION('',(-1.,0.,0.));
#25182=DIRECTION('',(0.,1.,0.));
#25183=DIRECTION('',(-1.,0.,0.));
#25184=DIRECTION('center_axis',(-1.,0.,0.));
#25185=DIRECTION('ref_axis',(0.,0.,1.));
#25186=DIRECTION('',(0.,0.,1.));
#25187=DIRECTION('',(0.,1.,0.));
#25188=DIRECTION('',(0.,0.,1.));
#25189=DIRECTION('center_axis',(0.,0.,1.));
#25190=DIRECTION('ref_axis',(1.,0.,0.));
#25191=DIRECTION('',(1.,0.,0.));
#25192=DIRECTION('',(0.,1.,0.));
#25193=DIRECTION('',(1.,0.,0.));
#25194=DIRECTION('center_axis',(-1.,0.,0.));
#25195=DIRECTION('ref_axis',(0.,0.,1.));
#25196=DIRECTION('',(0.,0.,1.));
#25197=DIRECTION('',(0.,1.,0.));
#25198=DIRECTION('',(0.,0.,1.));
#25199=DIRECTION('center_axis',(-0.710721462348357,0.,-0.703473526834815));
#25200=DIRECTION('ref_axis',(-0.703473526834815,0.,0.710721462348357));
#25201=DIRECTION('',(-0.703473526834815,0.,0.710721462348357));
#25202=DIRECTION('',(0.,1.,0.));
#25203=DIRECTION('',(-0.703473526834815,0.,0.710721462348357));
#25204=DIRECTION('center_axis',(0.,0.,-1.));
#25205=DIRECTION('ref_axis',(-1.,0.,0.));
#25206=DIRECTION('',(-1.,0.,0.));
#25207=DIRECTION('',(0.,1.,0.));
#25208=DIRECTION('',(1.,0.,0.));
#25209=DIRECTION('center_axis',(1.,0.,0.));
#25210=DIRECTION('ref_axis',(0.,0.,-1.));
#25211=DIRECTION('',(0.,0.,-1.));
#25212=DIRECTION('',(0.,1.,0.));
#25213=DIRECTION('',(0.,0.,-1.));
#25214=DIRECTION('center_axis',(0.,0.,-1.));
#25215=DIRECTION('ref_axis',(-1.,0.,0.));
#25216=DIRECTION('',(-1.,0.,0.));
#25217=DIRECTION('',(0.,1.,0.));
#25218=DIRECTION('',(-1.,0.,0.));
#25219=DIRECTION('center_axis',(0.710721462348357,0.,-0.703473526834815));
#25220=DIRECTION('ref_axis',(-0.703473526834815,0.,-0.710721462348357));
#25221=DIRECTION('',(-0.703473526834815,0.,-0.710721462348357));
#25222=DIRECTION('',(0.,1.,0.));
#25223=DIRECTION('',(-0.703473526834815,0.,-0.710721462348357));
#25224=DIRECTION('center_axis',(1.,0.,0.));
#25225=DIRECTION('ref_axis',(0.,0.,-1.));
#25226=DIRECTION('',(0.,0.,1.));
#25227=DIRECTION('',(0.,0.,-1.));
#25228=DIRECTION('center_axis',(0.,1.,0.));
#25229=DIRECTION('ref_axis',(1.,0.,0.));
#25230=DIRECTION('center_axis',(0.,1.,0.));
#25231=DIRECTION('ref_axis',(1.,0.,0.));
#25232=DIRECTION('',(0.,-1.,0.));
#25233=DIRECTION('center_axis',(0.,1.,0.));
#25234=DIRECTION('ref_axis',(-1.,0.,0.));
#25235=DIRECTION('center_axis',(0.,0.,1.));
#25236=DIRECTION('ref_axis',(1.,0.,0.));
#25237=DIRECTION('',(1.,0.,0.));
#25238=DIRECTION('',(0.,1.,0.));
#25239=DIRECTION('',(-1.,0.,0.));
#25240=DIRECTION('center_axis',(0.,0.,1.));
#25241=DIRECTION('ref_axis',(1.,0.,0.));
#25242=DIRECTION('',(-1.,0.,0.));
#25243=DIRECTION('',(1.,0.,0.));
#25244=DIRECTION('',(0.,1.,0.));
#25245=DIRECTION('center_axis',(-1.,0.,0.));
#25246=DIRECTION('ref_axis',(0.,0.,1.));
#25247=DIRECTION('',(0.,0.,1.));
#25248=DIRECTION('',(0.,0.,1.));
#25249=DIRECTION('',(0.,1.,0.));
#25250=DIRECTION('center_axis',(0.,0.,1.));
#25251=DIRECTION('ref_axis',(1.,0.,0.));
#25252=DIRECTION('',(1.,0.,0.));
#25253=DIRECTION('',(1.,0.,0.));
#25254=DIRECTION('',(0.,1.,0.));
#25255=DIRECTION('center_axis',(-1.,0.,0.));
#25256=DIRECTION('ref_axis',(0.,0.,1.));
#25257=DIRECTION('',(0.,0.,1.));
#25258=DIRECTION('',(0.,0.,1.));
#25259=DIRECTION('',(0.,1.,0.));
#25260=DIRECTION('center_axis',(0.,0.,-1.));
#25261=DIRECTION('ref_axis',(-1.,0.,0.));
#25262=DIRECTION('',(-1.,0.,0.));
#25263=DIRECTION('',(-1.,0.,0.));
#25264=DIRECTION('',(0.,1.,0.));
#25265=DIRECTION('center_axis',(-1.,0.,0.));
#25266=DIRECTION('ref_axis',(0.,0.,1.));
#25267=DIRECTION('',(0.,0.,1.));
#25268=DIRECTION('',(0.,0.,1.));
#25269=DIRECTION('',(0.,1.,0.));
#25270=DIRECTION('center_axis',(-0.710721462348357,0.,0.703473526834815));
#25271=DIRECTION('ref_axis',(0.703473526834815,0.,0.710721462348357));
#25272=DIRECTION('',(0.703473526834815,0.,0.710721462348357));
#25273=DIRECTION('',(0.703473526834815,0.,0.710721462348357));
#25274=DIRECTION('center_axis',(0.,0.,1.));
#25275=DIRECTION('ref_axis',(1.,0.,0.));
#25276=DIRECTION('',(1.,0.,0.));
#25277=DIRECTION('',(0.,1.,0.));
#25278=DIRECTION('',(1.,0.,0.));
#25279=DIRECTION('',(0.,1.,0.));
#25280=DIRECTION('center_axis',(0.,-1.,0.));
#25281=DIRECTION('ref_axis',(1.,0.,0.));
#25282=DIRECTION('center_axis',(0.,1.,0.));
#25283=DIRECTION('ref_axis',(1.,0.,0.));
#25284=DIRECTION('center_axis',(0.,1.,0.));
#25285=DIRECTION('ref_axis',(1.,0.,0.));
#25286=DIRECTION('',(0.,1.,0.));
#25287=DIRECTION('center_axis',(1.,0.,-3.86959901105515E-16));
#25288=DIRECTION('ref_axis',(-3.86959901105515E-16,0.,-1.));
#25289=DIRECTION('',(-3.86959901105515E-16,0.,-1.));
#25290=DIRECTION('',(-3.86959901105515E-16,0.,-1.));
#25291=DIRECTION('',(0.,1.,0.));
#25292=DIRECTION('center_axis',(0.,-1.,0.));
#25293=DIRECTION('ref_axis',(0.,0.,-1.));
#25294=DIRECTION('center_axis',(0.,1.,0.));
#25295=DIRECTION('ref_axis',(0.,0.,-1.));
#25296=DIRECTION('center_axis',(0.,1.,0.));
#25297=DIRECTION('ref_axis',(0.,0.,-1.));
#25298=DIRECTION('',(0.,1.,0.));
#25299=DIRECTION('center_axis',(0.710721462348357,0.,0.703473526834815));
#25300=DIRECTION('ref_axis',(0.703473526834815,0.,-0.710721462348357));
#25301=DIRECTION('',(0.703473526834815,0.,-0.710721462348357));
#25302=DIRECTION('',(0.,1.,0.));
#25303=DIRECTION('',(0.703473526834815,0.,-0.710721462348357));
#25304=DIRECTION('',(0.,1.,0.));
#25305=DIRECTION('center_axis',(1.,0.,0.));
#25306=DIRECTION('ref_axis',(0.,0.,-1.));
#25307=DIRECTION('',(0.,0.,-1.));
#25308=DIRECTION('',(0.,0.,-1.));
#25309=DIRECTION('',(0.,1.,0.));
#25310=DIRECTION('center_axis',(0.,0.,-1.));
#25311=DIRECTION('ref_axis',(-1.,0.,0.));
#25312=DIRECTION('',(-1.,0.,0.));
#25313=DIRECTION('',(-1.,0.,0.));
#25314=DIRECTION('',(0.,1.,0.));
#25315=DIRECTION('center_axis',(1.,0.,0.));
#25316=DIRECTION('ref_axis',(0.,0.,-1.));
#25317=DIRECTION('',(0.,0.,-1.));
#25318=DIRECTION('',(0.,0.,-1.));
#25319=DIRECTION('',(0.,1.,0.));
#25320=DIRECTION('center_axis',(0.,0.,1.));
#25321=DIRECTION('ref_axis',(1.,0.,0.));
#25322=DIRECTION('',(1.,0.,0.));
#25323=DIRECTION('',(1.,0.,0.));
#25324=DIRECTION('',(0.,1.,0.));
#25325=DIRECTION('center_axis',(1.,0.,0.));
#25326=DIRECTION('ref_axis',(0.,0.,-1.));
#25327=DIRECTION('',(0.,0.,-1.));
#25328=DIRECTION('',(0.,0.,-1.));
#25329=DIRECTION('',(0.,1.,0.));
#25330=DIRECTION('center_axis',(0.,0.,1.));
#25331=DIRECTION('ref_axis',(1.,0.,0.));
#25332=DIRECTION('',(-1.,0.,0.));
#25333=DIRECTION('',(1.,0.,0.));
#25334=DIRECTION('center_axis',(0.,0.,-1.));
#25335=DIRECTION('ref_axis',(-1.,0.,0.));
#25336=DIRECTION('',(-1.,0.,0.));
#25337=DIRECTION('',(1.,0.,0.));
#25338=DIRECTION('',(0.,1.,0.));
#25339=DIRECTION('center_axis',(-1.,0.,0.));
#25340=DIRECTION('ref_axis',(0.,0.,1.));
#25341=DIRECTION('',(0.,0.,1.));
#25342=DIRECTION('',(0.,0.,1.));
#25343=DIRECTION('',(0.,1.,0.));
#25344=DIRECTION('center_axis',(0.,0.,-1.));
#25345=DIRECTION('ref_axis',(-1.,0.,0.));
#25346=DIRECTION('',(-1.,0.,0.));
#25347=DIRECTION('',(-1.,0.,0.));
#25348=DIRECTION('',(0.,1.,0.));
#25349=DIRECTION('center_axis',(-0.710721462348357,0.,-0.703473526834815));
#25350=DIRECTION('ref_axis',(-0.703473526834815,0.,0.710721462348357));
#25351=DIRECTION('',(-0.703473526834815,0.,0.710721462348357));
#25352=DIRECTION('',(-0.703473526834815,0.,0.710721462348357));
#25353=DIRECTION('',(0.,1.,0.));
#25354=DIRECTION('center_axis',(0.,-1.,0.));
#25355=DIRECTION('ref_axis',(0.,0.,1.));
#25356=DIRECTION('center_axis',(0.,1.,0.));
#25357=DIRECTION('ref_axis',(0.,0.,1.));
#25358=DIRECTION('',(0.,1.,0.));
#25359=DIRECTION('center_axis',(0.,1.,0.));
#25360=DIRECTION('ref_axis',(0.,0.,1.));
#25361=DIRECTION('center_axis',(-1.,0.,-1.93479950552757E-16));
#25362=DIRECTION('ref_axis',(-1.93479950552757E-16,0.,1.));
#25363=DIRECTION('',(-1.93479950552757E-16,0.,1.));
#25364=DIRECTION('',(0.,1.,0.));
#25365=DIRECTION('',(-1.93479950552757E-16,0.,1.));
#25366=DIRECTION('center_axis',(0.,-1.,0.));
#25367=DIRECTION('ref_axis',(-1.,0.,-1.77635683940026E-14));
#25368=DIRECTION('center_axis',(0.,1.,0.));
#25369=DIRECTION('ref_axis',(-1.,0.,-1.77635683940026E-14));
#25370=DIRECTION('',(0.,1.,0.));
#25371=DIRECTION('center_axis',(0.,1.,0.));
#25372=DIRECTION('ref_axis',(-1.,0.,-1.77635683940026E-14));
#25373=DIRECTION('center_axis',(0.,0.,-1.));
#25374=DIRECTION('ref_axis',(-1.,0.,0.));
#25375=DIRECTION('',(-1.,0.,0.));
#25376=DIRECTION('',(-1.,0.,0.));
#25377=DIRECTION('center_axis',(0.,0.,1.));
#25378=DIRECTION('ref_axis',(1.,0.,0.));
#25379=DIRECTION('',(1.,0.,0.));
#25380=DIRECTION('',(0.,1.,0.));
#25381=DIRECTION('',(1.,0.,0.));
#25382=DIRECTION('center_axis',(-0.710721462348357,0.,0.703473526834815));
#25383=DIRECTION('ref_axis',(0.703473526834815,0.,0.710721462348357));
#25384=DIRECTION('',(0.703473526834815,0.,0.710721462348357));
#25385=DIRECTION('',(0.,1.,0.));
#25386=DIRECTION('',(0.703473526834815,0.,0.710721462348357));
#25387=DIRECTION('center_axis',(-1.,0.,0.));
#25388=DIRECTION('ref_axis',(0.,0.,1.));
#25389=DIRECTION('',(0.,0.,1.));
#25390=DIRECTION('',(0.,1.,0.));
#25391=DIRECTION('',(0.,0.,1.));
#25392=DIRECTION('center_axis',(0.,0.,-1.));
#25393=DIRECTION('ref_axis',(-1.,0.,0.));
#25394=DIRECTION('',(-1.,0.,0.));
#25395=DIRECTION('',(0.,1.,0.));
#25396=DIRECTION('',(-1.,0.,0.));
#25397=DIRECTION('center_axis',(-1.,0.,0.));
#25398=DIRECTION('ref_axis',(0.,0.,1.));
#25399=DIRECTION('',(0.,0.,1.));
#25400=DIRECTION('',(0.,1.,0.));
#25401=DIRECTION('',(0.,0.,1.));
#25402=DIRECTION('center_axis',(0.,0.,1.));
#25403=DIRECTION('ref_axis',(1.,0.,0.));
#25404=DIRECTION('',(1.,0.,0.));
#25405=DIRECTION('',(0.,1.,0.));
#25406=DIRECTION('',(1.,0.,0.));
#25407=DIRECTION('center_axis',(-1.,0.,0.));
#25408=DIRECTION('ref_axis',(0.,0.,1.));
#25409=DIRECTION('',(0.,0.,1.));
#25410=DIRECTION('',(0.,1.,0.));
#25411=DIRECTION('',(0.,0.,1.));
#25412=DIRECTION('center_axis',(0.,0.,1.));
#25413=DIRECTION('ref_axis',(1.,0.,0.));
#25414=DIRECTION('',(1.,0.,0.));
#25415=DIRECTION('',(0.,1.,0.));
#25416=DIRECTION('',(1.,0.,0.));
#25417=DIRECTION('center_axis',(0.,-1.,0.));
#25418=DIRECTION('ref_axis',(-1.,0.,0.));
#25419=DIRECTION('center_axis',(0.,-1.,0.));
#25420=DIRECTION('ref_axis',(-1.,0.,0.));
#25421=DIRECTION('',(0.,1.,0.));
#25422=DIRECTION('center_axis',(0.,-1.,0.));
#25423=DIRECTION('ref_axis',(-1.,0.,0.));
#25424=DIRECTION('center_axis',(1.,0.,0.));
#25425=DIRECTION('ref_axis',(0.,0.,-1.));
#25426=DIRECTION('',(0.,0.,-1.));
#25427=DIRECTION('',(0.,1.,0.));
#25428=DIRECTION('',(0.,0.,-1.));
#25429=DIRECTION('center_axis',(0.,0.,-1.));
#25430=DIRECTION('ref_axis',(-1.,0.,0.));
#25431=DIRECTION('',(-1.,0.,0.));
#25432=DIRECTION('',(0.,1.,0.));
#25433=DIRECTION('',(-1.,0.,0.));
#25434=DIRECTION('center_axis',(1.,0.,2.57947203208822E-15));
#25435=DIRECTION('ref_axis',(2.57947203208822E-15,0.,-1.));
#25436=DIRECTION('',(2.57947203208822E-15,0.,-1.));
#25437=DIRECTION('',(0.,1.,0.));
#25438=DIRECTION('',(2.57947203208822E-15,0.,-1.));
#25439=DIRECTION('center_axis',(-2.26980252028671E-15,0.,-1.));
#25440=DIRECTION('ref_axis',(-1.,0.,2.26980252028671E-15));
#25441=DIRECTION('',(-1.,0.,2.26980252028671E-15));
#25442=DIRECTION('',(0.,1.,0.));
#25443=DIRECTION('',(-1.,0.,2.26980252028671E-15));
#25444=DIRECTION('center_axis',(-1.,0.,0.));
#25445=DIRECTION('ref_axis',(0.,0.,1.));
#25446=DIRECTION('',(0.,0.,1.));
#25447=DIRECTION('',(0.,1.,0.));
#25448=DIRECTION('',(0.,0.,1.));
#25449=DIRECTION('center_axis',(0.,0.,-1.));
#25450=DIRECTION('ref_axis',(-1.,0.,0.));
#25451=DIRECTION('',(-1.,0.,0.));
#25452=DIRECTION('',(0.,1.,0.));
#25453=DIRECTION('',(-1.,0.,0.));
#25454=DIRECTION('center_axis',(0.710721462348357,0.,-0.703473526834815));
#25455=DIRECTION('ref_axis',(-0.703473526834815,0.,-0.710721462348357));
#25456=DIRECTION('',(-0.703473526834815,0.,-0.710721462348357));
#25457=DIRECTION('',(0.,1.,0.));
#25458=DIRECTION('',(-0.703473526834815,0.,-0.710721462348357));
#25459=DIRECTION('center_axis',(0.,1.,0.));
#25460=DIRECTION('ref_axis',(1.,0.,0.));
#25461=DIRECTION('',(-1.,0.,0.));
#25462=DIRECTION('',(0.,0.,1.));
#25463=DIRECTION('',(1.,0.,0.));
#25464=DIRECTION('',(0.,0.,1.));
#25465=DIRECTION('',(-1.,0.,0.));
#25466=DIRECTION('',(0.,0.,1.));
#25467=DIRECTION('',(0.703473526834815,0.,0.710721462348357));
#25468=DIRECTION('',(1.,0.,0.));
#25469=DIRECTION('',(0.703473526834815,0.,-0.710721462348357));
#25470=DIRECTION('',(0.,0.,-1.));
#25471=DIRECTION('',(-1.,0.,0.));
#25472=DIRECTION('',(0.,0.,-1.));
#25473=DIRECTION('',(1.,0.,0.));
#25474=DIRECTION('',(0.,0.,-1.));
#25475=DIRECTION('',(1.,0.,0.));
#25476=DIRECTION('center_axis',(0.,1.,0.));
#25477=DIRECTION('ref_axis',(-1.,0.,0.));
#25478=DIRECTION('',(0.,0.,1.));
#25479=DIRECTION('',(-1.,0.,0.));
#25480=DIRECTION('',(2.57947203208822E-15,0.,1.));
#25481=DIRECTION('',(-1.,0.,-2.26980252028671E-15));
#25482=DIRECTION('',(0.,0.,-1.));
#25483=DIRECTION('',(-1.,0.,0.));
#25484=DIRECTION('',(-0.703473526834815,0.,0.710721462348357));
#25485=DIRECTION('',(0.,0.,1.));
#25486=DIRECTION('',(0.,0.,1.));
#25487=DIRECTION('',(-0.703473526834815,0.,-0.710721462348357));
#25488=DIRECTION('',(-1.,0.,0.));
#25489=DIRECTION('',(0.,0.,-1.));
#25490=DIRECTION('',(-1.,0.,0.));
#25491=DIRECTION('center_axis',(0.,-1.,0.));
#25492=DIRECTION('ref_axis',(0.,0.,1.));
#25493=DIRECTION('',(-3.86959901105515E-16,0.,1.));
#25494=DIRECTION('center_axis',(0.,-1.,0.));
#25495=DIRECTION('ref_axis',(1.,0.,0.));
#25496=DIRECTION('',(1.,0.,0.));
#25497=DIRECTION('center_axis',(0.,-1.,0.));
#25498=DIRECTION('ref_axis',(0.,0.,-1.));
#25499=DIRECTION('',(-1.93479950552757E-16,0.,-1.));
#25500=DIRECTION('center_axis',(0.,-1.,0.));
#25501=DIRECTION('ref_axis',(-1.,0.,1.77635683940026E-14));
#25502=DIRECTION('',(-1.,0.,0.));
#25503=DIRECTION('center_axis',(0.,1.,0.));
#25504=DIRECTION('ref_axis',(1.,0.,0.));
#25505=DIRECTION('center_axis',(0.,0.,1.));
#25506=DIRECTION('ref_axis',(1.,0.,0.));
#25507=DIRECTION('',(0.,1.,0.));
#25508=DIRECTION('',(1.,0.,0.));
#25509=DIRECTION('',(0.,1.,0.));
#25510=DIRECTION('center_axis',(0.,1.,0.));
#25511=DIRECTION('ref_axis',(1.,0.,0.));
#25512=DIRECTION('',(0.,1.,0.));
#25513=DIRECTION('center_axis',(0.,-1.,0.));
#25514=DIRECTION('ref_axis',(1.,0.,0.));
#25515=DIRECTION('center_axis',(-1.,0.,-3.86959901105515E-16));
#25516=DIRECTION('ref_axis',(-3.86959901105515E-16,0.,1.));
#25517=DIRECTION('',(0.,1.,0.));
#25518=DIRECTION('',(-3.86959901105515E-16,0.,1.));
#25519=DIRECTION('center_axis',(0.,1.,0.));
#25520=DIRECTION('ref_axis',(0.,0.,1.));
#25521=DIRECTION('',(0.,1.,0.));
#25522=DIRECTION('center_axis',(0.,-1.,0.));
#25523=DIRECTION('ref_axis',(0.,0.,1.));
#25524=DIRECTION('center_axis',(-0.710721462348357,0.,0.703473526834815));
#25525=DIRECTION('ref_axis',(0.703473526834815,0.,0.710721462348357));
#25526=DIRECTION('',(0.,1.,0.));
#25527=DIRECTION('',(0.703473526834815,0.,0.710721462348357));
#25528=DIRECTION('',(0.,1.,0.));
#25529=DIRECTION('center_axis',(-1.,0.,0.));
#25530=DIRECTION('ref_axis',(0.,0.,1.));
#25531=DIRECTION('',(0.,1.,0.));
#25532=DIRECTION('',(0.,0.,1.));
#25533=DIRECTION('center_axis',(0.,0.,-1.));
#25534=DIRECTION('ref_axis',(-1.,0.,0.));
#25535=DIRECTION('',(0.,1.,0.));
#25536=DIRECTION('',(-1.,0.,0.));
#25537=DIRECTION('center_axis',(-1.,0.,0.));
#25538=DIRECTION('ref_axis',(0.,0.,1.));
#25539=DIRECTION('',(0.,1.,0.));
#25540=DIRECTION('',(0.,0.,1.));
#25541=DIRECTION('center_axis',(0.,0.,1.));
#25542=DIRECTION('ref_axis',(1.,0.,0.));
#25543=DIRECTION('',(0.,1.,0.));
#25544=DIRECTION('',(1.,0.,0.));
#25545=DIRECTION('center_axis',(-1.,0.,0.));
#25546=DIRECTION('ref_axis',(0.,0.,1.));
#25547=DIRECTION('',(0.,1.,0.));
#25548=DIRECTION('',(0.,0.,1.));
#25549=DIRECTION('center_axis',(0.,0.,1.));
#25550=DIRECTION('ref_axis',(1.,0.,0.));
#25551=DIRECTION('',(1.,0.,0.));
#25552=DIRECTION('center_axis',(0.,0.,-1.));
#25553=DIRECTION('ref_axis',(-1.,0.,0.));
#25554=DIRECTION('',(0.,1.,0.));
#25555=DIRECTION('',(1.,0.,0.));
#25556=DIRECTION('center_axis',(1.,0.,0.));
#25557=DIRECTION('ref_axis',(0.,0.,-1.));
#25558=DIRECTION('',(0.,1.,0.));
#25559=DIRECTION('',(0.,0.,-1.));
#25560=DIRECTION('center_axis',(0.,0.,-1.));
#25561=DIRECTION('ref_axis',(-1.,0.,0.));
#25562=DIRECTION('',(0.,1.,0.));
#25563=DIRECTION('',(-1.,0.,0.));
#25564=DIRECTION('center_axis',(0.710721462348357,0.,-0.703473526834815));
#25565=DIRECTION('ref_axis',(-0.703473526834815,0.,-0.710721462348357));
#25566=DIRECTION('',(0.,1.,0.));
#25567=DIRECTION('',(-0.703473526834815,0.,-0.710721462348357));
#25568=DIRECTION('center_axis',(1.,0.,0.));
#25569=DIRECTION('ref_axis',(0.,0.,-1.));
#25570=DIRECTION('',(0.,0.,-1.));
#25571=DIRECTION('center_axis',(0.,1.,0.));
#25572=DIRECTION('ref_axis',(1.,0.,0.));
#25573=DIRECTION('center_axis',(0.,-1.,0.));
#25574=DIRECTION('ref_axis',(1.,0.,0.));
#25575=DIRECTION('',(0.,-1.,0.));
#25576=DIRECTION('center_axis',(-1.,0.,0.));
#25577=DIRECTION('ref_axis',(0.,0.,1.));
#25578=DIRECTION('',(0.,1.,0.));
#25579=DIRECTION('',(0.,0.,-1.));
#25580=DIRECTION('center_axis',(0.,1.,0.));
#25581=DIRECTION('ref_axis',(0.,0.,-1.));
#25582=DIRECTION('center_axis',(0.,-1.,0.));
#25583=DIRECTION('ref_axis',(0.,0.,-1.));
#25584=DIRECTION('',(0.,1.,0.));
#25585=DIRECTION('center_axis',(1.,0.,-1.93479950552757E-16));
#25586=DIRECTION('ref_axis',(-1.93479950552757E-16,0.,-1.));
#25587=DIRECTION('',(-1.93479950552757E-16,0.,-1.));
#25588=DIRECTION('',(0.,1.,0.));
#25589=DIRECTION('center_axis',(0.,1.,0.));
#25590=DIRECTION('ref_axis',(-1.,0.,1.77635683940026E-14));
#25591=DIRECTION('center_axis',(0.,-1.,0.));
#25592=DIRECTION('ref_axis',(-1.,0.,1.77635683940026E-14));
#25593=DIRECTION('',(0.,1.,0.));
#25594=DIRECTION('center_axis',(0.,0.,-1.));
#25595=DIRECTION('ref_axis',(-1.,0.,0.));
#25596=DIRECTION('',(-1.,0.,0.));
#25597=DIRECTION('center_axis',(0.,0.,1.));
#25598=DIRECTION('ref_axis',(1.,0.,0.));
#25599=DIRECTION('',(1.,0.,0.));
#25600=DIRECTION('',(0.,1.,0.));
#25601=DIRECTION('center_axis',(0.710721462348357,0.,0.703473526834815));
#25602=DIRECTION('ref_axis',(0.703473526834815,0.,-0.710721462348357));
#25603=DIRECTION('',(0.703473526834815,0.,-0.710721462348357));
#25604=DIRECTION('',(0.,1.,0.));
#25605=DIRECTION('center_axis',(1.,0.,0.));
#25606=DIRECTION('ref_axis',(0.,0.,-1.));
#25607=DIRECTION('',(0.,0.,-1.));
#25608=DIRECTION('',(0.,1.,0.));
#25609=DIRECTION('center_axis',(0.,0.,-1.));
#25610=DIRECTION('ref_axis',(-1.,0.,0.));
#25611=DIRECTION('',(-1.,0.,0.));
#25612=DIRECTION('',(0.,1.,0.));
#25613=DIRECTION('center_axis',(1.,0.,0.));
#25614=DIRECTION('ref_axis',(0.,0.,-1.));
#25615=DIRECTION('',(0.,0.,-1.));
#25616=DIRECTION('',(0.,1.,0.));
#25617=DIRECTION('center_axis',(0.,0.,1.));
#25618=DIRECTION('ref_axis',(1.,0.,0.));
#25619=DIRECTION('',(1.,0.,0.));
#25620=DIRECTION('',(0.,1.,0.));
#25621=DIRECTION('center_axis',(1.,0.,0.));
#25622=DIRECTION('ref_axis',(0.,0.,-1.));
#25623=DIRECTION('',(0.,0.,-1.));
#25624=DIRECTION('',(0.,1.,0.));
#25625=DIRECTION('center_axis',(0.,0.,1.));
#25626=DIRECTION('ref_axis',(1.,0.,0.));
#25627=DIRECTION('',(1.,0.,0.));
#25628=DIRECTION('',(0.,1.,0.));
#25629=DIRECTION('center_axis',(0.,1.,0.));
#25630=DIRECTION('ref_axis',(-1.,0.,0.));
#25631=DIRECTION('center_axis',(0.,1.,0.));
#25632=DIRECTION('ref_axis',(-1.,0.,0.));
#25633=DIRECTION('',(0.,1.,0.));
#25634=DIRECTION('center_axis',(-1.,0.,0.));
#25635=DIRECTION('ref_axis',(0.,0.,1.));
#25636=DIRECTION('',(0.,0.,1.));
#25637=DIRECTION('',(0.,1.,0.));
#25638=DIRECTION('center_axis',(0.,0.,-1.));
#25639=DIRECTION('ref_axis',(-1.,0.,0.));
#25640=DIRECTION('',(-1.,0.,0.));
#25641=DIRECTION('',(0.,1.,0.));
#25642=DIRECTION('center_axis',(-1.,0.,2.57947203208822E-15));
#25643=DIRECTION('ref_axis',(2.57947203208822E-15,0.,1.));
#25644=DIRECTION('',(2.57947203208822E-15,0.,1.));
#25645=DIRECTION('',(0.,1.,0.));
#25646=DIRECTION('center_axis',(2.26980252028671E-15,0.,-1.));
#25647=DIRECTION('ref_axis',(-1.,0.,-2.26980252028671E-15));
#25648=DIRECTION('',(-1.,0.,-2.26980252028671E-15));
#25649=DIRECTION('',(0.,1.,0.));
#25650=DIRECTION('center_axis',(1.,0.,0.));
#25651=DIRECTION('ref_axis',(0.,0.,-1.));
#25652=DIRECTION('',(0.,0.,-1.));
#25653=DIRECTION('',(0.,1.,0.));
#25654=DIRECTION('center_axis',(0.,0.,-1.));
#25655=DIRECTION('ref_axis',(-1.,0.,0.));
#25656=DIRECTION('',(-1.,0.,0.));
#25657=DIRECTION('',(0.,1.,0.));
#25658=DIRECTION('center_axis',(-0.710721462348357,0.,-0.703473526834815));
#25659=DIRECTION('ref_axis',(-0.703473526834815,0.,0.710721462348357));
#25660=DIRECTION('',(-0.703473526834815,0.,0.710721462348357));
#25661=DIRECTION('center_axis',(0.,1.,0.));
#25662=DIRECTION('ref_axis',(1.,0.,0.));
#29325=CARTESIAN_POINT('',(0.,0.,0.));
#29326=CARTESIAN_POINT('Origin',(94.9508316648812,0.,1.95651033903146));
#29327=CARTESIAN_POINT('',(94.9508316648812,15.,1.95651033903146));
#29328=CARTESIAN_POINT('',(94.9508316648812,15.,6.95083166488121));
#29329=CARTESIAN_POINT('',(94.9508316648812,15.,4.72825516951573));
#29330=CARTESIAN_POINT('',(94.9508316648812,495.,6.95083166488121));
#29331=CARTESIAN_POINT('',(94.9508316648812,0.,6.95083166488121));
#29332=CARTESIAN_POINT('',(94.9508316648812,495.,1.95651033903146));
#29333=CARTESIAN_POINT('',(94.9508316648812,495.,6.95083166488121));
#29334=CARTESIAN_POINT('',(94.9508316648812,0.,1.95651033903146));
#29335=CARTESIAN_POINT('Origin',(94.9508316648812,0.,6.95083166488121));
#29336=CARTESIAN_POINT('',(95.6258960932749,15.,6.95083166488121));
#29337=CARTESIAN_POINT('',(96.2254158324406,15.,6.95083166488121));
#29338=CARTESIAN_POINT('',(95.6258960932749,495.,6.95083166488121));
#29339=CARTESIAN_POINT('',(95.6258960932749,0.,6.95083166488121));
#29340=CARTESIAN_POINT('',(96.9508316648812,495.,6.95083166488121));
#29341=CARTESIAN_POINT('Origin',(95.6258960932749,0.,6.95083166488121));
#29342=CARTESIAN_POINT('',(99.25,15.,10.6122749602376));
#29343=CARTESIAN_POINT('',(96.2269045529402,15.,7.55803235551558));
#29344=CARTESIAN_POINT('',(99.25,495.,10.6122749602376));
#29345=CARTESIAN_POINT('',(99.25,0.,10.6122749602376));
#29346=CARTESIAN_POINT('',(95.6258960932749,495.,6.95083166488121));
#29347=CARTESIAN_POINT('Origin',(99.936778624571,0.,0.978255169515729));
#29348=CARTESIAN_POINT('',(99.936778624571,15.,0.978255169515729));
#29349=CARTESIAN_POINT('',(99.936778624571,15.,0.));
#29350=CARTESIAN_POINT('',(99.936778624571,15.,4.23912758475787));
#29351=CARTESIAN_POINT('',(99.936778624571,495.,0.));
#29352=CARTESIAN_POINT('',(99.936778624571,0.,0.));
#29353=CARTESIAN_POINT('',(99.936778624571,495.,0.978255169515729));
#29354=CARTESIAN_POINT('',(99.936778624571,495.,0.978255169515729));
#29355=CARTESIAN_POINT('',(99.936778624571,0.,0.978255169515729));
#29356=CARTESIAN_POINT('Origin',(100.797592784069,0.,0.978255169515729));
#29357=CARTESIAN_POINT('',(100.797592784069,15.,0.978255169515729));
#29358=CARTESIAN_POINT('',(99.1487963920345,15.,0.978255169515729));
#29359=CARTESIAN_POINT('',(100.797592784069,495.,0.978255169515729));
#29360=CARTESIAN_POINT('',(100.797592784069,495.,0.978255169515729));
#29361=CARTESIAN_POINT('',(100.797592784069,0.,0.978255169515729));
#29362=CARTESIAN_POINT('Origin',(100.797592784069,0.,1.95651033903146));
#29363=CARTESIAN_POINT('',(100.797592784069,15.,1.95651033903146));
#29364=CARTESIAN_POINT('',(100.797592784069,15.,4.72825516951573));
#29365=CARTESIAN_POINT('',(100.797592784069,495.,1.95651033903146));
#29366=CARTESIAN_POINT('',(100.797592784069,495.,1.95651033903146));
#29367=CARTESIAN_POINT('',(100.797592784069,0.,1.95651033903146));
#29368=CARTESIAN_POINT('Origin',(96.9508316648812,0.,1.95651033903146));
#29369=CARTESIAN_POINT('',(96.9508316648812,15.,1.95651033903146));
#29370=CARTESIAN_POINT('',(97.2254158324406,15.,1.95651033903146));
#29371=CARTESIAN_POINT('',(96.9508316648812,495.,1.95651033903146));
#29372=CARTESIAN_POINT('',(96.9508316648812,495.,1.95651033903146));
#29373=CARTESIAN_POINT('',(96.9508316648812,0.,1.95651033903146));
#29374=CARTESIAN_POINT('Origin',(96.9508316648812,0.,5.44638293630937));
#29375=CARTESIAN_POINT('',(96.9508316648812,15.,5.44638293630937));
#29376=CARTESIAN_POINT('',(96.9508316648812,15.,6.47319146815469));
#29377=CARTESIAN_POINT('',(96.9508316648812,495.,5.44638293630937));
#29378=CARTESIAN_POINT('',(96.9508316648812,495.,6.95083166488121));
#29379=CARTESIAN_POINT('',(96.9508316648812,0.,5.44638293630937));
#29380=CARTESIAN_POINT('Origin',(100.715659452243,0.,9.25));
#29381=CARTESIAN_POINT('',(100.715659452243,15.,9.25));
#29382=CARTESIAN_POINT('',(99.4825076947727,15.,8.00414299624016));
#29383=CARTESIAN_POINT('',(100.715659452243,495.,9.25));
#29384=CARTESIAN_POINT('',(96.9508316648812,495.,5.44638293630937));
#29385=CARTESIAN_POINT('',(100.715659452243,0.,9.25));
#29386=CARTESIAN_POINT('Origin',(115.049168335119,0.,1.95651033903146));
#29387=CARTESIAN_POINT('',(115.049168335119,15.,1.95651033903146));
#29388=CARTESIAN_POINT('',(115.049168335119,15.,6.95083166488121));
#29389=CARTESIAN_POINT('',(115.049168335119,15.,4.72825516951573));
#29390=CARTESIAN_POINT('',(115.049168335119,495.,1.95651033903146));
#29391=CARTESIAN_POINT('',(115.049168335119,0.,1.95651033903146));
#29392=CARTESIAN_POINT('',(115.049168335119,495.,6.95083166488121));
#29393=CARTESIAN_POINT('',(115.049168335119,495.,6.95083166488121));
#29394=CARTESIAN_POINT('',(115.049168335119,0.,6.95083166488121));
#29395=CARTESIAN_POINT('Origin',(115.049168335119,0.,6.95083166488121));
#29396=CARTESIAN_POINT('',(114.374103906725,15.,6.95083166488121));
#29397=CARTESIAN_POINT('',(113.774584167559,15.,6.95083166488121));
#29398=CARTESIAN_POINT('',(114.374103906725,495.,6.95083166488121));
#29399=CARTESIAN_POINT('',(113.049168335119,495.,6.95083166488121));
#29400=CARTESIAN_POINT('',(114.374103906725,0.,6.95083166488121));
#29401=CARTESIAN_POINT('Origin',(114.374103906725,0.,6.95083166488121));
#29402=CARTESIAN_POINT('',(110.75,15.,10.6122749602376));
#29403=CARTESIAN_POINT('',(113.77309544706,15.,7.55803235551558));
#29404=CARTESIAN_POINT('',(110.75,495.,10.6122749602376));
#29405=CARTESIAN_POINT('',(114.374103906725,495.,6.95083166488121));
#29406=CARTESIAN_POINT('',(110.75,0.,10.6122749602376));
#29407=CARTESIAN_POINT('Origin',(105.,0.,9.25));
#29408=CARTESIAN_POINT('',(109.284340547757,15.,9.25));
#29409=CARTESIAN_POINT('',(108.75,15.,9.25));
#29410=CARTESIAN_POINT('',(109.284340547757,495.,9.25));
#29411=CARTESIAN_POINT('',(110.75,495.,9.25));
#29412=CARTESIAN_POINT('',(109.284340547757,0.,9.25));
#29413=CARTESIAN_POINT('Origin',(110.063221375429,0.,0.978255169515729));
#29414=CARTESIAN_POINT('',(110.063221375429,15.,0.978255169515729));
#29415=CARTESIAN_POINT('',(110.063221375429,15.,0.));
#29416=CARTESIAN_POINT('',(110.063221375429,15.,4.23912758475787));
#29417=CARTESIAN_POINT('',(110.063221375429,495.,0.978255169515729));
#29418=CARTESIAN_POINT('',(110.063221375429,0.,0.978255169515729));
#29419=CARTESIAN_POINT('',(110.063221375429,495.,0.));
#29420=CARTESIAN_POINT('',(110.063221375429,495.,0.978255169515729));
#29421=CARTESIAN_POINT('',(110.063221375429,0.,0.));
#29422=CARTESIAN_POINT('Origin',(109.202407215931,0.,0.978255169515729));
#29423=CARTESIAN_POINT('',(109.202407215931,15.,0.978255169515729));
#29424=CARTESIAN_POINT('',(110.851203607966,15.,0.978255169515729));
#29425=CARTESIAN_POINT('',(109.202407215931,495.,0.978255169515729));
#29426=CARTESIAN_POINT('',(109.202407215931,0.,0.978255169515729));
#29427=CARTESIAN_POINT('',(109.202407215931,495.,0.978255169515729));
#29428=CARTESIAN_POINT('Origin',(109.202407215931,0.,1.95651033903146));
#29429=CARTESIAN_POINT('',(109.202407215931,15.,1.95651033903146));
#29430=CARTESIAN_POINT('',(109.202407215931,15.,4.72825516951573));
#29431=CARTESIAN_POINT('',(109.202407215931,495.,1.95651033903146));
#29432=CARTESIAN_POINT('',(109.202407215931,0.,1.95651033903146));
#29433=CARTESIAN_POINT('',(109.202407215931,495.,1.95651033903146));
#29434=CARTESIAN_POINT('Origin',(113.049168335119,0.,1.95651033903146));
#29435=CARTESIAN_POINT('',(113.049168335119,15.,1.95651033903146));
#29436=CARTESIAN_POINT('',(112.774584167559,15.,1.95651033903146));
#29437=CARTESIAN_POINT('',(113.049168335119,495.,1.95651033903146));
#29438=CARTESIAN_POINT('',(113.049168335119,0.,1.95651033903146));
#29439=CARTESIAN_POINT('',(113.049168335119,495.,1.95651033903146));
#29440=CARTESIAN_POINT('Origin',(113.049168335119,0.,5.44638293630937));
#29441=CARTESIAN_POINT('',(113.049168335119,15.,5.44638293630937));
#29442=CARTESIAN_POINT('',(113.049168335119,15.,6.47319146815469));
#29443=CARTESIAN_POINT('',(113.049168335119,495.,5.44638293630937));
#29444=CARTESIAN_POINT('',(113.049168335119,0.,5.44638293630937));
#29445=CARTESIAN_POINT('',(113.049168335119,495.,6.95083166488121));
#29446=CARTESIAN_POINT('Origin',(109.284340547757,0.,9.25));
#29447=CARTESIAN_POINT('',(110.517492305227,15.,8.00414299624016));
#29448=CARTESIAN_POINT('',(113.049168335119,495.,5.44638293630937));
#29449=CARTESIAN_POINT('Origin',(94.9508316648812,0.,28.0434896609685));
#29450=CARTESIAN_POINT('',(94.9508316648812,15.,28.0434896609685));
#29451=CARTESIAN_POINT('',(94.9508316648812,15.,23.0491683351188));
#29452=CARTESIAN_POINT('',(94.9508316648812,15.,25.2717448304843));
#29453=CARTESIAN_POINT('',(94.9508316648812,495.,28.0434896609685));
#29454=CARTESIAN_POINT('',(94.9508316648812,0.,28.0434896609685));
#29455=CARTESIAN_POINT('',(94.9508316648812,495.,23.0491683351188));
#29456=CARTESIAN_POINT('',(94.9508316648812,495.,23.0491683351188));
#29457=CARTESIAN_POINT('',(94.9508316648812,0.,23.0491683351188));
#29458=CARTESIAN_POINT('Origin',(94.9508316648812,0.,23.0491683351188));
#29459=CARTESIAN_POINT('',(95.6258960932749,15.,23.0491683351188));
#29460=CARTESIAN_POINT('',(96.2254158324406,15.,23.0491683351188));
#29461=CARTESIAN_POINT('',(95.6258960932749,495.,23.0491683351188));
#29462=CARTESIAN_POINT('',(96.9508316648812,495.,23.0491683351188));
#29463=CARTESIAN_POINT('',(95.6258960932749,0.,23.0491683351188));
#29464=CARTESIAN_POINT('Origin',(95.6258960932749,0.,23.0491683351188));
#29465=CARTESIAN_POINT('',(99.25,15.,19.3877250397624));
#29466=CARTESIAN_POINT('',(96.2269045529402,15.,22.4419676444844));
#29467=CARTESIAN_POINT('',(99.25,495.,19.3877250397624));
#29468=CARTESIAN_POINT('',(95.6258960932749,495.,23.0491683351188));
#29469=CARTESIAN_POINT('',(99.25,0.,19.3877250397624));
#29470=CARTESIAN_POINT('Origin',(99.25,0.,19.3877250397624));
#29471=CARTESIAN_POINT('',(99.25,15.,9.05613748011882));
#29472=CARTESIAN_POINT('',(99.25,495.,20.75));
#29473=CARTESIAN_POINT('Origin',(99.936778624571,0.,29.0217448304843));
#29474=CARTESIAN_POINT('',(99.936778624571,15.,29.0217448304843));
#29475=CARTESIAN_POINT('',(99.936778624571,15.,30.));
#29476=CARTESIAN_POINT('',(99.936778624571,15.,25.7608724152421));
#29477=CARTESIAN_POINT('',(99.936778624571,495.,29.0217448304843));
#29478=CARTESIAN_POINT('',(99.936778624571,0.,29.0217448304843));
#29479=CARTESIAN_POINT('',(99.936778624571,495.,30.));
#29480=CARTESIAN_POINT('',(99.936778624571,495.,29.0217448304843));
#29481=CARTESIAN_POINT('',(99.936778624571,0.,30.));
#29482=CARTESIAN_POINT('Origin',(100.797592784069,0.,29.0217448304843));
#29483=CARTESIAN_POINT('',(100.797592784069,15.,29.0217448304843));
#29484=CARTESIAN_POINT('',(99.1487963920345,15.,29.0217448304843));
#29485=CARTESIAN_POINT('',(100.797592784069,495.,29.0217448304843));
#29486=CARTESIAN_POINT('',(100.797592784069,0.,29.0217448304843));
#29487=CARTESIAN_POINT('',(100.797592784069,495.,29.0217448304843));
#29488=CARTESIAN_POINT('Origin',(100.797592784069,0.,28.0434896609685));
#29489=CARTESIAN_POINT('',(100.797592784069,15.,28.0434896609685));
#29490=CARTESIAN_POINT('',(100.797592784069,15.,25.2717448304843));
#29491=CARTESIAN_POINT('',(100.797592784069,495.,28.0434896609685));
#29492=CARTESIAN_POINT('',(100.797592784069,0.,28.0434896609685));
#29493=CARTESIAN_POINT('',(100.797592784069,495.,28.0434896609685));
#29494=CARTESIAN_POINT('Origin',(96.9508316648812,0.,28.0434896609685));
#29495=CARTESIAN_POINT('',(96.9508316648812,15.,28.0434896609685));
#29496=CARTESIAN_POINT('',(97.2254158324406,15.,28.0434896609685));
#29497=CARTESIAN_POINT('',(96.9508316648812,495.,28.0434896609685));
#29498=CARTESIAN_POINT('',(96.9508316648812,0.,28.0434896609685));
#29499=CARTESIAN_POINT('',(96.9508316648812,495.,28.0434896609685));
#29500=CARTESIAN_POINT('Origin',(96.9508316648812,0.,24.5536170636906));
#29501=CARTESIAN_POINT('',(96.9508316648812,15.,24.5536170636906));
#29502=CARTESIAN_POINT('',(96.9508316648812,15.,23.5268085318453));
#29503=CARTESIAN_POINT('',(96.9508316648812,495.,24.5536170636906));
#29504=CARTESIAN_POINT('',(96.9508316648812,0.,24.5536170636906));
#29505=CARTESIAN_POINT('',(96.9508316648812,495.,23.0491683351188));
#29506=CARTESIAN_POINT('Origin',(100.715659452243,0.,20.75));
#29507=CARTESIAN_POINT('',(100.715659452243,15.,20.75));
#29508=CARTESIAN_POINT('',(99.4825076947727,15.,21.9958570037598));
#29509=CARTESIAN_POINT('',(100.715659452243,495.,20.75));
#29510=CARTESIAN_POINT('',(100.715659452243,0.,20.75));
#29511=CARTESIAN_POINT('',(96.9508316648812,495.,24.5536170636906));
#29512=CARTESIAN_POINT('Origin',(115.049168335119,0.,28.0434896609685));
#29513=CARTESIAN_POINT('',(115.049168335119,15.,28.0434896609685));
#29514=CARTESIAN_POINT('',(115.049168335119,15.,23.0491683351188));
#29515=CARTESIAN_POINT('',(115.049168335119,15.,25.2717448304843));
#29516=CARTESIAN_POINT('',(115.049168335119,495.,23.0491683351188));
#29517=CARTESIAN_POINT('',(115.049168335119,0.,23.0491683351188));
#29518=CARTESIAN_POINT('',(115.049168335119,495.,28.0434896609685));
#29519=CARTESIAN_POINT('',(115.049168335119,495.,23.0491683351188));
#29520=CARTESIAN_POINT('',(115.049168335119,0.,28.0434896609685));
#29521=CARTESIAN_POINT('Origin',(115.049168335119,0.,23.0491683351188));
#29522=CARTESIAN_POINT('',(114.374103906725,15.,23.0491683351188));
#29523=CARTESIAN_POINT('',(113.774584167559,15.,23.0491683351188));
#29524=CARTESIAN_POINT('',(114.374103906725,495.,23.0491683351188));
#29525=CARTESIAN_POINT('',(114.374103906725,0.,23.0491683351188));
#29526=CARTESIAN_POINT('',(113.049168335119,495.,23.0491683351188));
#29527=CARTESIAN_POINT('Origin',(114.374103906725,0.,23.0491683351188));
#29528=CARTESIAN_POINT('',(110.75,15.,19.3877250397624));
#29529=CARTESIAN_POINT('',(113.77309544706,15.,22.4419676444844));
#29530=CARTESIAN_POINT('',(110.75,495.,19.3877250397624));
#29531=CARTESIAN_POINT('',(110.75,0.,19.3877250397624));
#29532=CARTESIAN_POINT('',(114.374103906725,495.,23.0491683351188));
#29533=CARTESIAN_POINT('Origin',(110.75,0.,19.3877250397624));
#29534=CARTESIAN_POINT('',(110.75,15.,9.05613748011882));
#29535=CARTESIAN_POINT('',(110.75,495.,20.75));
#29536=CARTESIAN_POINT('Origin',(105.,0.,15.));
#29537=CARTESIAN_POINT('',(101.75,495.,15.));
#29538=CARTESIAN_POINT('Origin',(105.,495.,15.));
#29539=CARTESIAN_POINT('',(101.75,15.,15.));
#29540=CARTESIAN_POINT('',(101.75,0.,15.));
#29541=CARTESIAN_POINT('Origin',(105.,15.,15.));
#29542=CARTESIAN_POINT('Origin',(105.,0.,20.75));
#29543=CARTESIAN_POINT('',(109.284340547757,15.,20.75));
#29544=CARTESIAN_POINT('',(108.75,15.,20.75));
#29545=CARTESIAN_POINT('',(109.284340547757,495.,20.75));
#29546=CARTESIAN_POINT('',(109.284340547757,0.,20.75));
#29547=CARTESIAN_POINT('',(110.75,495.,20.75));
#29548=CARTESIAN_POINT('Origin',(110.063221375429,0.,29.0217448304843));
#29549=CARTESIAN_POINT('',(110.063221375429,15.,29.0217448304843));
#29550=CARTESIAN_POINT('',(110.063221375429,15.,30.));
#29551=CARTESIAN_POINT('',(110.063221375429,15.,25.7608724152421));
#29552=CARTESIAN_POINT('',(110.063221375429,495.,30.));
#29553=CARTESIAN_POINT('',(110.063221375429,0.,30.));
#29554=CARTESIAN_POINT('',(110.063221375429,495.,29.0217448304843));
#29555=CARTESIAN_POINT('',(110.063221375429,495.,29.0217448304843));
#29556=CARTESIAN_POINT('',(110.063221375429,0.,29.0217448304843));
#29557=CARTESIAN_POINT('Origin',(109.202407215931,0.,29.0217448304843));
#29558=CARTESIAN_POINT('',(109.202407215931,15.,29.0217448304843));
#29559=CARTESIAN_POINT('',(110.851203607966,15.,29.0217448304843));
#29560=CARTESIAN_POINT('',(109.202407215931,495.,29.0217448304843));
#29561=CARTESIAN_POINT('',(109.202407215931,495.,29.0217448304843));
#29562=CARTESIAN_POINT('',(109.202407215931,0.,29.0217448304843));
#29563=CARTESIAN_POINT('Origin',(109.202407215931,0.,28.0434896609685));
#29564=CARTESIAN_POINT('',(109.202407215931,15.,28.0434896609685));
#29565=CARTESIAN_POINT('',(109.202407215931,15.,25.2717448304843));
#29566=CARTESIAN_POINT('',(109.202407215931,495.,28.0434896609685));
#29567=CARTESIAN_POINT('',(109.202407215931,495.,28.0434896609685));
#29568=CARTESIAN_POINT('',(109.202407215931,0.,28.0434896609685));
#29569=CARTESIAN_POINT('Origin',(113.049168335119,0.,28.0434896609685));
#29570=CARTESIAN_POINT('',(113.049168335119,15.,28.0434896609685));
#29571=CARTESIAN_POINT('',(112.774584167559,15.,28.0434896609685));
#29572=CARTESIAN_POINT('',(113.049168335119,495.,28.0434896609685));
#29573=CARTESIAN_POINT('',(113.049168335119,495.,28.0434896609685));
#29574=CARTESIAN_POINT('',(113.049168335119,0.,28.0434896609685));
#29575=CARTESIAN_POINT('Origin',(113.049168335119,0.,24.5536170636906));
#29576=CARTESIAN_POINT('',(113.049168335119,15.,24.5536170636906));
#29577=CARTESIAN_POINT('',(113.049168335119,15.,23.5268085318453));
#29578=CARTESIAN_POINT('',(113.049168335119,495.,24.5536170636906));
#29579=CARTESIAN_POINT('',(113.049168335119,495.,23.0491683351188));
#29580=CARTESIAN_POINT('',(113.049168335119,0.,24.5536170636906));
#29581=CARTESIAN_POINT('Origin',(109.284340547757,0.,20.75));
#29582=CARTESIAN_POINT('',(110.517492305227,15.,21.9958570037598));
#29583=CARTESIAN_POINT('',(113.049168335119,495.,24.5536170636906));
#29584=CARTESIAN_POINT('Origin',(148.100393916659,0.,24.8185447775707));
#29585=CARTESIAN_POINT('',(148.100393916659,15.,24.8185447775707));
#29586=CARTESIAN_POINT('',(145.213316286378,15.,24.8185447775707));
#29587=CARTESIAN_POINT('',(141.550196958329,15.,24.8185447775707));
#29588=CARTESIAN_POINT('',(148.100393916659,495.,24.8185447775707));
#29589=CARTESIAN_POINT('',(148.100393916659,0.,24.8185447775707));
#29590=CARTESIAN_POINT('',(145.213316286378,495.,24.8185447775707));
#29591=CARTESIAN_POINT('',(148.100393916659,495.,24.8185447775707));
#29592=CARTESIAN_POINT('',(145.213316286378,0.,24.8185447775707));
#29593=CARTESIAN_POINT('Origin',(145.213316286378,0.,25.3185447775707));
#29594=CARTESIAN_POINT('',(144.713316286378,15.,25.3185447775707));
#29595=CARTESIAN_POINT('Origin',(145.213316286378,15.,25.3185447775707));
#29596=CARTESIAN_POINT('',(144.713316286378,495.,25.3185447775707));
#29597=CARTESIAN_POINT('Origin',(145.213316286378,495.,25.3185447775707));
#29598=CARTESIAN_POINT('',(144.713316286378,0.,25.3185447775707));
#29599=CARTESIAN_POINT('Origin',(144.713316286378,0.,25.3185447775707));
#29600=CARTESIAN_POINT('',(144.713316286378,15.,28.1876354028612));
#29601=CARTESIAN_POINT('',(144.713316286378,15.,23.9092723887854));
#29602=CARTESIAN_POINT('',(144.713316286378,495.,28.1876354028612));
#29603=CARTESIAN_POINT('',(144.713316286378,495.,25.3185447775707));
#29604=CARTESIAN_POINT('',(144.713316286378,0.,28.1876354028612));
#29605=CARTESIAN_POINT('Origin',(145.213316286378,0.,28.1876354028611));
#29606=CARTESIAN_POINT('',(145.213316286378,15.,28.6876354028611));
#29607=CARTESIAN_POINT('Origin',(145.213316286378,15.,28.1876354028611));
#29608=CARTESIAN_POINT('',(145.213316286378,495.,28.6876354028611));
#29609=CARTESIAN_POINT('Origin',(145.213316286378,495.,28.1876354028611));
#29610=CARTESIAN_POINT('',(145.213316286378,0.,28.6876354028611));
#29611=CARTESIAN_POINT('Origin',(130.715659452243,0.,20.75));
#29612=CARTESIAN_POINT('',(130.715659452243,15.,20.75));
#29613=CARTESIAN_POINT('',(126.950831664881,15.,24.5536170636906));
#29614=CARTESIAN_POINT('',(131.338288955863,15.,20.1209555023271));
#29615=CARTESIAN_POINT('',(130.715659452243,495.,20.75));
#29616=CARTESIAN_POINT('',(130.715659452243,0.,20.75));
#29617=CARTESIAN_POINT('',(126.950831664881,495.,24.5536170636906));
#29618=CARTESIAN_POINT('',(126.950831664881,495.,24.5536170636906));
#29619=CARTESIAN_POINT('',(126.950831664881,0.,24.5536170636906));
#29620=CARTESIAN_POINT('Origin',(126.950831664881,0.,24.5536170636906));
#29621=CARTESIAN_POINT('',(126.950831664881,15.,28.0434896609686));
#29622=CARTESIAN_POINT('',(126.950831664881,15.,23.5268085318453));
#29623=CARTESIAN_POINT('',(126.950831664881,495.,28.0434896609686));
#29624=CARTESIAN_POINT('',(126.950831664881,495.,23.0491683351188));
#29625=CARTESIAN_POINT('',(126.950831664881,0.,28.0434896609686));
#29626=CARTESIAN_POINT('Origin',(126.950831664881,0.,28.0434896609686));
#29627=CARTESIAN_POINT('',(130.797592784069,15.,28.0434896609686));
#29628=CARTESIAN_POINT('',(130.975415832441,15.,28.0434896609686));
#29629=CARTESIAN_POINT('',(130.797592784069,495.,28.0434896609686));
#29630=CARTESIAN_POINT('',(126.950831664881,495.,28.0434896609686));
#29631=CARTESIAN_POINT('',(130.797592784069,0.,28.0434896609686));
#29632=CARTESIAN_POINT('Origin',(130.797592784069,0.,28.0434896609686));
#29633=CARTESIAN_POINT('',(130.797592784069,15.,29.0217448304843));
#29634=CARTESIAN_POINT('',(130.797592784069,15.,25.2717448304843));
#29635=CARTESIAN_POINT('',(130.797592784069,495.,29.0217448304843));
#29636=CARTESIAN_POINT('',(130.797592784069,495.,28.0434896609686));
#29637=CARTESIAN_POINT('',(130.797592784069,0.,29.0217448304843));
#29638=CARTESIAN_POINT('Origin',(130.797592784069,0.,29.0217448304843));
#29639=CARTESIAN_POINT('',(129.936778624571,15.,29.0217448304843));
#29640=CARTESIAN_POINT('',(132.898796392034,15.,29.0217448304843));
#29641=CARTESIAN_POINT('',(129.936778624571,495.,29.0217448304843));
#29642=CARTESIAN_POINT('',(130.797592784069,495.,29.0217448304843));
#29643=CARTESIAN_POINT('',(129.936778624571,0.,29.0217448304843));
#29644=CARTESIAN_POINT('Origin',(129.936778624571,0.,29.0217448304843));
#29645=CARTESIAN_POINT('',(129.936778624571,15.,30.));
#29646=CARTESIAN_POINT('',(129.936778624571,15.,25.7608724152422));
#29647=CARTESIAN_POINT('',(129.936778624571,495.,30.));
#29648=CARTESIAN_POINT('',(129.936778624571,495.,29.0217448304843));
#29649=CARTESIAN_POINT('',(129.936778624571,0.,30.));
#29650=CARTESIAN_POINT('Origin',(129.936778624571,0.,30.));
#29651=CARTESIAN_POINT('',(111.281610687714,15.,30.));
#29652=CARTESIAN_POINT('',(135.,495.,30.));
#29653=CARTESIAN_POINT('Origin',(120.,0.,28.0434896609686));
#29654=CARTESIAN_POINT('',(124.950831664881,15.,28.0434896609686));
#29655=CARTESIAN_POINT('',(127.5,15.,28.0434896609686));
#29656=CARTESIAN_POINT('',(124.950831664881,495.,28.0434896609686));
#29657=CARTESIAN_POINT('',(113.049168335119,495.,28.0434896609685));
#29658=CARTESIAN_POINT('',(124.950831664881,0.,28.0434896609686));
#29659=CARTESIAN_POINT('Origin',(124.950831664881,0.,28.0434896609686));
#29660=CARTESIAN_POINT('',(124.950831664881,15.,23.0491683351188));
#29661=CARTESIAN_POINT('',(124.950831664881,15.,25.2717448304843));
#29662=CARTESIAN_POINT('',(124.950831664881,495.,23.0491683351188));
#29663=CARTESIAN_POINT('',(124.950831664881,495.,23.0491683351188));
#29664=CARTESIAN_POINT('',(124.950831664881,0.,23.0491683351188));
#29665=CARTESIAN_POINT('Origin',(124.950831664881,0.,23.0491683351188));
#29666=CARTESIAN_POINT('',(125.625896093275,15.,23.0491683351188));
#29667=CARTESIAN_POINT('',(129.975415832441,15.,23.0491683351188));
#29668=CARTESIAN_POINT('',(125.625896093275,495.,23.0491683351188));
#29669=CARTESIAN_POINT('',(126.950831664881,495.,23.0491683351188));
#29670=CARTESIAN_POINT('',(125.625896093275,0.,23.0491683351188));
#29671=CARTESIAN_POINT('Origin',(125.625896093275,0.,23.0491683351188));
#29672=CARTESIAN_POINT('',(129.25,15.,19.3877250397624));
#29673=CARTESIAN_POINT('',(128.082685814031,15.,20.5670661430517));
#29674=CARTESIAN_POINT('',(129.25,495.,19.3877250397624));
#29675=CARTESIAN_POINT('',(125.625896093275,495.,23.0491683351188));
#29676=CARTESIAN_POINT('',(129.25,0.,19.3877250397624));
#29677=CARTESIAN_POINT('Origin',(148.100393916659,0.,25.3185447775707));
#29678=CARTESIAN_POINT('',(148.600393916659,15.,25.3185447775707));
#29679=CARTESIAN_POINT('Origin',(148.100393916659,15.,25.3185447775707));
#29680=CARTESIAN_POINT('',(148.600393916659,495.,25.3185447775707));
#29681=CARTESIAN_POINT('',(148.600393916659,0.,25.3185447775707));
#29682=CARTESIAN_POINT('Origin',(148.100393916659,495.,25.3185447775707));
#29683=CARTESIAN_POINT('Origin',(148.600393916659,0.,28.1876354028612));
#29684=CARTESIAN_POINT('',(148.600393916659,15.,28.1876354028612));
#29685=CARTESIAN_POINT('',(148.600393916659,15.,25.3438177014306));
#29686=CARTESIAN_POINT('',(148.600393916659,495.,28.1876354028612));
#29687=CARTESIAN_POINT('',(148.600393916659,0.,28.1876354028612));
#29688=CARTESIAN_POINT('',(148.600393916659,495.,28.1876354028612));
#29689=CARTESIAN_POINT('Origin',(148.100393916659,0.,28.1876354028611));
#29690=CARTESIAN_POINT('',(148.100393916659,15.,28.6876354028611));
#29691=CARTESIAN_POINT('Origin',(148.100393916659,15.,28.1876354028611));
#29692=CARTESIAN_POINT('',(148.100393916659,495.,28.6876354028611));
#29693=CARTESIAN_POINT('',(148.100393916659,0.,28.6876354028611));
#29694=CARTESIAN_POINT('Origin',(148.100393916659,495.,28.1876354028611));
#29695=CARTESIAN_POINT('Origin',(145.213316286378,0.,28.6876354028611));
#29696=CARTESIAN_POINT('',(140.106658143189,15.,28.6876354028611));
#29697=CARTESIAN_POINT('',(145.213316286378,495.,28.6876354028611));
#29698=CARTESIAN_POINT('Origin',(139.284340547757,0.,20.75));
#29699=CARTESIAN_POINT('',(139.284340547757,15.,20.75));
#29700=CARTESIAN_POINT('',(137.142170273878,15.,20.75));
#29701=CARTESIAN_POINT('',(139.284340547757,495.,20.75));
#29702=CARTESIAN_POINT('',(139.284340547757,0.,20.75));
#29703=CARTESIAN_POINT('',(140.75,495.,20.75));
#29704=CARTESIAN_POINT('Origin',(143.049168335119,0.,24.5536170636906));
#29705=CARTESIAN_POINT('',(143.049168335119,15.,24.5536170636906));
#29706=CARTESIAN_POINT('',(140.544124937818,15.,22.0227640341724));
#29707=CARTESIAN_POINT('',(143.049168335119,495.,24.5536170636906));
#29708=CARTESIAN_POINT('',(143.049168335119,0.,24.5536170636906));
#29709=CARTESIAN_POINT('',(143.049168335119,495.,24.5536170636906));
#29710=CARTESIAN_POINT('Origin',(143.049168335119,0.,28.0434896609686));
#29711=CARTESIAN_POINT('',(143.049168335119,15.,28.0434896609686));
#29712=CARTESIAN_POINT('',(143.049168335119,15.,25.2717448304843));
#29713=CARTESIAN_POINT('',(143.049168335119,495.,28.0434896609686));
#29714=CARTESIAN_POINT('',(143.049168335119,0.,28.0434896609686));
#29715=CARTESIAN_POINT('',(143.049168335119,495.,23.0491683351188));
#29716=CARTESIAN_POINT('Origin',(139.202407215931,0.,28.0434896609686));
#29717=CARTESIAN_POINT('',(139.202407215931,15.,28.0434896609686));
#29718=CARTESIAN_POINT('',(137.101203607966,15.,28.0434896609686));
#29719=CARTESIAN_POINT('',(139.202407215931,495.,28.0434896609686));
#29720=CARTESIAN_POINT('',(139.202407215931,0.,28.0434896609686));
#29721=CARTESIAN_POINT('',(140.063221375429,495.,28.0434896609686));
#29722=CARTESIAN_POINT('Origin',(139.202407215931,0.,29.0217448304843));
#29723=CARTESIAN_POINT('',(139.202407215931,15.,29.0217448304843));
#29724=CARTESIAN_POINT('',(139.202407215931,15.,25.7608724152422));
#29725=CARTESIAN_POINT('',(139.202407215931,495.,29.0217448304843));
#29726=CARTESIAN_POINT('',(139.202407215931,0.,29.0217448304843));
#29727=CARTESIAN_POINT('',(139.202407215931,495.,28.0434896609686));
#29728=CARTESIAN_POINT('Origin',(140.063221375429,0.,29.0217448304843));
#29729=CARTESIAN_POINT('',(140.063221375429,15.,29.0217448304843));
#29730=CARTESIAN_POINT('',(137.531610687714,15.,29.0217448304843));
#29731=CARTESIAN_POINT('',(140.063221375429,495.,29.0217448304843));
#29732=CARTESIAN_POINT('',(140.063221375429,0.,29.0217448304843));
#29733=CARTESIAN_POINT('',(139.202407215931,495.,29.0217448304843));
#29734=CARTESIAN_POINT('Origin',(140.063221375429,0.,30.));
#29735=CARTESIAN_POINT('',(140.063221375429,15.,30.));
#29736=CARTESIAN_POINT('',(140.063221375429,15.,26.25));
#29737=CARTESIAN_POINT('',(140.063221375429,495.,30.));
#29738=CARTESIAN_POINT('',(140.063221375429,0.,30.));
#29739=CARTESIAN_POINT('',(140.063221375429,495.,29.0217448304843));
#29740=CARTESIAN_POINT('Origin',(148.,0.,30.));
#29741=CARTESIAN_POINT('',(148.,15.,30.));
#29742=CARTESIAN_POINT('',(141.5,15.,30.));
#29743=CARTESIAN_POINT('',(148.,495.,30.));
#29744=CARTESIAN_POINT('',(148.,0.,30.));
#29745=CARTESIAN_POINT('',(135.,495.,30.));
#29746=CARTESIAN_POINT('Origin',(148.,0.,28.));
#29747=CARTESIAN_POINT('',(150.,15.,28.));
#29748=CARTESIAN_POINT('Origin',(148.,15.,28.));
#29749=CARTESIAN_POINT('',(150.,495.,28.));
#29750=CARTESIAN_POINT('',(150.,0.,28.));
#29751=CARTESIAN_POINT('Origin',(148.,495.,28.));
#29752=CARTESIAN_POINT('Origin',(150.,0.,20.063221375429));
#29753=CARTESIAN_POINT('',(150.,15.,20.063221375429));
#29754=CARTESIAN_POINT('',(150.,15.,21.2816106877145));
#29755=CARTESIAN_POINT('',(150.,495.,20.063221375429));
#29756=CARTESIAN_POINT('',(150.,0.,20.063221375429));
#29757=CARTESIAN_POINT('',(150.,495.,20.063221375429));
#29758=CARTESIAN_POINT('Origin',(149.021744830484,0.,20.063221375429));
#29759=CARTESIAN_POINT('',(149.021744830484,15.,20.063221375429));
#29760=CARTESIAN_POINT('',(142.010872415242,15.,20.063221375429));
#29761=CARTESIAN_POINT('',(149.021744830484,495.,20.063221375429));
#29762=CARTESIAN_POINT('',(149.021744830484,0.,20.063221375429));
#29763=CARTESIAN_POINT('',(149.021744830484,495.,20.063221375429));
#29764=CARTESIAN_POINT('Origin',(149.021744830484,0.,19.2024072159311));
#29765=CARTESIAN_POINT('',(149.021744830484,15.,19.2024072159311));
#29766=CARTESIAN_POINT('',(149.021744830484,15.,20.8512036079656));
#29767=CARTESIAN_POINT('',(149.021744830484,495.,19.2024072159311));
#29768=CARTESIAN_POINT('',(149.021744830484,0.,19.2024072159311));
#29769=CARTESIAN_POINT('',(149.021744830484,495.,19.2024072159311));
#29770=CARTESIAN_POINT('Origin',(148.043489660969,0.,19.2024072159311));
#29771=CARTESIAN_POINT('',(148.043489660969,15.,19.2024072159311));
#29772=CARTESIAN_POINT('',(141.521744830484,15.,19.2024072159311));
#29773=CARTESIAN_POINT('',(148.043489660969,495.,19.2024072159311));
#29774=CARTESIAN_POINT('',(148.043489660969,0.,19.2024072159311));
#29775=CARTESIAN_POINT('',(148.043489660969,495.,19.2024072159311));
#29776=CARTESIAN_POINT('Origin',(148.043489660969,0.,23.0491683351188));
#29777=CARTESIAN_POINT('',(148.043489660969,15.,23.0491683351188));
#29778=CARTESIAN_POINT('',(148.043489660969,15.,22.7745841675594));
#29779=CARTESIAN_POINT('',(148.043489660969,495.,23.0491683351188));
#29780=CARTESIAN_POINT('',(148.043489660969,0.,23.0491683351188));
#29781=CARTESIAN_POINT('',(148.043489660969,495.,23.0491683351188));
#29782=CARTESIAN_POINT('Origin',(144.374103906725,0.,23.0491683351188));
#29783=CARTESIAN_POINT('',(144.374103906725,15.,23.0491683351188));
#29784=CARTESIAN_POINT('',(139.687051953363,15.,23.0491683351188));
#29785=CARTESIAN_POINT('',(144.374103906725,495.,23.0491683351188));
#29786=CARTESIAN_POINT('',(144.374103906725,0.,23.0491683351188));
#29787=CARTESIAN_POINT('',(148.043489660969,495.,23.0491683351188));
#29788=CARTESIAN_POINT('Origin',(140.75,0.,19.3877250397624));
#29789=CARTESIAN_POINT('',(140.75,15.,19.3877250397624));
#29790=CARTESIAN_POINT('',(140.105262232607,15.,18.7363444953735));
#29791=CARTESIAN_POINT('',(140.75,495.,19.3877250397624));
#29792=CARTESIAN_POINT('',(140.75,0.,19.3877250397624));
#29793=CARTESIAN_POINT('',(144.374103906725,495.,23.0491683351188));
#29794=CARTESIAN_POINT('Origin',(148.100393916659,0.,5.18145522242934));
#29795=CARTESIAN_POINT('',(148.100393916659,15.,5.18145522242934));
#29796=CARTESIAN_POINT('',(145.213316286378,15.,5.18145522242934));
#29797=CARTESIAN_POINT('',(141.550196958329,15.,5.18145522242934));
#29798=CARTESIAN_POINT('',(145.213316286378,495.,5.18145522242934));
#29799=CARTESIAN_POINT('',(145.213316286378,0.,5.18145522242934));
#29800=CARTESIAN_POINT('',(148.100393916659,495.,5.18145522242934));
#29801=CARTESIAN_POINT('',(148.100393916659,495.,5.18145522242934));
#29802=CARTESIAN_POINT('',(148.100393916659,0.,5.18145522242934));
#29803=CARTESIAN_POINT('Origin',(145.213316286378,0.,4.68145522242934));
#29804=CARTESIAN_POINT('',(144.713316286378,15.,4.68145522242934));
#29805=CARTESIAN_POINT('Origin',(145.213316286378,15.,4.68145522242934));
#29806=CARTESIAN_POINT('',(144.713316286378,495.,4.68145522242934));
#29807=CARTESIAN_POINT('',(144.713316286378,0.,4.68145522242934));
#29808=CARTESIAN_POINT('Origin',(145.213316286378,495.,4.68145522242934));
#29809=CARTESIAN_POINT('Origin',(144.713316286378,0.,4.68145522242934));
#29810=CARTESIAN_POINT('',(144.713316286378,15.,1.81236459713888));
#29811=CARTESIAN_POINT('',(144.713316286378,15.,6.09072761121468));
#29812=CARTESIAN_POINT('',(144.713316286378,495.,1.81236459713888));
#29813=CARTESIAN_POINT('',(144.713316286378,0.,1.81236459713888));
#29814=CARTESIAN_POINT('',(144.713316286378,495.,4.68145522242934));
#29815=CARTESIAN_POINT('Origin',(145.213316286378,0.,1.81236459713889));
#29816=CARTESIAN_POINT('',(145.213316286378,15.,1.3123645971389));
#29817=CARTESIAN_POINT('Origin',(145.213316286378,15.,1.81236459713889));
#29818=CARTESIAN_POINT('',(145.213316286378,495.,1.3123645971389));
#29819=CARTESIAN_POINT('',(145.213316286378,0.,1.3123645971389));
#29820=CARTESIAN_POINT('Origin',(145.213316286378,495.,1.81236459713889));
#29821=CARTESIAN_POINT('Origin',(130.715659452243,0.,9.25000000000001));
#29822=CARTESIAN_POINT('',(130.715659452243,15.,9.25000000000001));
#29823=CARTESIAN_POINT('',(126.950831664881,15.,5.44638293630938));
#29824=CARTESIAN_POINT('',(131.338288955863,15.,9.8790444976729));
#29825=CARTESIAN_POINT('',(126.950831664881,495.,5.44638293630938));
#29826=CARTESIAN_POINT('',(126.950831664881,0.,5.44638293630938));
#29827=CARTESIAN_POINT('',(130.715659452243,495.,9.25000000000001));
#29828=CARTESIAN_POINT('',(126.950831664881,495.,5.44638293630938));
#29829=CARTESIAN_POINT('',(130.715659452243,0.,9.25000000000001));
#29830=CARTESIAN_POINT('Origin',(126.950831664881,0.,5.44638293630938));
#29831=CARTESIAN_POINT('',(126.950831664881,15.,1.95651033903147));
#29832=CARTESIAN_POINT('',(126.950831664881,15.,6.4731914681547));
#29833=CARTESIAN_POINT('',(126.950831664881,495.,1.95651033903147));
#29834=CARTESIAN_POINT('',(126.950831664881,0.,1.95651033903147));
#29835=CARTESIAN_POINT('',(126.950831664881,495.,6.95083166488122));
#29836=CARTESIAN_POINT('Origin',(126.950831664881,0.,1.95651033903147));
#29837=CARTESIAN_POINT('',(130.797592784069,15.,1.95651033903147));
#29838=CARTESIAN_POINT('',(130.975415832441,15.,1.95651033903147));
#29839=CARTESIAN_POINT('',(130.797592784069,495.,1.95651033903147));
#29840=CARTESIAN_POINT('',(130.797592784069,0.,1.95651033903147));
#29841=CARTESIAN_POINT('',(126.950831664881,495.,1.95651033903147));
#29842=CARTESIAN_POINT('Origin',(130.797592784069,0.,1.95651033903147));
#29843=CARTESIAN_POINT('',(130.797592784069,15.,0.978255169515743));
#29844=CARTESIAN_POINT('',(130.797592784069,15.,4.72825516951574));
#29845=CARTESIAN_POINT('',(130.797592784069,495.,0.978255169515743));
#29846=CARTESIAN_POINT('',(130.797592784069,0.,0.978255169515743));
#29847=CARTESIAN_POINT('',(130.797592784069,495.,1.95651033903147));
#29848=CARTESIAN_POINT('Origin',(130.797592784069,0.,0.978255169515743));
#29849=CARTESIAN_POINT('',(129.936778624571,15.,0.978255169515743));
#29850=CARTESIAN_POINT('',(132.898796392034,15.,0.978255169515747));
#29851=CARTESIAN_POINT('',(129.936778624571,495.,0.978255169515743));
#29852=CARTESIAN_POINT('',(129.936778624571,0.,0.978255169515743));
#29853=CARTESIAN_POINT('',(130.797592784069,495.,0.978255169515743));
#29854=CARTESIAN_POINT('Origin',(129.936778624571,0.,0.978255169515743));
#29855=CARTESIAN_POINT('',(129.936778624571,15.,1.33226762955019E-14));
#29856=CARTESIAN_POINT('',(129.936778624571,15.,4.23912758475788));
#29857=CARTESIAN_POINT('',(129.936778624571,495.,1.33226762955019E-14));
#29858=CARTESIAN_POINT('',(129.936778624571,0.,1.33226762955019E-14));
#29859=CARTESIAN_POINT('',(129.936778624571,495.,0.978255169515743));
#29860=CARTESIAN_POINT('Origin',(129.936778624571,0.,1.33226762955019E-14));
#29861=CARTESIAN_POINT('',(111.281610687714,15.,0.));
#29862=CARTESIAN_POINT('',(135.,495.,1.77635683940025E-14));
#29863=CARTESIAN_POINT('Origin',(120.,0.,1.95651033903147));
#29864=CARTESIAN_POINT('',(124.950831664881,15.,1.95651033903147));
#29865=CARTESIAN_POINT('',(127.5,15.,1.95651033903147));
#29866=CARTESIAN_POINT('',(124.950831664881,495.,1.95651033903147));
#29867=CARTESIAN_POINT('',(124.950831664881,0.,1.95651033903147));
#29868=CARTESIAN_POINT('',(113.049168335119,495.,1.95651033903146));
#29869=CARTESIAN_POINT('Origin',(124.950831664881,0.,1.95651033903147));
#29870=CARTESIAN_POINT('',(124.950831664881,15.,6.95083166488122));
#29871=CARTESIAN_POINT('',(124.950831664881,15.,4.72825516951574));
#29872=CARTESIAN_POINT('',(124.950831664881,495.,6.95083166488122));
#29873=CARTESIAN_POINT('',(124.950831664881,0.,6.95083166488122));
#29874=CARTESIAN_POINT('',(124.950831664881,495.,6.95083166488122));
#29875=CARTESIAN_POINT('Origin',(124.950831664881,0.,6.95083166488122));
#29876=CARTESIAN_POINT('',(125.625896093275,15.,6.95083166488122));
#29877=CARTESIAN_POINT('',(129.975415832441,15.,6.95083166488122));
#29878=CARTESIAN_POINT('',(125.625896093275,495.,6.95083166488122));
#29879=CARTESIAN_POINT('',(125.625896093275,0.,6.95083166488122));
#29880=CARTESIAN_POINT('',(126.950831664881,495.,6.95083166488122));
#29881=CARTESIAN_POINT('Origin',(125.625896093275,0.,6.95083166488122));
#29882=CARTESIAN_POINT('',(129.25,15.,10.6122749602377));
#29883=CARTESIAN_POINT('',(128.082685814031,15.,9.43293385694832));
#29884=CARTESIAN_POINT('',(129.25,495.,10.6122749602377));
#29885=CARTESIAN_POINT('',(129.25,0.,10.6122749602377));
#29886=CARTESIAN_POINT('',(125.625896093275,495.,6.95083166488122));
#29887=CARTESIAN_POINT('Origin',(129.25,0.,10.6122749602377));
#29888=CARTESIAN_POINT('',(129.25,15.,20.9438625198812));
#29889=CARTESIAN_POINT('',(129.25,495.,9.25000000000001));
#29890=CARTESIAN_POINT('Origin',(135.,0.,15.));
#29891=CARTESIAN_POINT('',(138.25,495.,15.));
#29892=CARTESIAN_POINT('Origin',(135.,495.,15.));
#29893=CARTESIAN_POINT('',(138.25,15.,15.));
#29894=CARTESIAN_POINT('',(138.25,0.,15.));
#29895=CARTESIAN_POINT('Origin',(135.,15.,15.));
#29896=CARTESIAN_POINT('Origin',(140.75,0.,15.));
#29897=CARTESIAN_POINT('',(140.75,15.,10.6122749602377));
#29898=CARTESIAN_POINT('',(140.75,15.,11.25));
#29899=CARTESIAN_POINT('',(140.75,495.,10.6122749602377));
#29900=CARTESIAN_POINT('',(140.75,0.,10.6122749602377));
#29901=CARTESIAN_POINT('',(140.75,495.,9.25000000000002));
#29902=CARTESIAN_POINT('Origin',(148.100393916659,0.,4.68145522242934));
#29903=CARTESIAN_POINT('',(148.600393916659,15.,4.68145522242934));
#29904=CARTESIAN_POINT('Origin',(148.100393916659,15.,4.68145522242934));
#29905=CARTESIAN_POINT('',(148.600393916659,495.,4.68145522242934));
#29906=CARTESIAN_POINT('Origin',(148.100393916659,495.,4.68145522242934));
#29907=CARTESIAN_POINT('',(148.600393916659,0.,4.68145522242934));
#29908=CARTESIAN_POINT('Origin',(148.600393916659,0.,1.81236459713888));
#29909=CARTESIAN_POINT('',(148.600393916659,15.,1.81236459713888));
#29910=CARTESIAN_POINT('',(148.600393916659,15.,4.65618229856945));
#29911=CARTESIAN_POINT('',(148.600393916659,495.,1.81236459713888));
#29912=CARTESIAN_POINT('',(148.600393916659,495.,1.81236459713888));
#29913=CARTESIAN_POINT('',(148.600393916659,0.,1.81236459713888));
#29914=CARTESIAN_POINT('Origin',(148.100393916659,0.,1.81236459713889));
#29915=CARTESIAN_POINT('',(148.100393916659,15.,1.3123645971389));
#29916=CARTESIAN_POINT('Origin',(148.100393916659,15.,1.81236459713889));
#29917=CARTESIAN_POINT('',(148.100393916659,495.,1.3123645971389));
#29918=CARTESIAN_POINT('Origin',(148.100393916659,495.,1.81236459713889));
#29919=CARTESIAN_POINT('',(148.100393916659,0.,1.3123645971389));
#29920=CARTESIAN_POINT('Origin',(145.213316286378,0.,1.3123645971389));
#29921=CARTESIAN_POINT('',(140.106658143189,15.,1.3123645971389));
#29922=CARTESIAN_POINT('',(145.213316286378,495.,1.3123645971389));
#29923=CARTESIAN_POINT('Origin',(139.284340547757,0.,9.25000000000002));
#29924=CARTESIAN_POINT('',(139.284340547757,15.,9.25000000000002));
#29925=CARTESIAN_POINT('',(137.142170273878,15.,9.25000000000002));
#29926=CARTESIAN_POINT('',(139.284340547757,495.,9.25000000000002));
#29927=CARTESIAN_POINT('',(140.75,495.,9.25000000000002));
#29928=CARTESIAN_POINT('',(139.284340547757,0.,9.25000000000002));
#29929=CARTESIAN_POINT('Origin',(143.049168335119,0.,5.44638293630939));
#29930=CARTESIAN_POINT('',(143.049168335119,15.,5.44638293630939));
#29931=CARTESIAN_POINT('',(140.544124937818,15.,7.9772359658276));
#29932=CARTESIAN_POINT('',(143.049168335119,495.,5.44638293630939));
#29933=CARTESIAN_POINT('',(143.049168335119,495.,5.44638293630939));
#29934=CARTESIAN_POINT('',(143.049168335119,0.,5.44638293630939));
#29935=CARTESIAN_POINT('Origin',(143.049168335119,0.,1.95651033903148));
#29936=CARTESIAN_POINT('',(143.049168335119,15.,1.95651033903148));
#29937=CARTESIAN_POINT('',(143.049168335119,15.,4.72825516951575));
#29938=CARTESIAN_POINT('',(143.049168335119,495.,1.95651033903148));
#29939=CARTESIAN_POINT('',(143.049168335119,495.,6.95083166488122));
#29940=CARTESIAN_POINT('',(143.049168335119,0.,1.95651033903148));
#29941=CARTESIAN_POINT('Origin',(139.202407215931,0.,1.95651033903148));
#29942=CARTESIAN_POINT('',(139.202407215931,15.,1.95651033903148));
#29943=CARTESIAN_POINT('',(137.101203607966,15.,1.95651033903148));
#29944=CARTESIAN_POINT('',(139.202407215931,495.,1.95651033903148));
#29945=CARTESIAN_POINT('',(140.063221375429,495.,1.95651033903148));
#29946=CARTESIAN_POINT('',(139.202407215931,0.,1.95651033903148));
#29947=CARTESIAN_POINT('Origin',(139.202407215931,0.,0.978255169515747));
#29948=CARTESIAN_POINT('',(139.202407215931,15.,0.978255169515747));
#29949=CARTESIAN_POINT('',(139.202407215931,15.,4.23912758475788));
#29950=CARTESIAN_POINT('',(139.202407215931,495.,0.978255169515747));
#29951=CARTESIAN_POINT('',(139.202407215931,495.,1.95651033903148));
#29952=CARTESIAN_POINT('',(139.202407215931,0.,0.978255169515747));
#29953=CARTESIAN_POINT('Origin',(140.063221375429,0.,0.978255169515747));
#29954=CARTESIAN_POINT('',(140.063221375429,15.,0.978255169515747));
#29955=CARTESIAN_POINT('',(137.531610687715,15.,0.978255169515747));
#29956=CARTESIAN_POINT('',(140.063221375429,495.,0.978255169515747));
#29957=CARTESIAN_POINT('',(139.202407215931,495.,0.978255169515747));
#29958=CARTESIAN_POINT('',(140.063221375429,0.,0.978255169515747));
#29959=CARTESIAN_POINT('Origin',(140.063221375429,0.,1.77635683940025E-14));
#29960=CARTESIAN_POINT('',(140.063221375429,15.,1.77635683940025E-14));
#29961=CARTESIAN_POINT('',(140.063221375429,15.,3.75000000000002));
#29962=CARTESIAN_POINT('',(140.063221375429,495.,1.77635683940025E-14));
#29963=CARTESIAN_POINT('',(140.063221375429,495.,0.978255169515747));
#29964=CARTESIAN_POINT('',(140.063221375429,0.,1.77635683940025E-14));
#29965=CARTESIAN_POINT('Origin',(148.,0.,1.77635683940025E-14));
#29966=CARTESIAN_POINT('',(148.,15.,1.77635683940025E-14));
#29967=CARTESIAN_POINT('',(141.5,15.,1.77635683940025E-14));
#29968=CARTESIAN_POINT('',(148.,495.,1.77635683940025E-14));
#29969=CARTESIAN_POINT('',(135.,495.,1.77635683940025E-14));
#29970=CARTESIAN_POINT('',(148.,0.,1.77635683940025E-14));
#29971=CARTESIAN_POINT('Origin',(148.,0.,2.00000000000002));
#29972=CARTESIAN_POINT('',(150.,15.,2.00000000000002));
#29973=CARTESIAN_POINT('Origin',(148.,15.,2.00000000000002));
#29974=CARTESIAN_POINT('',(150.,495.,2.00000000000002));
#29975=CARTESIAN_POINT('Origin',(148.,495.,2.00000000000002));
#29976=CARTESIAN_POINT('',(150.,0.,2.00000000000002));
#29977=CARTESIAN_POINT('Origin',(150.,0.,9.93677862457105));
#29978=CARTESIAN_POINT('',(150.,15.,9.93677862457105));
#29979=CARTESIAN_POINT('',(150.,15.,8.71838931228553));
#29980=CARTESIAN_POINT('',(150.,495.,9.93677862457105));
#29981=CARTESIAN_POINT('',(150.,495.,9.93677862457105));
#29982=CARTESIAN_POINT('',(150.,0.,9.93677862457105));
#29983=CARTESIAN_POINT('Origin',(149.021744830484,0.,9.93677862457105));
#29984=CARTESIAN_POINT('',(149.021744830484,15.,9.93677862457105));
#29985=CARTESIAN_POINT('',(142.010872415242,15.,9.93677862457105));
#29986=CARTESIAN_POINT('',(149.021744830484,495.,9.93677862457105));
#29987=CARTESIAN_POINT('',(149.021744830484,495.,9.93677862457105));
#29988=CARTESIAN_POINT('',(149.021744830484,0.,9.93677862457105));
#29989=CARTESIAN_POINT('Origin',(149.021744830484,0.,10.7975927840689));
#29990=CARTESIAN_POINT('',(149.021744830484,15.,10.7975927840689));
#29991=CARTESIAN_POINT('',(149.021744830484,15.,9.14879639203446));
#29992=CARTESIAN_POINT('',(149.021744830484,495.,10.7975927840689));
#29993=CARTESIAN_POINT('',(149.021744830484,495.,10.7975927840689));
#29994=CARTESIAN_POINT('',(149.021744830484,0.,10.7975927840689));
#29995=CARTESIAN_POINT('Origin',(148.043489660969,0.,10.7975927840689));
#29996=CARTESIAN_POINT('',(148.043489660969,15.,10.7975927840689));
#29997=CARTESIAN_POINT('',(141.521744830484,15.,10.7975927840689));
#29998=CARTESIAN_POINT('',(148.043489660969,495.,10.7975927840689));
#29999=CARTESIAN_POINT('',(148.043489660969,495.,10.7975927840689));
#30000=CARTESIAN_POINT('',(148.043489660969,0.,10.7975927840689));
#30001=CARTESIAN_POINT('Origin',(148.043489660969,0.,6.95083166488122));
#30002=CARTESIAN_POINT('',(148.043489660969,15.,6.95083166488122));
#30003=CARTESIAN_POINT('',(148.043489660969,15.,7.22541583244062));
#30004=CARTESIAN_POINT('',(148.043489660969,495.,6.95083166488122));
#30005=CARTESIAN_POINT('',(148.043489660969,495.,6.95083166488122));
#30006=CARTESIAN_POINT('',(148.043489660969,0.,6.95083166488122));
#30007=CARTESIAN_POINT('Origin',(144.374103906725,0.,6.95083166488122));
#30008=CARTESIAN_POINT('',(144.374103906725,15.,6.95083166488122));
#30009=CARTESIAN_POINT('',(139.687051953363,15.,6.95083166488122));
#30010=CARTESIAN_POINT('',(144.374103906725,495.,6.95083166488122));
#30011=CARTESIAN_POINT('',(148.043489660969,495.,6.95083166488122));
#30012=CARTESIAN_POINT('',(144.374103906725,0.,6.95083166488122));
#30013=CARTESIAN_POINT('Origin',(140.75,0.,10.6122749602377));
#30014=CARTESIAN_POINT('',(140.105262232607,15.,11.2636555046265));
#30015=CARTESIAN_POINT('',(144.374103906725,495.,6.95083166488122));
#30016=CARTESIAN_POINT('Origin',(64.9508316648812,0.,1.95651033903146));
#30017=CARTESIAN_POINT('',(64.9508316648812,15.,1.95651033903146));
#30018=CARTESIAN_POINT('',(64.9508316648812,15.,6.95083166488121));
#30019=CARTESIAN_POINT('',(64.9508316648812,15.,4.72825516951573));
#30020=CARTESIAN_POINT('',(64.9508316648812,495.,6.95083166488121));
#30021=CARTESIAN_POINT('',(64.9508316648812,0.,6.95083166488121));
#30022=CARTESIAN_POINT('',(64.9508316648812,495.,1.95651033903146));
#30023=CARTESIAN_POINT('',(64.9508316648812,495.,6.95083166488121));
#30024=CARTESIAN_POINT('',(64.9508316648812,0.,1.95651033903146));
#30025=CARTESIAN_POINT('Origin',(64.9508316648812,0.,6.95083166488121));
#30026=CARTESIAN_POINT('',(65.6258960932749,15.,6.95083166488121));
#30027=CARTESIAN_POINT('',(66.2254158324406,15.,6.95083166488121));
#30028=CARTESIAN_POINT('',(65.6258960932749,495.,6.95083166488121));
#30029=CARTESIAN_POINT('',(65.6258960932749,0.,6.95083166488121));
#30030=CARTESIAN_POINT('',(66.9508316648812,495.,6.95083166488121));
#30031=CARTESIAN_POINT('Origin',(65.6258960932749,0.,6.95083166488121));
#30032=CARTESIAN_POINT('',(69.25,15.,10.6122749602376));
#30033=CARTESIAN_POINT('',(66.2269045529402,15.,7.55803235551558));
#30034=CARTESIAN_POINT('',(69.25,495.,10.6122749602376));
#30035=CARTESIAN_POINT('',(69.25,0.,10.6122749602376));
#30036=CARTESIAN_POINT('',(65.6258960932749,495.,6.95083166488121));
#30037=CARTESIAN_POINT('Origin',(69.936778624571,0.,0.978255169515729));
#30038=CARTESIAN_POINT('',(69.936778624571,15.,0.978255169515729));
#30039=CARTESIAN_POINT('',(69.936778624571,15.,0.));
#30040=CARTESIAN_POINT('',(69.936778624571,15.,4.23912758475787));
#30041=CARTESIAN_POINT('',(69.936778624571,495.,0.));
#30042=CARTESIAN_POINT('',(69.936778624571,0.,0.));
#30043=CARTESIAN_POINT('',(69.936778624571,495.,0.978255169515729));
#30044=CARTESIAN_POINT('',(69.936778624571,495.,0.978255169515729));
#30045=CARTESIAN_POINT('',(69.936778624571,0.,0.978255169515729));
#30046=CARTESIAN_POINT('Origin',(70.7975927840689,0.,0.978255169515729));
#30047=CARTESIAN_POINT('',(70.7975927840689,15.,0.978255169515729));
#30048=CARTESIAN_POINT('',(69.1487963920345,15.,0.978255169515729));
#30049=CARTESIAN_POINT('',(70.7975927840689,495.,0.978255169515729));
#30050=CARTESIAN_POINT('',(70.7975927840689,495.,0.978255169515729));
#30051=CARTESIAN_POINT('',(70.7975927840689,0.,0.978255169515729));
#30052=CARTESIAN_POINT('Origin',(70.7975927840689,0.,1.95651033903146));
#30053=CARTESIAN_POINT('',(70.7975927840689,15.,1.95651033903146));
#30054=CARTESIAN_POINT('',(70.7975927840689,15.,4.72825516951573));
#30055=CARTESIAN_POINT('',(70.7975927840689,495.,1.95651033903146));
#30056=CARTESIAN_POINT('',(70.7975927840689,495.,1.95651033903146));
#30057=CARTESIAN_POINT('',(70.7975927840689,0.,1.95651033903146));
#30058=CARTESIAN_POINT('Origin',(66.9508316648812,0.,1.95651033903146));
#30059=CARTESIAN_POINT('',(66.9508316648812,15.,1.95651033903146));
#30060=CARTESIAN_POINT('',(67.2254158324406,15.,1.95651033903146));
#30061=CARTESIAN_POINT('',(66.9508316648812,495.,1.95651033903146));
#30062=CARTESIAN_POINT('',(66.9508316648812,495.,1.95651033903146));
#30063=CARTESIAN_POINT('',(66.9508316648812,0.,1.95651033903146));
#30064=CARTESIAN_POINT('Origin',(66.9508316648812,0.,5.44638293630937));
#30065=CARTESIAN_POINT('',(66.9508316648812,15.,5.44638293630937));
#30066=CARTESIAN_POINT('',(66.9508316648812,15.,6.47319146815469));
#30067=CARTESIAN_POINT('',(66.9508316648812,495.,5.44638293630937));
#30068=CARTESIAN_POINT('',(66.9508316648812,495.,6.95083166488121));
#30069=CARTESIAN_POINT('',(66.9508316648812,0.,5.44638293630937));
#30070=CARTESIAN_POINT('Origin',(70.715659452243,0.,9.25));
#30071=CARTESIAN_POINT('',(70.715659452243,15.,9.25));
#30072=CARTESIAN_POINT('',(69.4825076947727,15.,8.00414299624016));
#30073=CARTESIAN_POINT('',(70.715659452243,495.,9.25));
#30074=CARTESIAN_POINT('',(66.9508316648812,495.,5.44638293630937));
#30075=CARTESIAN_POINT('',(70.715659452243,0.,9.25));
#30076=CARTESIAN_POINT('Origin',(90.,0.,1.95651033903146));
#30077=CARTESIAN_POINT('',(85.0491683351188,15.,1.95651033903146));
#30078=CARTESIAN_POINT('',(86.25,15.,1.95651033903146));
#30079=CARTESIAN_POINT('',(85.0491683351188,495.,1.95651033903146));
#30080=CARTESIAN_POINT('',(83.0491683351188,495.,1.95651033903146));
#30081=CARTESIAN_POINT('',(85.0491683351188,0.,1.95651033903146));
#30082=CARTESIAN_POINT('Origin',(85.0491683351188,0.,1.95651033903146));
#30083=CARTESIAN_POINT('',(85.0491683351188,15.,6.95083166488121));
#30084=CARTESIAN_POINT('',(85.0491683351188,15.,4.72825516951573));
#30085=CARTESIAN_POINT('',(85.0491683351188,495.,6.95083166488121));
#30086=CARTESIAN_POINT('',(85.0491683351188,495.,6.95083166488121));
#30087=CARTESIAN_POINT('',(85.0491683351188,0.,6.95083166488121));
#30088=CARTESIAN_POINT('Origin',(85.0491683351188,0.,6.95083166488121));
#30089=CARTESIAN_POINT('',(84.3741039067251,15.,6.95083166488121));
#30090=CARTESIAN_POINT('',(83.7745841675594,15.,6.95083166488121));
#30091=CARTESIAN_POINT('',(84.3741039067251,495.,6.95083166488121));
#30092=CARTESIAN_POINT('',(83.0491683351188,495.,6.95083166488121));
#30093=CARTESIAN_POINT('',(84.3741039067251,0.,6.95083166488121));
#30094=CARTESIAN_POINT('Origin',(84.3741039067251,0.,6.95083166488121));
#30095=CARTESIAN_POINT('',(80.75,15.,10.6122749602376));
#30096=CARTESIAN_POINT('',(83.7730954470598,15.,7.55803235551558));
#30097=CARTESIAN_POINT('',(80.75,495.,10.6122749602376));
#30098=CARTESIAN_POINT('',(84.3741039067251,495.,6.95083166488121));
#30099=CARTESIAN_POINT('',(80.75,0.,10.6122749602376));
#30100=CARTESIAN_POINT('Origin',(75.,0.,9.25));
#30101=CARTESIAN_POINT('',(79.284340547757,15.,9.25));
#30102=CARTESIAN_POINT('',(78.75,15.,9.25));
#30103=CARTESIAN_POINT('',(79.284340547757,495.,9.25));
#30104=CARTESIAN_POINT('',(80.75,495.,9.25));
#30105=CARTESIAN_POINT('',(79.284340547757,0.,9.25));
#30106=CARTESIAN_POINT('Origin',(80.063221375429,0.,0.));
#30107=CARTESIAN_POINT('',(80.063221375429,15.,0.));
#30108=CARTESIAN_POINT('',(98.7183893122855,15.,0.));
#30109=CARTESIAN_POINT('',(80.063221375429,495.,0.));
#30110=CARTESIAN_POINT('',(80.063221375429,0.,0.));
#30111=CARTESIAN_POINT('',(75.,495.,0.));
#30112=CARTESIAN_POINT('Origin',(80.063221375429,0.,0.978255169515729));
#30113=CARTESIAN_POINT('',(80.063221375429,15.,0.978255169515729));
#30114=CARTESIAN_POINT('',(80.063221375429,15.,4.23912758475787));
#30115=CARTESIAN_POINT('',(80.063221375429,495.,0.978255169515729));
#30116=CARTESIAN_POINT('',(80.063221375429,0.,0.978255169515729));
#30117=CARTESIAN_POINT('',(80.063221375429,495.,0.978255169515729));
#30118=CARTESIAN_POINT('Origin',(79.2024072159311,0.,0.978255169515729));
#30119=CARTESIAN_POINT('',(79.2024072159311,15.,0.978255169515729));
#30120=CARTESIAN_POINT('',(80.8512036079655,15.,0.978255169515729));
#30121=CARTESIAN_POINT('',(79.2024072159311,495.,0.978255169515729));
#30122=CARTESIAN_POINT('',(79.2024072159311,0.,0.978255169515729));
#30123=CARTESIAN_POINT('',(79.2024072159311,495.,0.978255169515729));
#30124=CARTESIAN_POINT('Origin',(79.2024072159311,0.,1.95651033903146));
#30125=CARTESIAN_POINT('',(79.2024072159311,15.,1.95651033903146));
#30126=CARTESIAN_POINT('',(79.2024072159311,15.,4.72825516951573));
#30127=CARTESIAN_POINT('',(79.2024072159311,495.,1.95651033903146));
#30128=CARTESIAN_POINT('',(79.2024072159311,0.,1.95651033903146));
#30129=CARTESIAN_POINT('',(79.2024072159311,495.,1.95651033903146));
#30130=CARTESIAN_POINT('Origin',(83.0491683351188,0.,1.95651033903146));
#30131=CARTESIAN_POINT('',(83.0491683351188,15.,1.95651033903146));
#30132=CARTESIAN_POINT('',(82.7745841675594,15.,1.95651033903146));
#30133=CARTESIAN_POINT('',(83.0491683351188,495.,1.95651033903146));
#30134=CARTESIAN_POINT('',(83.0491683351188,0.,1.95651033903146));
#30135=CARTESIAN_POINT('',(83.0491683351188,495.,1.95651033903146));
#30136=CARTESIAN_POINT('Origin',(83.0491683351188,0.,5.44638293630937));
#30137=CARTESIAN_POINT('',(83.0491683351188,15.,5.44638293630937));
#30138=CARTESIAN_POINT('',(83.0491683351188,15.,6.47319146815469));
#30139=CARTESIAN_POINT('',(83.0491683351188,495.,5.44638293630937));
#30140=CARTESIAN_POINT('',(83.0491683351188,0.,5.44638293630937));
#30141=CARTESIAN_POINT('',(83.0491683351188,495.,6.95083166488121));
#30142=CARTESIAN_POINT('Origin',(79.284340547757,0.,9.25));
#30143=CARTESIAN_POINT('',(80.5174923052273,15.,8.00414299624016));
#30144=CARTESIAN_POINT('',(83.0491683351188,495.,5.44638293630937));
#30145=CARTESIAN_POINT('Origin',(64.9508316648812,0.,28.0434896609685));
#30146=CARTESIAN_POINT('',(64.9508316648812,15.,28.0434896609685));
#30147=CARTESIAN_POINT('',(64.9508316648812,15.,23.0491683351188));
#30148=CARTESIAN_POINT('',(64.9508316648812,15.,25.2717448304843));
#30149=CARTESIAN_POINT('',(64.9508316648812,495.,28.0434896609685));
#30150=CARTESIAN_POINT('',(64.9508316648812,0.,28.0434896609685));
#30151=CARTESIAN_POINT('',(64.9508316648812,495.,23.0491683351188));
#30152=CARTESIAN_POINT('',(64.9508316648812,495.,23.0491683351188));
#30153=CARTESIAN_POINT('',(64.9508316648812,0.,23.0491683351188));
#30154=CARTESIAN_POINT('Origin',(64.9508316648812,0.,23.0491683351188));
#30155=CARTESIAN_POINT('',(65.6258960932749,15.,23.0491683351188));
#30156=CARTESIAN_POINT('',(66.2254158324406,15.,23.0491683351188));
#30157=CARTESIAN_POINT('',(65.6258960932749,495.,23.0491683351188));
#30158=CARTESIAN_POINT('',(66.9508316648812,495.,23.0491683351188));
#30159=CARTESIAN_POINT('',(65.6258960932749,0.,23.0491683351188));
#30160=CARTESIAN_POINT('Origin',(65.6258960932749,0.,23.0491683351188));
#30161=CARTESIAN_POINT('',(69.25,15.,19.3877250397624));
#30162=CARTESIAN_POINT('',(66.2269045529402,15.,22.4419676444844));
#30163=CARTESIAN_POINT('',(69.25,495.,19.3877250397624));
#30164=CARTESIAN_POINT('',(65.6258960932749,495.,23.0491683351188));
#30165=CARTESIAN_POINT('',(69.25,0.,19.3877250397624));
#30166=CARTESIAN_POINT('Origin',(69.25,0.,19.3877250397624));
#30167=CARTESIAN_POINT('',(69.25,15.,9.05613748011882));
#30168=CARTESIAN_POINT('',(69.25,495.,20.75));
#30169=CARTESIAN_POINT('Origin',(69.936778624571,0.,29.0217448304843));
#30170=CARTESIAN_POINT('',(69.936778624571,15.,29.0217448304843));
#30171=CARTESIAN_POINT('',(69.936778624571,15.,30.));
#30172=CARTESIAN_POINT('',(69.936778624571,15.,25.7608724152421));
#30173=CARTESIAN_POINT('',(69.936778624571,495.,29.0217448304843));
#30174=CARTESIAN_POINT('',(69.936778624571,0.,29.0217448304843));
#30175=CARTESIAN_POINT('',(69.936778624571,495.,30.));
#30176=CARTESIAN_POINT('',(69.936778624571,495.,29.0217448304843));
#30177=CARTESIAN_POINT('',(69.936778624571,0.,30.));
#30178=CARTESIAN_POINT('Origin',(70.7975927840689,0.,29.0217448304843));
#30179=CARTESIAN_POINT('',(70.7975927840689,15.,29.0217448304843));
#30180=CARTESIAN_POINT('',(69.1487963920345,15.,29.0217448304843));
#30181=CARTESIAN_POINT('',(70.7975927840689,495.,29.0217448304843));
#30182=CARTESIAN_POINT('',(70.7975927840689,0.,29.0217448304843));
#30183=CARTESIAN_POINT('',(70.7975927840689,495.,29.0217448304843));
#30184=CARTESIAN_POINT('Origin',(70.7975927840689,0.,28.0434896609685));
#30185=CARTESIAN_POINT('',(70.7975927840689,15.,28.0434896609685));
#30186=CARTESIAN_POINT('',(70.7975927840689,15.,25.2717448304843));
#30187=CARTESIAN_POINT('',(70.7975927840689,495.,28.0434896609685));
#30188=CARTESIAN_POINT('',(70.7975927840689,0.,28.0434896609685));
#30189=CARTESIAN_POINT('',(70.7975927840689,495.,28.0434896609685));
#30190=CARTESIAN_POINT('Origin',(66.9508316648812,0.,28.0434896609685));
#30191=CARTESIAN_POINT('',(66.9508316648812,15.,28.0434896609685));
#30192=CARTESIAN_POINT('',(67.2254158324406,15.,28.0434896609685));
#30193=CARTESIAN_POINT('',(66.9508316648812,495.,28.0434896609685));
#30194=CARTESIAN_POINT('',(66.9508316648812,0.,28.0434896609685));
#30195=CARTESIAN_POINT('',(66.9508316648812,495.,28.0434896609685));
#30196=CARTESIAN_POINT('Origin',(66.9508316648812,0.,24.5536170636906));
#30197=CARTESIAN_POINT('',(66.9508316648812,15.,24.5536170636906));
#30198=CARTESIAN_POINT('',(66.9508316648812,15.,23.5268085318453));
#30199=CARTESIAN_POINT('',(66.9508316648812,495.,24.5536170636906));
#30200=CARTESIAN_POINT('',(66.9508316648812,0.,24.5536170636906));
#30201=CARTESIAN_POINT('',(66.9508316648812,495.,23.0491683351188));
#30202=CARTESIAN_POINT('Origin',(70.715659452243,0.,20.75));
#30203=CARTESIAN_POINT('',(70.715659452243,15.,20.75));
#30204=CARTESIAN_POINT('',(69.4825076947727,15.,21.9958570037598));
#30205=CARTESIAN_POINT('',(70.715659452243,495.,20.75));
#30206=CARTESIAN_POINT('',(70.715659452243,0.,20.75));
#30207=CARTESIAN_POINT('',(66.9508316648812,495.,24.5536170636906));
#30208=CARTESIAN_POINT('Origin',(90.,0.,28.0434896609685));
#30209=CARTESIAN_POINT('',(85.0491683351188,15.,28.0434896609685));
#30210=CARTESIAN_POINT('',(86.25,15.,28.0434896609685));
#30211=CARTESIAN_POINT('',(85.0491683351188,495.,28.0434896609685));
#30212=CARTESIAN_POINT('',(85.0491683351188,0.,28.0434896609685));
#30213=CARTESIAN_POINT('',(96.9508316648812,495.,28.0434896609685));
#30214=CARTESIAN_POINT('Origin',(85.0491683351188,0.,28.0434896609685));
#30215=CARTESIAN_POINT('',(85.0491683351188,15.,23.0491683351188));
#30216=CARTESIAN_POINT('',(85.0491683351188,15.,25.2717448304843));
#30217=CARTESIAN_POINT('',(85.0491683351188,495.,23.0491683351188));
#30218=CARTESIAN_POINT('',(85.0491683351188,0.,23.0491683351188));
#30219=CARTESIAN_POINT('',(85.0491683351188,495.,23.0491683351188));
#30220=CARTESIAN_POINT('Origin',(85.0491683351188,0.,23.0491683351188));
#30221=CARTESIAN_POINT('',(84.3741039067251,15.,23.0491683351188));
#30222=CARTESIAN_POINT('',(83.7745841675594,15.,23.0491683351188));
#30223=CARTESIAN_POINT('',(84.3741039067251,495.,23.0491683351188));
#30224=CARTESIAN_POINT('',(84.3741039067251,0.,23.0491683351188));
#30225=CARTESIAN_POINT('',(83.0491683351188,495.,23.0491683351188));
#30226=CARTESIAN_POINT('Origin',(84.3741039067251,0.,23.0491683351188));
#30227=CARTESIAN_POINT('',(80.75,15.,19.3877250397624));
#30228=CARTESIAN_POINT('',(83.7730954470598,15.,22.4419676444844));
#30229=CARTESIAN_POINT('',(80.75,495.,19.3877250397624));
#30230=CARTESIAN_POINT('',(80.75,0.,19.3877250397624));
#30231=CARTESIAN_POINT('',(84.3741039067251,495.,23.0491683351188));
#30232=CARTESIAN_POINT('Origin',(80.75,0.,19.3877250397624));
#30233=CARTESIAN_POINT('',(80.75,15.,9.05613748011882));
#30234=CARTESIAN_POINT('',(80.75,495.,20.75));
#30235=CARTESIAN_POINT('Origin',(75.,0.,15.));
#30236=CARTESIAN_POINT('',(71.75,495.,15.));
#30237=CARTESIAN_POINT('Origin',(75.,495.,15.));
#30238=CARTESIAN_POINT('',(71.75,15.,15.));
#30239=CARTESIAN_POINT('',(71.75,0.,15.));
#30240=CARTESIAN_POINT('Origin',(75.,15.,15.));
#30241=CARTESIAN_POINT('Origin',(75.,0.,20.75));
#30242=CARTESIAN_POINT('',(79.284340547757,15.,20.75));
#30243=CARTESIAN_POINT('',(78.75,15.,20.75));
#30244=CARTESIAN_POINT('',(79.284340547757,495.,20.75));
#30245=CARTESIAN_POINT('',(79.284340547757,0.,20.75));
#30246=CARTESIAN_POINT('',(80.75,495.,20.75));
#30247=CARTESIAN_POINT('Origin',(80.063221375429,0.,30.));
#30248=CARTESIAN_POINT('',(80.063221375429,15.,30.));
#30249=CARTESIAN_POINT('',(98.7183893122855,15.,30.));
#30250=CARTESIAN_POINT('',(80.063221375429,495.,30.));
#30251=CARTESIAN_POINT('',(75.,495.,30.));
#30252=CARTESIAN_POINT('',(80.063221375429,0.,30.));
#30253=CARTESIAN_POINT('Origin',(80.063221375429,0.,29.0217448304843));
#30254=CARTESIAN_POINT('',(80.063221375429,15.,29.0217448304843));
#30255=CARTESIAN_POINT('',(80.063221375429,15.,25.7608724152421));
#30256=CARTESIAN_POINT('',(80.063221375429,495.,29.0217448304843));
#30257=CARTESIAN_POINT('',(80.063221375429,495.,29.0217448304843));
#30258=CARTESIAN_POINT('',(80.063221375429,0.,29.0217448304843));
#30259=CARTESIAN_POINT('Origin',(79.2024072159311,0.,29.0217448304843));
#30260=CARTESIAN_POINT('',(79.2024072159311,15.,29.0217448304843));
#30261=CARTESIAN_POINT('',(80.8512036079655,15.,29.0217448304843));
#30262=CARTESIAN_POINT('',(79.2024072159311,495.,29.0217448304843));
#30263=CARTESIAN_POINT('',(79.2024072159311,495.,29.0217448304843));
#30264=CARTESIAN_POINT('',(79.2024072159311,0.,29.0217448304843));
#30265=CARTESIAN_POINT('Origin',(79.2024072159311,0.,28.0434896609685));
#30266=CARTESIAN_POINT('',(79.2024072159311,15.,28.0434896609685));
#30267=CARTESIAN_POINT('',(79.2024072159311,15.,25.2717448304843));
#30268=CARTESIAN_POINT('',(79.2024072159311,495.,28.0434896609685));
#30269=CARTESIAN_POINT('',(79.2024072159311,495.,28.0434896609685));
#30270=CARTESIAN_POINT('',(79.2024072159311,0.,28.0434896609685));
#30271=CARTESIAN_POINT('Origin',(83.0491683351188,0.,28.0434896609685));
#30272=CARTESIAN_POINT('',(83.0491683351188,15.,28.0434896609685));
#30273=CARTESIAN_POINT('',(82.7745841675594,15.,28.0434896609685));
#30274=CARTESIAN_POINT('',(83.0491683351188,495.,28.0434896609685));
#30275=CARTESIAN_POINT('',(83.0491683351188,495.,28.0434896609685));
#30276=CARTESIAN_POINT('',(83.0491683351188,0.,28.0434896609685));
#30277=CARTESIAN_POINT('Origin',(83.0491683351188,0.,24.5536170636906));
#30278=CARTESIAN_POINT('',(83.0491683351188,15.,24.5536170636906));
#30279=CARTESIAN_POINT('',(83.0491683351188,15.,23.5268085318453));
#30280=CARTESIAN_POINT('',(83.0491683351188,495.,24.5536170636906));
#30281=CARTESIAN_POINT('',(83.0491683351188,495.,23.0491683351188));
#30282=CARTESIAN_POINT('',(83.0491683351188,0.,24.5536170636906));
#30283=CARTESIAN_POINT('Origin',(79.284340547757,0.,20.75));
#30284=CARTESIAN_POINT('',(80.5174923052273,15.,21.9958570037598));
#30285=CARTESIAN_POINT('',(83.0491683351188,495.,24.5536170636906));
#30286=CARTESIAN_POINT('Origin',(34.9508316648812,0.,1.95651033903146));
#30287=CARTESIAN_POINT('',(34.9508316648812,15.,1.95651033903146));
#30288=CARTESIAN_POINT('',(34.9508316648812,15.,6.95083166488121));
#30289=CARTESIAN_POINT('',(34.9508316648812,15.,4.72825516951573));
#30290=CARTESIAN_POINT('',(34.9508316648812,495.,6.95083166488121));
#30291=CARTESIAN_POINT('',(34.9508316648812,0.,6.95083166488121));
#30292=CARTESIAN_POINT('',(34.9508316648812,495.,1.95651033903146));
#30293=CARTESIAN_POINT('',(34.9508316648812,495.,6.95083166488121));
#30294=CARTESIAN_POINT('',(34.9508316648812,0.,1.95651033903146));
#30295=CARTESIAN_POINT('Origin',(34.9508316648812,0.,6.95083166488121));
#30296=CARTESIAN_POINT('',(35.6258960932749,15.,6.95083166488121));
#30297=CARTESIAN_POINT('',(36.2254158324406,15.,6.95083166488121));
#30298=CARTESIAN_POINT('',(35.6258960932749,495.,6.95083166488121));
#30299=CARTESIAN_POINT('',(35.6258960932749,0.,6.95083166488121));
#30300=CARTESIAN_POINT('',(36.9508316648812,495.,6.95083166488121));
#30301=CARTESIAN_POINT('Origin',(35.6258960932749,0.,6.95083166488121));
#30302=CARTESIAN_POINT('',(39.25,15.,10.6122749602376));
#30303=CARTESIAN_POINT('',(36.2269045529402,15.,7.55803235551558));
#30304=CARTESIAN_POINT('',(39.25,495.,10.6122749602376));
#30305=CARTESIAN_POINT('',(39.25,0.,10.6122749602376));
#30306=CARTESIAN_POINT('',(35.6258960932749,495.,6.95083166488121));
#30307=CARTESIAN_POINT('Origin',(39.936778624571,0.,0.978255169515729));
#30308=CARTESIAN_POINT('',(39.936778624571,15.,0.978255169515729));
#30309=CARTESIAN_POINT('',(39.936778624571,15.,0.));
#30310=CARTESIAN_POINT('',(39.936778624571,15.,4.23912758475787));
#30311=CARTESIAN_POINT('',(39.936778624571,495.,0.));
#30312=CARTESIAN_POINT('',(39.936778624571,0.,0.));
#30313=CARTESIAN_POINT('',(39.936778624571,495.,0.978255169515729));
#30314=CARTESIAN_POINT('',(39.936778624571,495.,0.978255169515729));
#30315=CARTESIAN_POINT('',(39.936778624571,0.,0.978255169515729));
#30316=CARTESIAN_POINT('Origin',(40.7975927840689,0.,0.978255169515729));
#30317=CARTESIAN_POINT('',(40.7975927840689,15.,0.978255169515729));
#30318=CARTESIAN_POINT('',(39.1487963920345,15.,0.978255169515729));
#30319=CARTESIAN_POINT('',(40.7975927840689,495.,0.978255169515729));
#30320=CARTESIAN_POINT('',(40.7975927840689,495.,0.978255169515729));
#30321=CARTESIAN_POINT('',(40.7975927840689,0.,0.978255169515729));
#30322=CARTESIAN_POINT('Origin',(40.7975927840689,0.,1.95651033903146));
#30323=CARTESIAN_POINT('',(40.7975927840689,15.,1.95651033903146));
#30324=CARTESIAN_POINT('',(40.7975927840689,15.,4.72825516951573));
#30325=CARTESIAN_POINT('',(40.7975927840689,495.,1.95651033903146));
#30326=CARTESIAN_POINT('',(40.7975927840689,495.,1.95651033903146));
#30327=CARTESIAN_POINT('',(40.7975927840689,0.,1.95651033903146));
#30328=CARTESIAN_POINT('Origin',(36.9508316648812,0.,1.95651033903146));
#30329=CARTESIAN_POINT('',(36.9508316648812,15.,1.95651033903146));
#30330=CARTESIAN_POINT('',(37.2254158324406,15.,1.95651033903146));
#30331=CARTESIAN_POINT('',(36.9508316648812,495.,1.95651033903146));
#30332=CARTESIAN_POINT('',(36.9508316648812,495.,1.95651033903146));
#30333=CARTESIAN_POINT('',(36.9508316648812,0.,1.95651033903146));
#30334=CARTESIAN_POINT('Origin',(36.9508316648812,0.,5.44638293630937));
#30335=CARTESIAN_POINT('',(36.9508316648812,15.,5.44638293630937));
#30336=CARTESIAN_POINT('',(36.9508316648812,15.,6.47319146815469));
#30337=CARTESIAN_POINT('',(36.9508316648812,495.,5.44638293630937));
#30338=CARTESIAN_POINT('',(36.9508316648812,495.,6.95083166488121));
#30339=CARTESIAN_POINT('',(36.9508316648812,0.,5.44638293630937));
#30340=CARTESIAN_POINT('Origin',(40.715659452243,0.,9.25));
#30341=CARTESIAN_POINT('',(40.715659452243,15.,9.25));
#30342=CARTESIAN_POINT('',(39.4825076947727,15.,8.00414299624016));
#30343=CARTESIAN_POINT('',(40.715659452243,495.,9.25));
#30344=CARTESIAN_POINT('',(36.9508316648812,495.,5.44638293630937));
#30345=CARTESIAN_POINT('',(40.715659452243,0.,9.25));
#30346=CARTESIAN_POINT('Origin',(60.,0.,1.95651033903146));
#30347=CARTESIAN_POINT('',(55.0491683351188,15.,1.95651033903146));
#30348=CARTESIAN_POINT('',(56.25,15.,1.95651033903146));
#30349=CARTESIAN_POINT('',(55.0491683351188,495.,1.95651033903146));
#30350=CARTESIAN_POINT('',(53.0491683351188,495.,1.95651033903146));
#30351=CARTESIAN_POINT('',(55.0491683351188,0.,1.95651033903146));
#30352=CARTESIAN_POINT('Origin',(55.0491683351188,0.,1.95651033903146));
#30353=CARTESIAN_POINT('',(55.0491683351188,15.,6.95083166488121));
#30354=CARTESIAN_POINT('',(55.0491683351188,15.,4.72825516951573));
#30355=CARTESIAN_POINT('',(55.0491683351188,495.,6.95083166488121));
#30356=CARTESIAN_POINT('',(55.0491683351188,495.,6.95083166488121));
#30357=CARTESIAN_POINT('',(55.0491683351188,0.,6.95083166488121));
#30358=CARTESIAN_POINT('Origin',(55.0491683351188,0.,6.95083166488121));
#30359=CARTESIAN_POINT('',(54.3741039067251,15.,6.95083166488121));
#30360=CARTESIAN_POINT('',(53.7745841675594,15.,6.95083166488121));
#30361=CARTESIAN_POINT('',(54.3741039067251,495.,6.95083166488121));
#30362=CARTESIAN_POINT('',(53.0491683351188,495.,6.95083166488121));
#30363=CARTESIAN_POINT('',(54.3741039067251,0.,6.95083166488121));
#30364=CARTESIAN_POINT('Origin',(54.3741039067251,0.,6.95083166488121));
#30365=CARTESIAN_POINT('',(50.75,15.,10.6122749602376));
#30366=CARTESIAN_POINT('',(53.7730954470598,15.,7.55803235551558));
#30367=CARTESIAN_POINT('',(50.75,495.,10.6122749602376));
#30368=CARTESIAN_POINT('',(54.3741039067251,495.,6.95083166488121));
#30369=CARTESIAN_POINT('',(50.75,0.,10.6122749602376));
#30370=CARTESIAN_POINT('Origin',(45.,0.,9.25));
#30371=CARTESIAN_POINT('',(49.284340547757,15.,9.25));
#30372=CARTESIAN_POINT('',(48.75,15.,9.25));
#30373=CARTESIAN_POINT('',(49.284340547757,495.,9.25));
#30374=CARTESIAN_POINT('',(50.75,495.,9.25));
#30375=CARTESIAN_POINT('',(49.284340547757,0.,9.25));
#30376=CARTESIAN_POINT('Origin',(50.063221375429,0.,0.));
#30377=CARTESIAN_POINT('',(50.063221375429,15.,0.));
#30378=CARTESIAN_POINT('',(68.7183893122855,15.,0.));
#30379=CARTESIAN_POINT('',(50.063221375429,495.,0.));
#30380=CARTESIAN_POINT('',(50.063221375429,0.,0.));
#30381=CARTESIAN_POINT('',(45.,495.,0.));
#30382=CARTESIAN_POINT('Origin',(50.063221375429,0.,0.978255169515729));
#30383=CARTESIAN_POINT('',(50.063221375429,15.,0.978255169515729));
#30384=CARTESIAN_POINT('',(50.063221375429,15.,4.23912758475787));
#30385=CARTESIAN_POINT('',(50.063221375429,495.,0.978255169515729));
#30386=CARTESIAN_POINT('',(50.063221375429,0.,0.978255169515729));
#30387=CARTESIAN_POINT('',(50.063221375429,495.,0.978255169515729));
#30388=CARTESIAN_POINT('Origin',(49.2024072159311,0.,0.978255169515729));
#30389=CARTESIAN_POINT('',(49.2024072159311,15.,0.978255169515729));
#30390=CARTESIAN_POINT('',(50.8512036079655,15.,0.978255169515729));
#30391=CARTESIAN_POINT('',(49.2024072159311,495.,0.978255169515729));
#30392=CARTESIAN_POINT('',(49.2024072159311,0.,0.978255169515729));
#30393=CARTESIAN_POINT('',(49.2024072159311,495.,0.978255169515729));
#30394=CARTESIAN_POINT('Origin',(49.2024072159311,0.,1.95651033903146));
#30395=CARTESIAN_POINT('',(49.2024072159311,15.,1.95651033903146));
#30396=CARTESIAN_POINT('',(49.2024072159311,15.,4.72825516951573));
#30397=CARTESIAN_POINT('',(49.2024072159311,495.,1.95651033903146));
#30398=CARTESIAN_POINT('',(49.2024072159311,0.,1.95651033903146));
#30399=CARTESIAN_POINT('',(49.2024072159311,495.,1.95651033903146));
#30400=CARTESIAN_POINT('Origin',(53.0491683351188,0.,1.95651033903146));
#30401=CARTESIAN_POINT('',(53.0491683351188,15.,1.95651033903146));
#30402=CARTESIAN_POINT('',(52.7745841675594,15.,1.95651033903146));
#30403=CARTESIAN_POINT('',(53.0491683351188,495.,1.95651033903146));
#30404=CARTESIAN_POINT('',(53.0491683351188,0.,1.95651033903146));
#30405=CARTESIAN_POINT('',(53.0491683351188,495.,1.95651033903146));
#30406=CARTESIAN_POINT('Origin',(53.0491683351188,0.,5.44638293630937));
#30407=CARTESIAN_POINT('',(53.0491683351188,15.,5.44638293630937));
#30408=CARTESIAN_POINT('',(53.0491683351188,15.,6.47319146815469));
#30409=CARTESIAN_POINT('',(53.0491683351188,495.,5.44638293630937));
#30410=CARTESIAN_POINT('',(53.0491683351188,0.,5.44638293630937));
#30411=CARTESIAN_POINT('',(53.0491683351188,495.,6.95083166488121));
#30412=CARTESIAN_POINT('Origin',(49.284340547757,0.,9.25));
#30413=CARTESIAN_POINT('',(50.5174923052273,15.,8.00414299624016));
#30414=CARTESIAN_POINT('',(53.0491683351188,495.,5.44638293630937));
#30415=CARTESIAN_POINT('Origin',(34.9508316648812,0.,28.0434896609685));
#30416=CARTESIAN_POINT('',(34.9508316648812,15.,28.0434896609685));
#30417=CARTESIAN_POINT('',(34.9508316648812,15.,23.0491683351188));
#30418=CARTESIAN_POINT('',(34.9508316648812,15.,25.2717448304843));
#30419=CARTESIAN_POINT('',(34.9508316648812,495.,28.0434896609685));
#30420=CARTESIAN_POINT('',(34.9508316648812,0.,28.0434896609685));
#30421=CARTESIAN_POINT('',(34.9508316648812,495.,23.0491683351188));
#30422=CARTESIAN_POINT('',(34.9508316648812,495.,23.0491683351188));
#30423=CARTESIAN_POINT('',(34.9508316648812,0.,23.0491683351188));
#30424=CARTESIAN_POINT('Origin',(34.9508316648812,0.,23.0491683351188));
#30425=CARTESIAN_POINT('',(35.6258960932749,15.,23.0491683351188));
#30426=CARTESIAN_POINT('',(36.2254158324406,15.,23.0491683351188));
#30427=CARTESIAN_POINT('',(35.6258960932749,495.,23.0491683351188));
#30428=CARTESIAN_POINT('',(36.9508316648812,495.,23.0491683351188));
#30429=CARTESIAN_POINT('',(35.6258960932749,0.,23.0491683351188));
#30430=CARTESIAN_POINT('Origin',(35.6258960932749,0.,23.0491683351188));
#30431=CARTESIAN_POINT('',(39.25,15.,19.3877250397624));
#30432=CARTESIAN_POINT('',(36.2269045529402,15.,22.4419676444844));
#30433=CARTESIAN_POINT('',(39.25,495.,19.3877250397624));
#30434=CARTESIAN_POINT('',(35.6258960932749,495.,23.0491683351188));
#30435=CARTESIAN_POINT('',(39.25,0.,19.3877250397624));
#30436=CARTESIAN_POINT('Origin',(39.25,0.,19.3877250397624));
#30437=CARTESIAN_POINT('',(39.25,15.,9.05613748011882));
#30438=CARTESIAN_POINT('',(39.25,495.,20.75));
#30439=CARTESIAN_POINT('Origin',(39.936778624571,0.,29.0217448304843));
#30440=CARTESIAN_POINT('',(39.936778624571,15.,29.0217448304843));
#30441=CARTESIAN_POINT('',(39.936778624571,15.,30.));
#30442=CARTESIAN_POINT('',(39.936778624571,15.,25.7608724152421));
#30443=CARTESIAN_POINT('',(39.936778624571,495.,29.0217448304843));
#30444=CARTESIAN_POINT('',(39.936778624571,0.,29.0217448304843));
#30445=CARTESIAN_POINT('',(39.936778624571,495.,30.));
#30446=CARTESIAN_POINT('',(39.936778624571,495.,29.0217448304843));
#30447=CARTESIAN_POINT('',(39.936778624571,0.,30.));
#30448=CARTESIAN_POINT('Origin',(40.7975927840689,0.,29.0217448304843));
#30449=CARTESIAN_POINT('',(40.7975927840689,15.,29.0217448304843));
#30450=CARTESIAN_POINT('',(39.1487963920345,15.,29.0217448304843));
#30451=CARTESIAN_POINT('',(40.7975927840689,495.,29.0217448304843));
#30452=CARTESIAN_POINT('',(40.7975927840689,0.,29.0217448304843));
#30453=CARTESIAN_POINT('',(40.7975927840689,495.,29.0217448304843));
#30454=CARTESIAN_POINT('Origin',(40.7975927840689,0.,28.0434896609685));
#30455=CARTESIAN_POINT('',(40.7975927840689,15.,28.0434896609685));
#30456=CARTESIAN_POINT('',(40.7975927840689,15.,25.2717448304843));
#30457=CARTESIAN_POINT('',(40.7975927840689,495.,28.0434896609685));
#30458=CARTESIAN_POINT('',(40.7975927840689,0.,28.0434896609685));
#30459=CARTESIAN_POINT('',(40.7975927840689,495.,28.0434896609685));
#30460=CARTESIAN_POINT('Origin',(36.9508316648812,0.,28.0434896609685));
#30461=CARTESIAN_POINT('',(36.9508316648812,15.,28.0434896609685));
#30462=CARTESIAN_POINT('',(37.2254158324406,15.,28.0434896609685));
#30463=CARTESIAN_POINT('',(36.9508316648812,495.,28.0434896609685));
#30464=CARTESIAN_POINT('',(36.9508316648812,0.,28.0434896609685));
#30465=CARTESIAN_POINT('',(36.9508316648812,495.,28.0434896609685));
#30466=CARTESIAN_POINT('Origin',(36.9508316648812,0.,24.5536170636906));
#30467=CARTESIAN_POINT('',(36.9508316648812,15.,24.5536170636906));
#30468=CARTESIAN_POINT('',(36.9508316648812,15.,23.5268085318453));
#30469=CARTESIAN_POINT('',(36.9508316648812,495.,24.5536170636906));
#30470=CARTESIAN_POINT('',(36.9508316648812,0.,24.5536170636906));
#30471=CARTESIAN_POINT('',(36.9508316648812,495.,23.0491683351188));
#30472=CARTESIAN_POINT('Origin',(40.715659452243,0.,20.75));
#30473=CARTESIAN_POINT('',(40.715659452243,15.,20.75));
#30474=CARTESIAN_POINT('',(39.4825076947727,15.,21.9958570037598));
#30475=CARTESIAN_POINT('',(40.715659452243,495.,20.75));
#30476=CARTESIAN_POINT('',(40.715659452243,0.,20.75));
#30477=CARTESIAN_POINT('',(36.9508316648812,495.,24.5536170636906));
#30478=CARTESIAN_POINT('Origin',(60.,0.,28.0434896609685));
#30479=CARTESIAN_POINT('',(55.0491683351188,15.,28.0434896609685));
#30480=CARTESIAN_POINT('',(56.25,15.,28.0434896609685));
#30481=CARTESIAN_POINT('',(55.0491683351188,495.,28.0434896609685));
#30482=CARTESIAN_POINT('',(55.0491683351188,0.,28.0434896609685));
#30483=CARTESIAN_POINT('',(66.9508316648812,495.,28.0434896609685));
#30484=CARTESIAN_POINT('Origin',(55.0491683351188,0.,28.0434896609685));
#30485=CARTESIAN_POINT('',(55.0491683351188,15.,23.0491683351188));
#30486=CARTESIAN_POINT('',(55.0491683351188,15.,25.2717448304843));
#30487=CARTESIAN_POINT('',(55.0491683351188,495.,23.0491683351188));
#30488=CARTESIAN_POINT('',(55.0491683351188,0.,23.0491683351188));
#30489=CARTESIAN_POINT('',(55.0491683351188,495.,23.0491683351188));
#30490=CARTESIAN_POINT('Origin',(55.0491683351188,0.,23.0491683351188));
#30491=CARTESIAN_POINT('',(54.3741039067251,15.,23.0491683351188));
#30492=CARTESIAN_POINT('',(53.7745841675594,15.,23.0491683351188));
#30493=CARTESIAN_POINT('',(54.3741039067251,495.,23.0491683351188));
#30494=CARTESIAN_POINT('',(54.3741039067251,0.,23.0491683351188));
#30495=CARTESIAN_POINT('',(53.0491683351188,495.,23.0491683351188));
#30496=CARTESIAN_POINT('Origin',(54.3741039067251,0.,23.0491683351188));
#30497=CARTESIAN_POINT('',(50.75,15.,19.3877250397624));
#30498=CARTESIAN_POINT('',(53.7730954470598,15.,22.4419676444844));
#30499=CARTESIAN_POINT('',(50.75,495.,19.3877250397624));
#30500=CARTESIAN_POINT('',(50.75,0.,19.3877250397624));
#30501=CARTESIAN_POINT('',(54.3741039067251,495.,23.0491683351188));
#30502=CARTESIAN_POINT('Origin',(50.75,0.,19.3877250397624));
#30503=CARTESIAN_POINT('',(50.75,15.,9.05613748011882));
#30504=CARTESIAN_POINT('',(50.75,495.,20.75));
#30505=CARTESIAN_POINT('Origin',(45.,0.,15.));
#30506=CARTESIAN_POINT('',(41.75,495.,15.));
#30507=CARTESIAN_POINT('Origin',(45.,495.,15.));
#30508=CARTESIAN_POINT('',(41.75,15.,15.));
#30509=CARTESIAN_POINT('',(41.75,0.,15.));
#30510=CARTESIAN_POINT('Origin',(45.,15.,15.));
#30511=CARTESIAN_POINT('Origin',(45.,0.,20.75));
#30512=CARTESIAN_POINT('',(49.284340547757,15.,20.75));
#30513=CARTESIAN_POINT('',(48.75,15.,20.75));
#30514=CARTESIAN_POINT('',(49.284340547757,495.,20.75));
#30515=CARTESIAN_POINT('',(49.284340547757,0.,20.75));
#30516=CARTESIAN_POINT('',(50.75,495.,20.75));
#30517=CARTESIAN_POINT('Origin',(50.063221375429,0.,30.));
#30518=CARTESIAN_POINT('',(50.063221375429,15.,30.));
#30519=CARTESIAN_POINT('',(68.7183893122855,15.,30.));
#30520=CARTESIAN_POINT('',(50.063221375429,495.,30.));
#30521=CARTESIAN_POINT('',(45.,495.,30.));
#30522=CARTESIAN_POINT('',(50.063221375429,0.,30.));
#30523=CARTESIAN_POINT('Origin',(50.063221375429,0.,29.0217448304843));
#30524=CARTESIAN_POINT('',(50.063221375429,15.,29.0217448304843));
#30525=CARTESIAN_POINT('',(50.063221375429,15.,25.7608724152421));
#30526=CARTESIAN_POINT('',(50.063221375429,495.,29.0217448304843));
#30527=CARTESIAN_POINT('',(50.063221375429,495.,29.0217448304843));
#30528=CARTESIAN_POINT('',(50.063221375429,0.,29.0217448304843));
#30529=CARTESIAN_POINT('Origin',(49.2024072159311,0.,29.0217448304843));
#30530=CARTESIAN_POINT('',(49.2024072159311,15.,29.0217448304843));
#30531=CARTESIAN_POINT('',(50.8512036079655,15.,29.0217448304843));
#30532=CARTESIAN_POINT('',(49.2024072159311,495.,29.0217448304843));
#30533=CARTESIAN_POINT('',(49.2024072159311,495.,29.0217448304843));
#30534=CARTESIAN_POINT('',(49.2024072159311,0.,29.0217448304843));
#30535=CARTESIAN_POINT('Origin',(49.2024072159311,0.,28.0434896609685));
#30536=CARTESIAN_POINT('',(49.2024072159311,15.,28.0434896609685));
#30537=CARTESIAN_POINT('',(49.2024072159311,15.,25.2717448304843));
#30538=CARTESIAN_POINT('',(49.2024072159311,495.,28.0434896609685));
#30539=CARTESIAN_POINT('',(49.2024072159311,495.,28.0434896609685));
#30540=CARTESIAN_POINT('',(49.2024072159311,0.,28.0434896609685));
#30541=CARTESIAN_POINT('Origin',(53.0491683351188,0.,28.0434896609685));
#30542=CARTESIAN_POINT('',(53.0491683351188,15.,28.0434896609685));
#30543=CARTESIAN_POINT('',(52.7745841675594,15.,28.0434896609685));
#30544=CARTESIAN_POINT('',(53.0491683351188,495.,28.0434896609685));
#30545=CARTESIAN_POINT('',(53.0491683351188,495.,28.0434896609685));
#30546=CARTESIAN_POINT('',(53.0491683351188,0.,28.0434896609685));
#30547=CARTESIAN_POINT('Origin',(53.0491683351188,0.,24.5536170636906));
#30548=CARTESIAN_POINT('',(53.0491683351188,15.,24.5536170636906));
#30549=CARTESIAN_POINT('',(53.0491683351188,15.,23.5268085318453));
#30550=CARTESIAN_POINT('',(53.0491683351188,495.,24.5536170636906));
#30551=CARTESIAN_POINT('',(53.0491683351188,495.,23.0491683351188));
#30552=CARTESIAN_POINT('',(53.0491683351188,0.,24.5536170636906));
#30553=CARTESIAN_POINT('Origin',(49.284340547757,0.,20.75));
#30554=CARTESIAN_POINT('',(50.5174923052273,15.,21.9958570037598));
#30555=CARTESIAN_POINT('',(53.0491683351188,495.,24.5536170636906));
#30556=CARTESIAN_POINT('Origin',(1.89960608334138,0.,5.18145522242933));
#30557=CARTESIAN_POINT('',(1.89960608334138,15.,5.18145522242933));
#30558=CARTESIAN_POINT('',(4.78668371362235,15.,5.18145522242933));
#30559=CARTESIAN_POINT('',(8.44980304167069,15.,5.18145522242933));
#30560=CARTESIAN_POINT('',(1.89960608334138,495.,5.18145522242933));
#30561=CARTESIAN_POINT('',(1.89960608334138,0.,5.18145522242933));
#30562=CARTESIAN_POINT('',(4.78668371362235,495.,5.18145522242933));
#30563=CARTESIAN_POINT('',(1.89960608334138,495.,5.18145522242933));
#30564=CARTESIAN_POINT('',(4.78668371362235,0.,5.18145522242933));
#30565=CARTESIAN_POINT('Origin',(4.78668371362236,0.,4.68145522242933));
#30566=CARTESIAN_POINT('',(5.28668371362236,15.,4.68145522242933));
#30567=CARTESIAN_POINT('Origin',(4.78668371362236,15.,4.68145522242933));
#30568=CARTESIAN_POINT('',(5.28668371362236,495.,4.68145522242933));
#30569=CARTESIAN_POINT('Origin',(4.78668371362236,495.,4.68145522242933));
#30570=CARTESIAN_POINT('',(5.28668371362236,0.,4.68145522242933));
#30571=CARTESIAN_POINT('Origin',(5.28668371362236,0.,4.68145522242933));
#30572=CARTESIAN_POINT('',(5.28668371362235,15.,1.81236459713887));
#30573=CARTESIAN_POINT('',(5.28668371362236,15.,6.09072761121467));
#30574=CARTESIAN_POINT('',(5.28668371362235,495.,1.81236459713887));
#30575=CARTESIAN_POINT('',(5.28668371362236,495.,4.68145522242933));
#30576=CARTESIAN_POINT('',(5.28668371362235,0.,1.81236459713887));
#30577=CARTESIAN_POINT('Origin',(4.78668371362235,0.,1.81236459713888));
#30578=CARTESIAN_POINT('',(4.78668371362235,15.,1.31236459713888));
#30579=CARTESIAN_POINT('Origin',(4.78668371362235,15.,1.81236459713888));
#30580=CARTESIAN_POINT('',(4.78668371362235,495.,1.31236459713888));
#30581=CARTESIAN_POINT('Origin',(4.78668371362235,495.,1.81236459713888));
#30582=CARTESIAN_POINT('',(4.78668371362235,0.,1.31236459713888));
#30583=CARTESIAN_POINT('Origin',(19.284340547757,0.,9.25));
#30584=CARTESIAN_POINT('',(19.284340547757,15.,9.25));
#30585=CARTESIAN_POINT('',(23.0491683351188,15.,5.44638293630937));
#30586=CARTESIAN_POINT('',(18.661711044137,15.,9.87904449767289));
#30587=CARTESIAN_POINT('',(19.284340547757,495.,9.25));
#30588=CARTESIAN_POINT('',(19.284340547757,0.,9.25));
#30589=CARTESIAN_POINT('',(23.0491683351188,495.,5.44638293630937));
#30590=CARTESIAN_POINT('',(23.0491683351188,495.,5.44638293630937));
#30591=CARTESIAN_POINT('',(23.0491683351188,0.,5.44638293630937));
#30592=CARTESIAN_POINT('Origin',(23.0491683351188,0.,5.44638293630937));
#30593=CARTESIAN_POINT('',(23.0491683351188,15.,1.95651033903146));
#30594=CARTESIAN_POINT('',(23.0491683351188,15.,6.47319146815469));
#30595=CARTESIAN_POINT('',(23.0491683351188,495.,1.95651033903146));
#30596=CARTESIAN_POINT('',(23.0491683351188,495.,6.95083166488121));
#30597=CARTESIAN_POINT('',(23.0491683351188,0.,1.95651033903146));
#30598=CARTESIAN_POINT('Origin',(23.0491683351188,0.,1.95651033903146));
#30599=CARTESIAN_POINT('',(19.2024072159311,15.,1.95651033903146));
#30600=CARTESIAN_POINT('',(19.0245841675594,15.,1.95651033903146));
#30601=CARTESIAN_POINT('',(19.2024072159311,495.,1.95651033903146));
#30602=CARTESIAN_POINT('',(23.0491683351188,495.,1.95651033903146));
#30603=CARTESIAN_POINT('',(19.2024072159311,0.,1.95651033903146));
#30604=CARTESIAN_POINT('Origin',(19.2024072159311,0.,1.95651033903146));
#30605=CARTESIAN_POINT('',(19.2024072159311,15.,0.978255169515729));
#30606=CARTESIAN_POINT('',(19.2024072159311,15.,4.72825516951573));
#30607=CARTESIAN_POINT('',(19.2024072159311,495.,0.978255169515729));
#30608=CARTESIAN_POINT('',(19.2024072159311,495.,1.95651033903146));
#30609=CARTESIAN_POINT('',(19.2024072159311,0.,0.978255169515729));
#30610=CARTESIAN_POINT('Origin',(19.2024072159311,0.,0.978255169515729));
#30611=CARTESIAN_POINT('',(20.063221375429,15.,0.978255169515729));
#30612=CARTESIAN_POINT('',(17.1012036079655,15.,0.978255169515729));
#30613=CARTESIAN_POINT('',(20.063221375429,495.,0.978255169515729));
#30614=CARTESIAN_POINT('',(19.2024072159311,495.,0.978255169515729));
#30615=CARTESIAN_POINT('',(20.063221375429,0.,0.978255169515729));
#30616=CARTESIAN_POINT('Origin',(20.063221375429,0.,0.978255169515729));
#30617=CARTESIAN_POINT('',(20.063221375429,15.,0.));
#30618=CARTESIAN_POINT('',(20.063221375429,15.,4.23912758475787));
#30619=CARTESIAN_POINT('',(20.063221375429,495.,0.));
#30620=CARTESIAN_POINT('',(20.063221375429,495.,0.978255169515729));
#30621=CARTESIAN_POINT('',(20.063221375429,0.,0.));
#30622=CARTESIAN_POINT('Origin',(20.063221375429,0.,0.));
#30623=CARTESIAN_POINT('',(38.7183893122855,15.,0.));
#30624=CARTESIAN_POINT('',(15.,495.,0.));
#30625=CARTESIAN_POINT('Origin',(30.,0.,1.95651033903146));
#30626=CARTESIAN_POINT('',(25.0491683351188,15.,1.95651033903146));
#30627=CARTESIAN_POINT('',(22.5,15.,1.95651033903146));
#30628=CARTESIAN_POINT('',(25.0491683351188,495.,1.95651033903146));
#30629=CARTESIAN_POINT('',(36.9508316648812,495.,1.95651033903146));
#30630=CARTESIAN_POINT('',(25.0491683351188,0.,1.95651033903146));
#30631=CARTESIAN_POINT('Origin',(25.0491683351188,0.,1.95651033903146));
#30632=CARTESIAN_POINT('',(25.0491683351188,15.,6.95083166488121));
#30633=CARTESIAN_POINT('',(25.0491683351188,15.,4.72825516951573));
#30634=CARTESIAN_POINT('',(25.0491683351188,495.,6.95083166488121));
#30635=CARTESIAN_POINT('',(25.0491683351188,495.,6.95083166488121));
#30636=CARTESIAN_POINT('',(25.0491683351188,0.,6.95083166488121));
#30637=CARTESIAN_POINT('Origin',(25.0491683351188,0.,6.95083166488121));
#30638=CARTESIAN_POINT('',(24.3741039067251,15.,6.95083166488121));
#30639=CARTESIAN_POINT('',(20.0245841675594,15.,6.95083166488121));
#30640=CARTESIAN_POINT('',(24.3741039067251,495.,6.95083166488121));
#30641=CARTESIAN_POINT('',(23.0491683351188,495.,6.95083166488121));
#30642=CARTESIAN_POINT('',(24.3741039067251,0.,6.95083166488121));
#30643=CARTESIAN_POINT('Origin',(24.3741039067251,0.,6.95083166488121));
#30644=CARTESIAN_POINT('',(20.75,15.,10.6122749602376));
#30645=CARTESIAN_POINT('',(21.9173141859695,15.,9.43293385694831));
#30646=CARTESIAN_POINT('',(20.75,495.,10.6122749602376));
#30647=CARTESIAN_POINT('',(24.3741039067251,495.,6.95083166488121));
#30648=CARTESIAN_POINT('',(20.75,0.,10.6122749602376));
#30649=CARTESIAN_POINT('Origin',(1.89960608334138,0.,4.68145522242933));
#30650=CARTESIAN_POINT('',(1.39960608334138,15.,4.68145522242933));
#30651=CARTESIAN_POINT('Origin',(1.89960608334138,15.,4.68145522242933));
#30652=CARTESIAN_POINT('',(1.39960608334138,495.,4.68145522242933));
#30653=CARTESIAN_POINT('',(1.39960608334138,0.,4.68145522242933));
#30654=CARTESIAN_POINT('Origin',(1.89960608334138,495.,4.68145522242933));
#30655=CARTESIAN_POINT('Origin',(1.39960608334138,0.,1.81236459713887));
#30656=CARTESIAN_POINT('',(1.39960608334138,15.,1.81236459713887));
#30657=CARTESIAN_POINT('',(1.39960608334138,15.,4.65618229856943));
#30658=CARTESIAN_POINT('',(1.39960608334138,495.,1.81236459713887));
#30659=CARTESIAN_POINT('',(1.39960608334138,0.,1.81236459713887));
#30660=CARTESIAN_POINT('',(1.39960608334138,495.,1.81236459713887));
#30661=CARTESIAN_POINT('Origin',(1.89960608334138,0.,1.81236459713888));
#30662=CARTESIAN_POINT('',(1.89960608334138,15.,1.31236459713888));
#30663=CARTESIAN_POINT('Origin',(1.89960608334138,15.,1.81236459713888));
#30664=CARTESIAN_POINT('',(1.89960608334138,495.,1.31236459713888));
#30665=CARTESIAN_POINT('',(1.89960608334138,0.,1.31236459713888));
#30666=CARTESIAN_POINT('Origin',(1.89960608334138,495.,1.81236459713888));
#30667=CARTESIAN_POINT('Origin',(4.78668371362235,0.,1.31236459713888));
#30668=CARTESIAN_POINT('',(9.89334185681118,15.,1.31236459713888));
#30669=CARTESIAN_POINT('',(4.78668371362235,495.,1.31236459713888));
#30670=CARTESIAN_POINT('Origin',(10.715659452243,0.,9.25));
#30671=CARTESIAN_POINT('',(10.715659452243,15.,9.25));
#30672=CARTESIAN_POINT('',(12.8578297261215,15.,9.25));
#30673=CARTESIAN_POINT('',(10.715659452243,495.,9.25));
#30674=CARTESIAN_POINT('',(10.715659452243,0.,9.25));
#30675=CARTESIAN_POINT('',(9.25,495.,9.25));
#30676=CARTESIAN_POINT('Origin',(6.9508316648812,0.,5.44638293630937));
#30677=CARTESIAN_POINT('',(6.9508316648812,15.,5.44638293630937));
#30678=CARTESIAN_POINT('',(9.45587506218205,15.,7.97723596582758));
#30679=CARTESIAN_POINT('',(6.9508316648812,495.,5.44638293630937));
#30680=CARTESIAN_POINT('',(6.9508316648812,0.,5.44638293630937));
#30681=CARTESIAN_POINT('',(6.9508316648812,495.,5.44638293630937));
#30682=CARTESIAN_POINT('Origin',(6.9508316648812,0.,1.95651033903146));
#30683=CARTESIAN_POINT('',(6.9508316648812,15.,1.95651033903146));
#30684=CARTESIAN_POINT('',(6.9508316648812,15.,4.72825516951573));
#30685=CARTESIAN_POINT('',(6.9508316648812,495.,1.95651033903146));
#30686=CARTESIAN_POINT('',(6.9508316648812,0.,1.95651033903146));
#30687=CARTESIAN_POINT('',(6.9508316648812,495.,6.95083166488121));
#30688=CARTESIAN_POINT('Origin',(10.7975927840689,0.,1.95651033903146));
#30689=CARTESIAN_POINT('',(10.7975927840689,15.,1.95651033903146));
#30690=CARTESIAN_POINT('',(12.8987963920345,15.,1.95651033903146));
#30691=CARTESIAN_POINT('',(10.7975927840689,495.,1.95651033903146));
#30692=CARTESIAN_POINT('',(10.7975927840689,0.,1.95651033903146));
#30693=CARTESIAN_POINT('',(9.93677862457103,495.,1.95651033903146));
#30694=CARTESIAN_POINT('Origin',(10.7975927840689,0.,0.978255169515729));
#30695=CARTESIAN_POINT('',(10.7975927840689,15.,0.978255169515729));
#30696=CARTESIAN_POINT('',(10.7975927840689,15.,4.23912758475787));
#30697=CARTESIAN_POINT('',(10.7975927840689,495.,0.978255169515729));
#30698=CARTESIAN_POINT('',(10.7975927840689,0.,0.978255169515729));
#30699=CARTESIAN_POINT('',(10.7975927840689,495.,1.95651033903146));
#30700=CARTESIAN_POINT('Origin',(9.93677862457103,0.,0.978255169515729));
#30701=CARTESIAN_POINT('',(9.93677862457103,15.,0.978255169515729));
#30702=CARTESIAN_POINT('',(12.4683893122855,15.,0.978255169515729));
#30703=CARTESIAN_POINT('',(9.93677862457103,495.,0.978255169515729));
#30704=CARTESIAN_POINT('',(9.93677862457103,0.,0.978255169515729));
#30705=CARTESIAN_POINT('',(10.7975927840689,495.,0.978255169515729));
#30706=CARTESIAN_POINT('Origin',(9.93677862457103,0.,0.));
#30707=CARTESIAN_POINT('',(9.93677862457103,15.,0.));
#30708=CARTESIAN_POINT('',(9.93677862457103,15.,3.75));
#30709=CARTESIAN_POINT('',(9.93677862457103,495.,0.));
#30710=CARTESIAN_POINT('',(9.93677862457103,0.,0.));
#30711=CARTESIAN_POINT('',(9.93677862457103,495.,0.978255169515729));
#30712=CARTESIAN_POINT('Origin',(2.,0.,0.));
#30713=CARTESIAN_POINT('',(2.,15.,0.));
#30714=CARTESIAN_POINT('',(8.5,15.,0.));
#30715=CARTESIAN_POINT('',(2.,495.,0.));
#30716=CARTESIAN_POINT('',(2.,0.,0.));
#30717=CARTESIAN_POINT('',(15.,495.,0.));
#30718=CARTESIAN_POINT('Origin',(2.,0.,2.));
#30719=CARTESIAN_POINT('',(2.22044604925031E-15,15.,2.));
#30720=CARTESIAN_POINT('Origin',(2.,15.,2.));
#30721=CARTESIAN_POINT('',(2.22044604925031E-15,495.,2.));
#30722=CARTESIAN_POINT('',(2.4980018054066E-15,0.,2.));
#30723=CARTESIAN_POINT('Origin',(2.,495.,2.));
#30724=CARTESIAN_POINT('Origin',(-2.22044604925031E-15,0.,9.93677862457103));
#30725=CARTESIAN_POINT('',(-2.22044604925031E-15,15.,9.93677862457103));
#30726=CARTESIAN_POINT('',(-2.22044604925031E-15,15.,8.71838931228551));
#30727=CARTESIAN_POINT('',(-2.22044604925031E-15,495.,9.93677862457103));
#30728=CARTESIAN_POINT('',(-2.22044604925031E-15,0.,9.93677862457103));
#30729=CARTESIAN_POINT('',(-2.22044604925031E-15,495.,9.93677862457103));
#30730=CARTESIAN_POINT('Origin',(0.978255169515727,0.,9.93677862457103));
#30731=CARTESIAN_POINT('',(0.978255169515727,15.,9.93677862457103));
#30732=CARTESIAN_POINT('',(7.98912758475786,15.,9.93677862457103));
#30733=CARTESIAN_POINT('',(0.978255169515727,495.,9.93677862457103));
#30734=CARTESIAN_POINT('',(0.978255169515727,0.,9.93677862457103));
#30735=CARTESIAN_POINT('',(0.978255169515727,495.,9.93677862457103));
#30736=CARTESIAN_POINT('Origin',(0.978255169515725,0.,10.7975927840689));
#30737=CARTESIAN_POINT('',(0.978255169515725,15.,10.7975927840689));
#30738=CARTESIAN_POINT('',(0.978255169515729,15.,9.14879639203444));
#30739=CARTESIAN_POINT('',(0.978255169515725,495.,10.7975927840689));
#30740=CARTESIAN_POINT('',(0.978255169515725,0.,10.7975927840689));
#30741=CARTESIAN_POINT('',(0.978255169515725,495.,10.7975927840689));
#30742=CARTESIAN_POINT('Origin',(1.95651033903146,0.,10.7975927840689));
#30743=CARTESIAN_POINT('',(1.95651033903146,15.,10.7975927840689));
#30744=CARTESIAN_POINT('',(8.47825516951573,15.,10.7975927840689));
#30745=CARTESIAN_POINT('',(1.95651033903146,495.,10.7975927840689));
#30746=CARTESIAN_POINT('',(1.95651033903146,0.,10.7975927840689));
#30747=CARTESIAN_POINT('',(1.95651033903146,495.,10.7975927840689));
#30748=CARTESIAN_POINT('Origin',(1.95651033903146,0.,6.95083166488121));
#30749=CARTESIAN_POINT('',(1.95651033903146,15.,6.95083166488121));
#30750=CARTESIAN_POINT('',(1.95651033903146,15.,7.2254158324406));
#30751=CARTESIAN_POINT('',(1.95651033903146,495.,6.95083166488121));
#30752=CARTESIAN_POINT('',(1.95651033903146,0.,6.95083166488121));
#30753=CARTESIAN_POINT('',(1.95651033903146,495.,6.95083166488121));
#30754=CARTESIAN_POINT('Origin',(5.62589609327486,0.,6.95083166488121));
#30755=CARTESIAN_POINT('',(5.62589609327486,15.,6.95083166488121));
#30756=CARTESIAN_POINT('',(10.3129480466374,15.,6.95083166488121));
#30757=CARTESIAN_POINT('',(5.62589609327486,495.,6.95083166488121));
#30758=CARTESIAN_POINT('',(5.62589609327486,0.,6.95083166488121));
#30759=CARTESIAN_POINT('',(1.95651033903146,495.,6.95083166488121));
#30760=CARTESIAN_POINT('Origin',(9.25,0.,10.6122749602376));
#30761=CARTESIAN_POINT('',(9.25,15.,10.6122749602376));
#30762=CARTESIAN_POINT('',(9.89473776739309,15.,11.2636555046265));
#30763=CARTESIAN_POINT('',(9.25,495.,10.6122749602376));
#30764=CARTESIAN_POINT('',(9.25,0.,10.6122749602376));
#30765=CARTESIAN_POINT('',(5.62589609327486,495.,6.95083166488121));
#30766=CARTESIAN_POINT('Origin',(15.,15.,22.5));
#30767=CARTESIAN_POINT('',(20.063221375429,15.,30.));
#30768=CARTESIAN_POINT('',(38.7183893122855,15.,30.));
#30769=CARTESIAN_POINT('',(20.063221375429,15.,29.0217448304843));
#30770=CARTESIAN_POINT('',(20.063221375429,15.,25.7608724152421));
#30771=CARTESIAN_POINT('',(19.2024072159311,15.,29.0217448304843));
#30772=CARTESIAN_POINT('',(17.1012036079655,15.,29.0217448304843));
#30773=CARTESIAN_POINT('',(19.2024072159311,15.,28.0434896609685));
#30774=CARTESIAN_POINT('',(19.2024072159311,15.,25.2717448304843));
#30775=CARTESIAN_POINT('',(23.0491683351188,15.,28.0434896609685));
#30776=CARTESIAN_POINT('',(19.0245841675594,15.,28.0434896609685));
#30777=CARTESIAN_POINT('',(23.0491683351188,15.,24.5536170636906));
#30778=CARTESIAN_POINT('',(23.0491683351188,15.,23.5268085318453));
#30779=CARTESIAN_POINT('',(19.284340547757,15.,20.75));
#30780=CARTESIAN_POINT('',(18.661711044137,15.,20.1209555023271));
#30781=CARTESIAN_POINT('',(10.715659452243,15.,20.75));
#30782=CARTESIAN_POINT('',(12.8578297261215,15.,20.75));
#30783=CARTESIAN_POINT('',(6.9508316648812,15.,24.5536170636906));
#30784=CARTESIAN_POINT('',(9.45587506218205,15.,22.0227640341724));
#30785=CARTESIAN_POINT('',(6.9508316648812,15.,28.0434896609685));
#30786=CARTESIAN_POINT('',(6.9508316648812,15.,25.2717448304843));
#30787=CARTESIAN_POINT('',(10.7975927840689,15.,28.0434896609685));
#30788=CARTESIAN_POINT('',(12.8987963920345,15.,28.0434896609685));
#30789=CARTESIAN_POINT('',(10.7975927840689,15.,29.0217448304843));
#30790=CARTESIAN_POINT('',(10.7975927840689,15.,25.7608724152421));
#30791=CARTESIAN_POINT('',(9.93677862457103,15.,29.0217448304843));
#30792=CARTESIAN_POINT('',(12.4683893122855,15.,29.0217448304843));
#30793=CARTESIAN_POINT('',(9.93677862457103,15.,30.));
#30794=CARTESIAN_POINT('',(9.93677862457103,15.,26.25));
#30795=CARTESIAN_POINT('',(2.,15.,30.));
#30796=CARTESIAN_POINT('',(8.5,15.,30.));
#30797=CARTESIAN_POINT('',(2.22044604925031E-15,15.,28.));
#30798=CARTESIAN_POINT('Origin',(2.,15.,28.));
#30799=CARTESIAN_POINT('',(-2.22044604925031E-15,15.,20.063221375429));
#30800=CARTESIAN_POINT('',(-2.22044604925031E-15,15.,21.2816106877145));
#30801=CARTESIAN_POINT('',(0.978255169515727,15.,20.063221375429));
#30802=CARTESIAN_POINT('',(7.98912758475786,15.,20.063221375429));
#30803=CARTESIAN_POINT('',(0.978255169515725,15.,19.2024072159311));
#30804=CARTESIAN_POINT('',(0.978255169515729,15.,20.8512036079656));
#30805=CARTESIAN_POINT('',(1.95651033903146,15.,19.2024072159311));
#30806=CARTESIAN_POINT('',(8.47825516951573,15.,19.2024072159311));
#30807=CARTESIAN_POINT('',(1.95651033903146,15.,23.0491683351188));
#30808=CARTESIAN_POINT('',(1.95651033903146,15.,22.7745841675594));
#30809=CARTESIAN_POINT('',(5.62589609327486,15.,23.0491683351188));
#30810=CARTESIAN_POINT('',(10.3129480466374,15.,23.0491683351188));
#30811=CARTESIAN_POINT('',(9.25,15.,19.3877250397624));
#30812=CARTESIAN_POINT('',(9.89473776739309,15.,18.7363444953735));
#30813=CARTESIAN_POINT('',(9.25,15.,18.75));
#30814=CARTESIAN_POINT('',(20.75,15.,19.3877250397624));
#30815=CARTESIAN_POINT('',(20.75,15.,9.05613748011882));
#30816=CARTESIAN_POINT('',(24.3741039067251,15.,23.0491683351188));
#30817=CARTESIAN_POINT('',(21.9173141859695,15.,20.5670661430517));
#30818=CARTESIAN_POINT('',(25.0491683351188,15.,23.0491683351188));
#30819=CARTESIAN_POINT('',(20.0245841675594,15.,23.0491683351188));
#30820=CARTESIAN_POINT('',(25.0491683351188,15.,28.0434896609685));
#30821=CARTESIAN_POINT('',(25.0491683351188,15.,25.2717448304843));
#30822=CARTESIAN_POINT('',(22.5,15.,28.0434896609685));
#30823=CARTESIAN_POINT('',(5.28668371362235,15.,28.1876354028611));
#30824=CARTESIAN_POINT('',(4.78668371362235,15.,28.6876354028611));
#30825=CARTESIAN_POINT('Origin',(4.78668371362235,15.,28.1876354028611));
#30826=CARTESIAN_POINT('',(5.28668371362236,15.,25.3185447775707));
#30827=CARTESIAN_POINT('',(5.28668371362236,15.,23.9092723887853));
#30828=CARTESIAN_POINT('',(4.78668371362235,15.,24.8185447775707));
#30829=CARTESIAN_POINT('Origin',(4.78668371362236,15.,25.3185447775707));
#30830=CARTESIAN_POINT('',(1.89960608334138,15.,24.8185447775707));
#30831=CARTESIAN_POINT('',(8.44980304167069,15.,24.8185447775707));
#30832=CARTESIAN_POINT('',(1.39960608334138,15.,25.3185447775707));
#30833=CARTESIAN_POINT('Origin',(1.89960608334138,15.,25.3185447775707));
#30834=CARTESIAN_POINT('',(1.39960608334138,15.,28.1876354028611));
#30835=CARTESIAN_POINT('',(1.39960608334138,15.,25.3438177014306));
#30836=CARTESIAN_POINT('',(1.89960608334138,15.,28.6876354028611));
#30837=CARTESIAN_POINT('Origin',(1.89960608334138,15.,28.1876354028611));
#30838=CARTESIAN_POINT('',(9.89334185681118,15.,28.6876354028611));
#30839=CARTESIAN_POINT('',(11.75,15.,15.));
#30840=CARTESIAN_POINT('Origin',(15.,15.,15.));
#30841=CARTESIAN_POINT('Origin',(1.89960608334138,0.,24.8185447775707));
#30842=CARTESIAN_POINT('',(4.78668371362235,495.,24.8185447775707));
#30843=CARTESIAN_POINT('',(4.78668371362235,0.,24.8185447775707));
#30844=CARTESIAN_POINT('',(1.89960608334138,495.,24.8185447775707));
#30845=CARTESIAN_POINT('',(1.89960608334138,495.,24.8185447775707));
#30846=CARTESIAN_POINT('',(1.89960608334138,0.,24.8185447775707));
#30847=CARTESIAN_POINT('Origin',(4.78668371362236,0.,25.3185447775707));
#30848=CARTESIAN_POINT('',(5.28668371362236,495.,25.3185447775707));
#30849=CARTESIAN_POINT('',(5.28668371362236,0.,25.3185447775707));
#30850=CARTESIAN_POINT('Origin',(4.78668371362236,495.,25.3185447775707));
#30851=CARTESIAN_POINT('Origin',(5.28668371362236,0.,25.3185447775707));
#30852=CARTESIAN_POINT('',(5.28668371362235,495.,28.1876354028611));
#30853=CARTESIAN_POINT('',(5.28668371362235,0.,28.1876354028611));
#30854=CARTESIAN_POINT('',(5.28668371362236,495.,25.3185447775707));
#30855=CARTESIAN_POINT('Origin',(4.78668371362235,0.,28.1876354028611));
#30856=CARTESIAN_POINT('',(4.78668371362235,495.,28.6876354028611));
#30857=CARTESIAN_POINT('',(4.78668371362235,0.,28.6876354028611));
#30858=CARTESIAN_POINT('Origin',(4.78668371362235,495.,28.1876354028611));
#30859=CARTESIAN_POINT('Origin',(19.284340547757,0.,20.75));
#30860=CARTESIAN_POINT('',(23.0491683351188,495.,24.5536170636906));
#30861=CARTESIAN_POINT('',(23.0491683351188,0.,24.5536170636906));
#30862=CARTESIAN_POINT('',(19.284340547757,495.,20.75));
#30863=CARTESIAN_POINT('',(23.0491683351188,495.,24.5536170636906));
#30864=CARTESIAN_POINT('',(19.284340547757,0.,20.75));
#30865=CARTESIAN_POINT('Origin',(23.0491683351188,0.,24.5536170636906));
#30866=CARTESIAN_POINT('',(23.0491683351188,495.,28.0434896609685));
#30867=CARTESIAN_POINT('',(23.0491683351188,0.,28.0434896609685));
#30868=CARTESIAN_POINT('',(23.0491683351188,495.,23.0491683351188));
#30869=CARTESIAN_POINT('Origin',(23.0491683351188,0.,28.0434896609685));
#30870=CARTESIAN_POINT('',(19.2024072159311,495.,28.0434896609685));
#30871=CARTESIAN_POINT('',(19.2024072159311,0.,28.0434896609685));
#30872=CARTESIAN_POINT('',(23.0491683351188,495.,28.0434896609685));
#30873=CARTESIAN_POINT('Origin',(19.2024072159311,0.,28.0434896609685));
#30874=CARTESIAN_POINT('',(19.2024072159311,495.,29.0217448304843));
#30875=CARTESIAN_POINT('',(19.2024072159311,0.,29.0217448304843));
#30876=CARTESIAN_POINT('',(19.2024072159311,495.,28.0434896609685));
#30877=CARTESIAN_POINT('Origin',(19.2024072159311,0.,29.0217448304843));
#30878=CARTESIAN_POINT('',(20.063221375429,495.,29.0217448304843));
#30879=CARTESIAN_POINT('',(20.063221375429,0.,29.0217448304843));
#30880=CARTESIAN_POINT('',(19.2024072159311,495.,29.0217448304843));
#30881=CARTESIAN_POINT('Origin',(20.063221375429,0.,29.0217448304843));
#30882=CARTESIAN_POINT('',(20.063221375429,495.,30.));
#30883=CARTESIAN_POINT('',(20.063221375429,0.,30.));
#30884=CARTESIAN_POINT('',(20.063221375429,495.,29.0217448304843));
#30885=CARTESIAN_POINT('Origin',(20.063221375429,0.,30.));
#30886=CARTESIAN_POINT('',(15.,495.,30.));
#30887=CARTESIAN_POINT('Origin',(30.,0.,28.0434896609685));
#30888=CARTESIAN_POINT('',(25.0491683351188,495.,28.0434896609685));
#30889=CARTESIAN_POINT('',(25.0491683351188,0.,28.0434896609685));
#30890=CARTESIAN_POINT('',(36.9508316648812,495.,28.0434896609685));
#30891=CARTESIAN_POINT('Origin',(25.0491683351188,0.,28.0434896609685));
#30892=CARTESIAN_POINT('',(25.0491683351188,495.,23.0491683351188));
#30893=CARTESIAN_POINT('',(25.0491683351188,0.,23.0491683351188));
#30894=CARTESIAN_POINT('',(25.0491683351188,495.,23.0491683351188));
#30895=CARTESIAN_POINT('Origin',(25.0491683351188,0.,23.0491683351188));
#30896=CARTESIAN_POINT('',(24.3741039067251,495.,23.0491683351188));
#30897=CARTESIAN_POINT('',(24.3741039067251,0.,23.0491683351188));
#30898=CARTESIAN_POINT('',(23.0491683351188,495.,23.0491683351188));
#30899=CARTESIAN_POINT('Origin',(24.3741039067251,0.,23.0491683351188));
#30900=CARTESIAN_POINT('',(20.75,495.,19.3877250397624));
#30901=CARTESIAN_POINT('',(20.75,0.,19.3877250397624));
#30902=CARTESIAN_POINT('',(24.3741039067251,495.,23.0491683351188));
#30903=CARTESIAN_POINT('Origin',(20.75,0.,19.3877250397624));
#30904=CARTESIAN_POINT('',(20.75,495.,20.75));
#30905=CARTESIAN_POINT('Origin',(15.,0.,15.));
#30906=CARTESIAN_POINT('',(11.75,495.,15.));
#30907=CARTESIAN_POINT('Origin',(15.,495.,15.));
#30908=CARTESIAN_POINT('',(11.75,0.,15.));
#30909=CARTESIAN_POINT('Origin',(9.25,0.,15.));
#30910=CARTESIAN_POINT('',(9.25,495.,19.3877250397624));
#30911=CARTESIAN_POINT('',(9.25,0.,19.3877250397624));
#30912=CARTESIAN_POINT('',(9.25,495.,20.75));
#30913=CARTESIAN_POINT('Origin',(1.89960608334138,0.,25.3185447775707));
#30914=CARTESIAN_POINT('',(1.39960608334138,495.,25.3185447775707));
#30915=CARTESIAN_POINT('Origin',(1.89960608334138,495.,25.3185447775707));
#30916=CARTESIAN_POINT('',(1.39960608334138,0.,25.3185447775707));
#30917=CARTESIAN_POINT('Origin',(1.39960608334138,0.,28.1876354028611));
#30918=CARTESIAN_POINT('',(1.39960608334138,495.,28.1876354028611));
#30919=CARTESIAN_POINT('',(1.39960608334138,495.,28.1876354028611));
#30920=CARTESIAN_POINT('',(1.39960608334138,0.,28.1876354028611));
#30921=CARTESIAN_POINT('Origin',(1.89960608334138,0.,28.1876354028611));
#30922=CARTESIAN_POINT('',(1.89960608334138,495.,28.6876354028611));
#30923=CARTESIAN_POINT('Origin',(1.89960608334138,495.,28.1876354028611));
#30924=CARTESIAN_POINT('',(1.89960608334138,0.,28.6876354028611));
#30925=CARTESIAN_POINT('Origin',(4.78668371362235,0.,28.6876354028611));
#30926=CARTESIAN_POINT('',(4.78668371362235,495.,28.6876354028611));
#30927=CARTESIAN_POINT('Origin',(10.715659452243,0.,20.75));
#30928=CARTESIAN_POINT('',(10.715659452243,495.,20.75));
#30929=CARTESIAN_POINT('',(9.25,495.,20.75));
#30930=CARTESIAN_POINT('',(10.715659452243,0.,20.75));
#30931=CARTESIAN_POINT('Origin',(6.9508316648812,0.,24.5536170636906));
#30932=CARTESIAN_POINT('',(6.9508316648812,495.,24.5536170636906));
#30933=CARTESIAN_POINT('',(6.9508316648812,495.,24.5536170636906));
#30934=CARTESIAN_POINT('',(6.9508316648812,0.,24.5536170636906));
#30935=CARTESIAN_POINT('Origin',(6.9508316648812,0.,28.0434896609685));
#30936=CARTESIAN_POINT('',(6.9508316648812,495.,28.0434896609685));
#30937=CARTESIAN_POINT('',(6.9508316648812,495.,23.0491683351188));
#30938=CARTESIAN_POINT('',(6.9508316648812,0.,28.0434896609685));
#30939=CARTESIAN_POINT('Origin',(10.7975927840689,0.,28.0434896609685));
#30940=CARTESIAN_POINT('',(10.7975927840689,495.,28.0434896609685));
#30941=CARTESIAN_POINT('',(9.93677862457103,495.,28.0434896609685));
#30942=CARTESIAN_POINT('',(10.7975927840689,0.,28.0434896609685));
#30943=CARTESIAN_POINT('Origin',(10.7975927840689,0.,29.0217448304843));
#30944=CARTESIAN_POINT('',(10.7975927840689,495.,29.0217448304843));
#30945=CARTESIAN_POINT('',(10.7975927840689,495.,28.0434896609685));
#30946=CARTESIAN_POINT('',(10.7975927840689,0.,29.0217448304843));
#30947=CARTESIAN_POINT('Origin',(9.93677862457103,0.,29.0217448304843));
#30948=CARTESIAN_POINT('',(9.93677862457103,495.,29.0217448304843));
#30949=CARTESIAN_POINT('',(10.7975927840689,495.,29.0217448304843));
#30950=CARTESIAN_POINT('',(9.93677862457103,0.,29.0217448304843));
#30951=CARTESIAN_POINT('Origin',(9.93677862457103,0.,30.));
#30952=CARTESIAN_POINT('',(9.93677862457103,495.,30.));
#30953=CARTESIAN_POINT('',(9.93677862457103,495.,29.0217448304843));
#30954=CARTESIAN_POINT('',(9.93677862457103,0.,30.));
#30955=CARTESIAN_POINT('Origin',(2.,0.,30.));
#30956=CARTESIAN_POINT('',(2.,495.,30.));
#30957=CARTESIAN_POINT('',(15.,495.,30.));
#30958=CARTESIAN_POINT('',(2.,0.,30.));
#30959=CARTESIAN_POINT('Origin',(2.,0.,28.));
#30960=CARTESIAN_POINT('',(2.22044604925031E-15,495.,28.));
#30961=CARTESIAN_POINT('Origin',(2.,495.,28.));
#30962=CARTESIAN_POINT('',(2.4980018054066E-15,0.,28.));
#30963=CARTESIAN_POINT('Origin',(-2.22044604925031E-15,0.,20.063221375429));
#30964=CARTESIAN_POINT('',(-2.22044604925031E-15,495.,20.063221375429));
#30965=CARTESIAN_POINT('',(-2.22044604925031E-15,495.,20.063221375429));
#30966=CARTESIAN_POINT('',(-2.22044604925031E-15,0.,20.063221375429));
#30967=CARTESIAN_POINT('Origin',(0.978255169515727,0.,20.063221375429));
#30968=CARTESIAN_POINT('',(0.978255169515727,495.,20.063221375429));
#30969=CARTESIAN_POINT('',(0.978255169515727,495.,20.063221375429));
#30970=CARTESIAN_POINT('',(0.978255169515727,0.,20.063221375429));
#30971=CARTESIAN_POINT('Origin',(0.978255169515725,0.,19.2024072159311));
#30972=CARTESIAN_POINT('',(0.978255169515725,495.,19.2024072159311));
#30973=CARTESIAN_POINT('',(0.978255169515725,495.,19.2024072159311));
#30974=CARTESIAN_POINT('',(0.978255169515725,0.,19.2024072159311));
#30975=CARTESIAN_POINT('Origin',(1.95651033903146,0.,19.2024072159311));
#30976=CARTESIAN_POINT('',(1.95651033903146,495.,19.2024072159311));
#30977=CARTESIAN_POINT('',(1.95651033903146,495.,19.2024072159311));
#30978=CARTESIAN_POINT('',(1.95651033903146,0.,19.2024072159311));
#30979=CARTESIAN_POINT('Origin',(1.95651033903146,0.,23.0491683351188));
#30980=CARTESIAN_POINT('',(1.95651033903146,495.,23.0491683351188));
#30981=CARTESIAN_POINT('',(1.95651033903146,495.,23.0491683351188));
#30982=CARTESIAN_POINT('',(1.95651033903146,0.,23.0491683351188));
#30983=CARTESIAN_POINT('Origin',(5.62589609327486,0.,23.0491683351188));
#30984=CARTESIAN_POINT('',(5.62589609327486,495.,23.0491683351188));
#30985=CARTESIAN_POINT('',(1.95651033903146,495.,23.0491683351188));
#30986=CARTESIAN_POINT('',(5.62589609327486,0.,23.0491683351188));
#30987=CARTESIAN_POINT('Origin',(9.25,0.,19.3877250397624));
#30988=CARTESIAN_POINT('',(5.62589609327486,495.,23.0491683351188));
#30989=CARTESIAN_POINT('Origin',(15.,495.,22.5));
#48348=UNCERTAINTY_MEASURE_WITH_UNIT(LENGTH_MEASURE(0.01),#48370,
'DISTANCE_ACCURACY_VALUE',
'Maximum model space distance between geometric entities at asserted c
onnectivities');
#48356=UNCERTAINTY_MEASURE_WITH_UNIT(LENGTH_MEASURE(0.01),#48370,
'DISTANCE_ACCURACY_VALUE',
'Maximum model space distance between geometric entities at asserted c
onnectivities');
#48361=(
GEOMETRIC_REPRESENTATION_CONTEXT(3)
GLOBAL_UNCERTAINTY_ASSIGNED_CONTEXT((#48348))
GLOBAL_UNIT_ASSIGNED_CONTEXT((#48370,#48372,#48373))
REPRESENTATION_CONTEXT('','3D')
);
#48369=(
GEOMETRIC_REPRESENTATION_CONTEXT(3)
GLOBAL_UNCERTAINTY_ASSIGNED_CONTEXT((#48356))
GLOBAL_UNIT_ASSIGNED_CONTEXT((#48370,#48372,#48373))
REPRESENTATION_CONTEXT('','3D')
);
#48370=(
LENGTH_UNIT()
NAMED_UNIT(*)
SI_UNIT(.MILLI.,.METRE.)
);
#48372=(
NAMED_UNIT(*)
PLANE_ANGLE_UNIT()
SI_UNIT($,.RADIAN.)
);
#48373=(
NAMED_UNIT(*)
SI_UNIT($,.STERADIAN.)
SOLID_ANGLE_UNIT()
);
#48378=SHAPE_DEFINITION_REPRESENTATION(#48390,#48416);
#48390=PRODUCT_DEFINITION_SHAPE('',$,#48429);
#48416=SHAPE_REPRESENTATION('',(#21080),#48361);
#48424=PRODUCT_DEFINITION_CONTEXT('part definition',#48462,'design');
#48429=PRODUCT_DEFINITION('V_Slot','V_Slot',#48441,#48424);
#48441=PRODUCT_DEFINITION_FORMATION('',$,#48468);
#48462=APPLICATION_CONTEXT(
'Core Data for Automotive Mechanical Design Process');
#48463=PRODUCT_CONTEXT('part definition',#48462,'mechanical');
#48468=PRODUCT('V_Slot','V_Slot',$,(#48463));
#48525=COLOUR_RGB('Off White',0.89,0.88,0.83);
#48526=FILL_AREA_STYLE_COLOUR('',#48525);
#48527=FILL_AREA_STYLE('',(#48526));
#48528=SURFACE_STYLE_FILL_AREA(#48527);
#48529=SURFACE_SIDE_STYLE('',(#48528));
#48530=SURFACE_STYLE_USAGE(.BOTH.,#48529);
#48531=PRESENTATION_STYLE_ASSIGNMENT((#48530));
ENDSEC;
END-ISO-10303-21;
